ISO-10303-21;
HEADER;
FILE_DESCRIPTION (('STEP AP214'),
    '1' );
FILE_NAME ('small gear_ISO - Spur gear 2M 40T 20PA 10FW ---S40A75H50L20.0N.step',
    '2026-09-30T12:41:04',
    ( '' ),
    ( '' ),
    'SwSTEP 2.0',
    'SolidWorks 2026',
    '' );
FILE_SCHEMA (( 'AUTOMOTIVE_DESIGN' ));
ENDSEC;

DATA;
#1=AXIS2_PLACEMENT_3D ( 'NONE', #4503, #33619, #30682 ) ;
#3=DIRECTION ( 'NONE',  ( -1.000000000000000000, 0.000000000000000000, 0.000000000000000000 ) ) ;
#11=ORIENTED_EDGE ( 'NONE', *, *, #30239, .T. ) ;
#12=ORIENTED_EDGE ( 'NONE', *, *, #41227, .F. ) ;
#16=ADVANCED_FACE ( 'NONE', ( #23120 ), #30468, .T. ) ;
#20=VERTEX_POINT ( 'NONE', #356 ) ;
#40=AXIS2_PLACEMENT_3D ( 'NONE', #4431, #34260, #12011 ) ;
#42=DIRECTION ( 'NONE',  ( -1.000000000000000000, -0.000000000000000000, -0.000000000000000000 ) ) ;
#48=AXIS2_PLACEMENT_3D ( 'NONE', #27504, #9364, #31182 ) ;
#51=VECTOR ( 'NONE', #46939, 1000.000000000000000 ) ;
#60=ORIENTED_EDGE ( 'NONE', *, *, #2903, .T. ) ;
#67=ORIENTED_EDGE ( 'NONE', *, *, #48394, .T. ) ;
#69=CIRCLE ( 'NONE', #28969, 16.00000000000000000 ) ;
#72=VECTOR ( 'NONE', #4615, 1000.000000000000000 ) ;
#77=EDGE_CURVE ( 'NONE', #36483, #38214, #37203, .T. ) ;
#83=ORIENTED_EDGE ( 'NONE', *, *, #8742, .F. ) ;
#95=DIRECTION ( 'NONE',  ( 1.000000000000000000, -0.000000000000000000, -0.000000000000000000 ) ) ;
#97=FACE_OUTER_BOUND ( 'NONE', #38480, .T. ) ;
#98=EDGE_CURVE ( 'NONE', #12600, #11050, #41482, .T. ) ;
#102=CARTESIAN_POINT ( 'NONE',  ( 0.000000000000000000, -35.38097989696503021, -12.42422080174676147 ) ) ;
#104=ORIENTED_EDGE ( 'NONE', *, *, #8668, .T. ) ;
#111=AXIS2_PLACEMENT_3D ( 'NONE', #11902, #26827, #41763 ) ;
#113=EDGE_CURVE ( 'NONE', #23918, #3261, #44911, .T. ) ;
#125=ORIENTED_EDGE ( 'NONE', *, *, #42452, .T. ) ;
#126=CARTESIAN_POINT ( 'NONE',  ( 0.000000000000000000, 0.000000000000000000, 0.000000000000000000 ) ) ;
#132=PLANE ( 'NONE',  #10280 ) ;
#137=ORIENTED_EDGE ( 'NONE', *, *, #38242, .F. ) ;
#142=CARTESIAN_POINT ( 'NONE',  ( 10.00000000000000000, 9.188173127307898369, -40.98264845739739570 ) ) ;
#145=CARTESIAN_POINT ( 'NONE',  ( 0.000000000000000000, -27.13269053701078448, -25.88420570971428702 ) ) ;
#168=AXIS2_PLACEMENT_3D ( 'NONE', #35916, #17077, #34956 ) ;
#175=EDGE_LOOP ( 'NONE', ( #21889, #27226, #23925, #32939 ) ) ;
#180=DIRECTION ( 'NONE',  ( 0.000000000000000000, 0.000000000000000000, 1.000000000000000000 ) ) ;
#190=ORIENTED_EDGE ( 'NONE', *, *, #24530, .T. ) ;
#195=AXIS2_PLACEMENT_3D ( 'NONE', #12772, #42643, #24265 ) ;
#208=FACE_OUTER_BOUND ( 'NONE', #42941, .T. ) ;
#210=DIRECTION ( 'NONE',  ( 0.000000000000000000, 0.000000000000000000, 1.000000000000000000 ) ) ;
#213=LINE ( 'NONE', #34466, #35925 ) ;
#214=AXIS2_PLACEMENT_3D ( 'NONE', #47187, #31809, #24426 ) ;
#220=CYLINDRICAL_SURFACE ( 'NONE', #39354, 42.00000000000000000 ) ;
#229=LINE ( 'NONE', #34247, #6562 ) ;
#235=EDGE_LOOP ( 'NONE', ( #42907, #14172, #33989, #24634 ) ) ;
#236=AXIS2_PLACEMENT_3D ( 'NONE', #34388, #44950, #7968 ) ;
#243=EDGE_CURVE ( 'NONE', #41330, #45432, #37225, .T. ) ;
#263=ORIENTED_EDGE ( 'NONE', *, *, #42270, .F. ) ;
#267=CARTESIAN_POINT ( 'NONE',  ( 10.00000000000000000, -39.04073710021356192, 15.48615015657568250 ) ) ;
#268=CYLINDRICAL_SURFACE ( 'NONE', #17660, 42.00000000000000000 ) ;
#275=ADVANCED_FACE ( 'NONE', ( #40907 ), #7371, .T. ) ;
#281=EDGE_CURVE ( 'NONE', #11209, #5995, #44811, .T. ) ;
#288=DIRECTION ( 'NONE',  ( 0.000000000000000000, 0.000000000000000000, 1.000000000000000000 ) ) ;
#299=CARTESIAN_POINT ( 'NONE',  ( 10.00000000000000000, 0.000000000000000000, 37.49900000000000233 ) ) ;
#305=ORIENTED_EDGE ( 'NONE', *, *, #40170, .F. ) ;
#306=AXIS2_PLACEMENT_3D ( 'NONE', #44003, #15120, #25632 ) ;
#314=EDGE_LOOP ( 'NONE', ( #30103, #6984, #5328, #6114 ) ) ;
#336=CARTESIAN_POINT ( 'NONE',  ( 0.000000000000000000, 0.000000000000000000, 0.000000000000000000 ) ) ;
#337=VERTEX_POINT ( 'NONE', #15210 ) ;
#353=CIRCLE ( 'NONE', #5049, 42.00000000000000000 ) ;
#356=CARTESIAN_POINT ( 'NONE',  ( 10.00000000000000000, -41.91543099594816368, -2.663952781846588014 ) ) ;
#359=DIRECTION ( 'NONE',  ( -1.000000000000000000, 0.000000000000000000, 0.000000000000000000 ) ) ;
#364=CIRCLE ( 'NONE', #26154, 16.00000000000000355 ) ;
#374=DIRECTION ( 'NONE',  ( -1.000000000000000000, -0.000000000000000000, -0.000000000000000000 ) ) ;
#375=EDGE_LOOP ( 'NONE', ( #30574, #18631, #26654, #43679 ) ) ;
#379=ORIENTED_EDGE ( 'NONE', *, *, #23228, .F. ) ;
#383=ORIENTED_EDGE ( 'NONE', *, *, #20661, .T. ) ;
#389=DIRECTION ( 'NONE',  ( 0.000000000000000000, -0.9510565162951500895, -0.3090169943749581649 ) ) ;
#393=DIRECTION ( 'NONE',  ( -1.000000000000000000, 0.000000000000000000, -0.000000000000000000 ) ) ;
#409=VERTEX_POINT ( 'NONE', #38435 ) ;
#414=CARTESIAN_POINT ( 'NONE',  ( 0.000000000000000000, -0.8828120875898013420, -37.48860685352291711 ) ) ;
#418=CARTESIAN_POINT ( 'NONE',  ( 10.00000000000000000, 32.34446384430010113, -26.79245525562679831 ) ) ;
#428=AXIS2_PLACEMENT_3D ( 'NONE', #42188, #26543, #8177 ) ;
#429=ORIENTED_EDGE ( 'NONE', *, *, #45946, .F. ) ;
#435=CIRCLE ( 'NONE', #37935, 16.00000000000000000 ) ;
#447=ORIENTED_EDGE ( 'NONE', *, *, #24140, .T. ) ;
#451=VERTEX_POINT ( 'NONE', #26459 ) ;
#452=EDGE_LOOP ( 'NONE', ( #39151, #42607, #27629, #45892 ) ) ;
#456=EDGE_CURVE ( 'NONE', #8338, #715, #31710, .T. ) ;
#464=FACE_OUTER_BOUND ( 'NONE', #20083, .T. ) ;
#466=ORIENTED_EDGE ( 'NONE', *, *, #39065, .F. ) ;
#475=DIRECTION ( 'NONE',  ( -0.000000000000000000, 6.938893903907229364E-16, 1.000000000000000000 ) ) ;
#478=CARTESIAN_POINT ( 'NONE',  ( 0.000000000000000000, -37.22597642581153821, -5.202137450156795850 ) ) ;
#479=VECTOR ( 'NONE', #15922, 1000.000000000000000 ) ;
#500=VERTEX_POINT ( 'NONE', #16404 ) ;
#512=CYLINDRICAL_SURFACE ( 'NONE', #29821, 16.00000000000000000 ) ;
#516=CARTESIAN_POINT ( 'NONE',  ( 10.00000000000000000, 0.000000000000000000, 0.000000000000000000 ) ) ;
#519=ORIENTED_EDGE ( 'NONE', *, *, #3917, .T. ) ;
#522=CYLINDRICAL_SURFACE ( 'NONE', #3979, 16.00000000000000000 ) ;
#539=CARTESIAN_POINT ( 'NONE',  ( 0.000000000000000000, -6.555932627142676772, 37.01155633439056203 ) ) ;
#541=DIRECTION ( 'NONE',  ( -1.000000000000000000, -0.000000000000000000, 0.000000000000000000 ) ) ;
#547=ORIENTED_EDGE ( 'NONE', *, *, #34805, .F. ) ;
#549=EDGE_CURVE ( 'NONE', #46629, #10383, #44192, .T. ) ;
#552=CARTESIAN_POINT ( 'NONE',  ( 10.00000000000000000, 15.48615015657638239, -39.04073710021328480 ) ) ;
#553=ADVANCED_FACE ( 'NONE', ( #16645 ), #46266, .T. ) ;
#556=ORIENTED_EDGE ( 'NONE', *, *, #41925, .F. ) ;
#566=CARTESIAN_POINT ( 'NONE',  ( 5.000000000000000000, -39.04073710021332744, -15.48615015657624205 ) ) ;
#572=CARTESIAN_POINT ( 'NONE',  ( 0.000000000000000000, 35.92658777277525672, -10.74501242461245809 ) ) ;
#596=DIRECTION ( 'NONE',  ( -1.000000000000000000, -0.000000000000000000, -0.000000000000000000 ) ) ;
#597=CYLINDRICAL_SURFACE ( 'NONE', #16693, 16.00000000000000000 ) ;
#604=ADVANCED_FACE ( 'NONE', ( #14175 ), #10985, .T. ) ;
#615=ORIENTED_EDGE ( 'NONE', *, *, #34197, .T. ) ;
#616=ADVANCED_FACE ( 'NONE', ( #6592 ), #18570, .T. ) ;
#625=ORIENTED_EDGE ( 'NONE', *, *, #43707, .T. ) ;
#630=ORIENTED_EDGE ( 'NONE', *, *, #5378, .T. ) ;
#637=DIRECTION ( 'NONE',  ( -1.000000000000000000, 0.000000000000000000, 0.000000000000000000 ) ) ;
#640=DIRECTION ( 'NONE',  ( -1.000000000000000000, 0.000000000000000000, 0.000000000000000000 ) ) ;
#643=CARTESIAN_POINT ( 'NONE',  ( 5.000000000000000000, 39.04073710021366139, -15.48615015657542138 ) ) ;
#648=VERTEX_POINT ( 'NONE', #33003 ) ;
#660=EDGE_CURVE ( 'NONE', #19520, #43729, #39526, .T. ) ;
#661=EDGE_CURVE ( 'NONE', #30938, #23562, #21515, .T. ) ;
#662=PRESENTATION_STYLE_ASSIGNMENT (( #11926 ) ) ;
#665=ORIENTED_EDGE ( 'NONE', *, *, #3488, .F. ) ;
#670=DIRECTION ( 'NONE',  ( 0.000000000000000000, 0.8090169943749486725, -0.5877852522924713607 ) ) ;
#679=CARTESIAN_POINT ( 'NONE',  ( 0.000000000000000000, -37.16516213103273714, -4.992566952385376844 ) ) ;
#683=EDGE_LOOP ( 'NONE', ( #21682, #11838, #793, #16650 ) ) ;
#701=DIRECTION ( 'NONE',  ( -1.000000000000000000, -0.000000000000000000, -0.000000000000000000 ) ) ;
#710=VECTOR ( 'NONE', #35157, 1000.000000000000000 ) ;
#711=DIRECTION ( 'NONE',  ( -1.000000000000000000, 0.000000000000000000, -0.000000000000000000 ) ) ;
#713=ADVANCED_FACE ( 'NONE', ( #33259 ), #6835, .T. ) ;
#715=VERTEX_POINT ( 'NONE', #2662 ) ;
#716=CARTESIAN_POINT ( 'NONE',  ( 10.00000000000000000, -6.555932627142143865, -37.01155633439065440 ) ) ;
#726=CARTESIAN_POINT ( 'NONE',  ( 10.00000000000000000, 0.6853352020795618893, -37.58145647212453611 ) ) ;
#736=ORIENTED_EDGE ( 'NONE', *, *, #18878, .F. ) ;
#750=CYLINDRICAL_SURFACE ( 'NONE', #22884, 37.49900000000000233 ) ;
#754=CYLINDRICAL_SURFACE ( 'NONE', #7068, 42.00000000000000000 ) ;
#759=CARTESIAN_POINT ( 'NONE',  ( 10.00000000000000000, 6.555932627142952995, -37.01155633439051940 ) ) ;
#760=ORIENTED_EDGE ( 'NONE', *, *, #16844, .T. ) ;
#761=FACE_OUTER_BOUND ( 'NONE', #5201, .T. ) ;
#771=ORIENTED_EDGE ( 'NONE', *, *, #42514, .T. ) ;
#785=CIRCLE ( 'NONE', #47688, 16.00000000000000355 ) ;
#791=DIRECTION ( 'NONE',  ( -1.000000000000000000, 0.000000000000000000, 0.000000000000000000 ) ) ;
#793=ORIENTED_EDGE ( 'NONE', *, *, #14867, .F. ) ;
#796=ADVANCED_FACE ( 'NONE', ( #15397 ), #45242, .T. ) ;
#802=CARTESIAN_POINT ( 'NONE',  ( 10.00000000000000000, 22.64427369931212297, -30.00120703465181293 ) ) ;
#803=ORIENTED_EDGE ( 'NONE', *, *, #18055, .T. ) ;
#808=EDGE_CURVE ( 'NONE', #42195, #25666, #13500, .T. ) ;
#812=ORIENTED_EDGE ( 'NONE', *, *, #18312, .T. ) ;
#815=CARTESIAN_POINT ( 'NONE',  ( 10.00000000000000000, -12.26510123303234501, -35.53030884539098366 ) ) ;
#819=CIRCLE ( 'NONE', #2393, 16.00000000000000355 ) ;
#838=ORIENTED_EDGE ( 'NONE', *, *, #16567, .F. ) ;
#842=VERTEX_POINT ( 'NONE', #29823 ) ;
#858=CARTESIAN_POINT ( 'NONE',  ( 5.000000000000000000, 32.34446384430010113, -26.79245525562679831 ) ) ;
#881=DIRECTION ( 'NONE',  ( -1.000000000000000000, 0.000000000000000000, 0.000000000000000000 ) ) ;
#884=CARTESIAN_POINT ( 'NONE',  ( 10.00000000000000000, 37.22597642581158084, -5.202137450156524068 ) ) ;
#886=CARTESIAN_POINT ( 'NONE',  ( 10.00000000000000000, 0.000000000000000000, 0.000000000000000000 ) ) ;
#905=VECTOR ( 'NONE', #29776, 1000.000000000000000 ) ;
#908=VERTEX_POINT ( 'NONE', #20751 ) ;
#915=EDGE_CURVE ( 'NONE', #27090, #32864, #9476, .T. ) ;
#921=DIRECTION ( 'NONE',  ( -1.000000000000000000, 0.000000000000000000, 0.000000000000000000 ) ) ;
#929=VERTEX_POINT ( 'NONE', #43263 ) ;
#931=EDGE_CURVE ( 'NONE', #18736, #38437, #11161, .T. ) ;
#944=AXIS2_PLACEMENT_3D ( 'NONE', #4438, #29878, #37708 ) ;
#946=CARTESIAN_POINT ( 'NONE',  ( 10.00000000000000000, -37.58145647212455032, 16.68533520207890319 ) ) ;
#958=DIRECTION ( 'NONE',  ( 0.000000000000000000, 0.000000000000000000, 1.000000000000000000 ) ) ;
#966=CIRCLE ( 'NONE', #47104, 16.00000000000000000 ) ;
#968=EDGE_LOOP ( 'NONE', ( #45128, #38184, #40200, #11196 ) ) ;
#973=DIRECTION ( 'NONE',  ( -1.000000000000000000, 0.000000000000000000, -0.000000000000000000 ) ) ;
#978=EDGE_CURVE ( 'NONE', #43018, #47530, #46348, .T. ) ;
#982=DIRECTION ( 'NONE',  ( 0.000000000000000000, 0.000000000000000000, 1.000000000000000000 ) ) ;
#986=ORIENTED_EDGE ( 'NONE', *, *, #39691, .T. ) ;
#995=CIRCLE ( 'NONE', #22097, 37.49900000000000233 ) ;
#998=DIRECTION ( 'NONE',  ( 0.000000000000000000, 0.000000000000000000, 1.000000000000000000 ) ) ;
#1003=CARTESIAN_POINT ( 'NONE',  ( 10.00000000000000000, -21.53537804866058991, -30.80686688397033635 ) ) ;
#1010=DIRECTION ( 'NONE',  ( 0.000000000000000000, 0.7071067811865487940, -0.7071067811865462405 ) ) ;
#1014=CARTESIAN_POINT ( 'NONE',  ( 10.00000000000000000, -30.00120703465222149, 22.64427369931158296 ) ) ;
#1034=EDGE_CURVE ( 'NONE', #715, #25865, #46377, .T. ) ;
#1040=AXIS2_PLACEMENT_3D ( 'NONE', #40870, #18818, #15177 ) ;
#1053=LINE ( 'NONE', #30214, #3540 ) ;
#1075=CARTESIAN_POINT ( 'NONE',  ( 0.000000000000000000, 41.81611651403861885, 3.925862922256313503 ) ) ;
#1077=ORIENTED_EDGE ( 'NONE', *, *, #30969, .F. ) ;
#1084=ORIENTED_EDGE ( 'NONE', *, *, #24140, .F. ) ;
#1086=AXIS2_PLACEMENT_3D ( 'NONE', #36826, #38287, #19916 ) ;
#1096=AXIS2_PLACEMENT_3D ( 'NONE', #43302, #16385, #16157 ) ;
#1104=ADVANCED_FACE ( 'NONE', ( #15345 ), #8223, .T. ) ;
#1106=DIRECTION ( 'NONE',  ( -1.000000000000000000, -0.000000000000000000, -0.000000000000000000 ) ) ;
#1118=DIRECTION ( 'NONE',  ( 0.000000000000000000, 0.5877852522924685852, 0.8090169943749508930 ) ) ;
#1130=CIRCLE ( 'NONE', #35513, 16.00000000000000000 ) ;
#1133=DIRECTION ( 'NONE',  ( 0.000000000000000000, 1.000000000000000000, -9.787530781167596740E-16 ) ) ;
#1136=DIRECTION ( 'NONE',  ( -1.000000000000000000, -0.000000000000000000, 0.000000000000000000 ) ) ;
#1137=AXIS2_PLACEMENT_3D ( 'NONE', #6055, #21192, #2136 ) ;
#1150=EDGE_CURVE ( 'NONE', #40355, #10383, #4177, .T. ) ;
#1159=DIRECTION ( 'NONE',  ( 1.000000000000000000, -0.000000000000000000, -0.000000000000000000 ) ) ;
#1160=EDGE_LOOP ( 'NONE', ( #13684, #21800, #27783, #5983 ) ) ;
#1170=ORIENTED_EDGE ( 'NONE', *, *, #42785, .F. ) ;
#1188=DIRECTION ( 'NONE',  ( -1.000000000000000000, 0.000000000000000000, -0.000000000000000000 ) ) ;
#1191=CARTESIAN_POINT ( 'NONE',  ( 10.00000000000000000, -27.75498641678720446, -31.52238457039628727 ) ) ;
#1192=EDGE_LOOP ( 'NONE', ( #46128, #20788, #45078, #27773 ) ) ;
#1193=LINE ( 'NONE', #27150, #21499 ) ;
#1199=ORIENTED_EDGE ( 'NONE', *, *, #4695, .T. ) ;
#1203=CARTESIAN_POINT ( 'NONE',  ( 10.00000000000000000, 30.00120703465236716, -22.64427369931138756 ) ) ;
#1214=VERTEX_POINT ( 'NONE', #142 ) ;
#1218=DIRECTION ( 'NONE',  ( -1.000000000000000000, 0.000000000000000000, 0.000000000000000000 ) ) ;
#1228=ORIENTED_EDGE ( 'NONE', *, *, #26320, .T. ) ;
#1229=ORIENTED_EDGE ( 'NONE', *, *, #3126, .T. ) ;
#1242=CARTESIAN_POINT ( 'NONE',  ( 4.999999999999999112, -41.81611651403864727, 3.925862922256025289 ) ) ;
#1254=CARTESIAN_POINT ( 'NONE',  ( 10.00000000000000000, -37.22597642581153821, -5.202137450156795850 ) ) ;
#1266=AXIS2_PLACEMENT_3D ( 'NONE', #25808, #44665, #11863 ) ;
#1268=DIRECTION ( 'NONE',  ( -1.000000000000000000, 0.000000000000000000, 0.000000000000000000 ) ) ;
#1278=AXIS2_PLACEMENT_3D ( 'NONE', #25443, #22741, #38164 ) ;
#1282=LINE ( 'NONE', #16217, #3372 ) ;
#1294=DIRECTION ( 'NONE',  ( 0.000000000000000000, 0.000000000000000000, 1.000000000000000000 ) ) ;
#1295=VERTEX_POINT ( 'NONE', #5517 ) ;
#1301=EDGE_LOOP ( 'NONE', ( #26832, #25489, #4890, #25246 ) ) ;
#1304=CARTESIAN_POINT ( 'NONE',  ( 0.000000000000000000, -30.84782396557201878, -21.32104025579148399 ) ) ;
#1313=ORIENTED_EDGE ( 'NONE', *, *, #44195, .F. ) ;
#1344=EDGE_CURVE ( 'NONE', #45431, #43260, #12727, .T. ) ;
#1350=DIRECTION ( 'NONE',  ( 0.000000000000000000, 0.000000000000000000, 1.000000000000000000 ) ) ;
#1381=ADVANCED_FACE ( 'NONE', ( #38826 ), #8689, .T. ) ;
#1384=EDGE_CURVE ( 'NONE', #15972, #17779, #966, .T. ) ;
#1392=CYLINDRICAL_SURFACE ( 'NONE', #37281, 42.00000000000000000 ) ;
#1409=ORIENTED_EDGE ( 'NONE', *, *, #931, .T. ) ;
#1420=VERTEX_POINT ( 'NONE', #6899 ) ;
#1421=DIRECTION ( 'NONE',  ( -1.000000000000000000, 0.000000000000000000, -0.000000000000000000 ) ) ;
#1423=VERTEX_POINT ( 'NONE', #33566 ) ;
#1431=CIRCLE ( 'NONE', #28779, 37.49900000000000233 ) ;
#1432=ORIENTED_EDGE ( 'NONE', *, *, #14859, .T. ) ;
#1438=ORIENTED_EDGE ( 'NONE', *, *, #17894, .T. ) ;
#1443=LINE ( 'NONE', #16366, #8344 ) ;
#1449=DIRECTION ( 'NONE',  ( -1.000000000000000000, 0.000000000000000000, 0.000000000000000000 ) ) ;
#1475=ORIENTED_EDGE ( 'NONE', *, *, #34688, .F. ) ;
#1481=ORIENTED_EDGE ( 'NONE', *, *, #42174, .F. ) ;
#1493=VERTEX_POINT ( 'NONE', #267 ) ;
#1494=AXIS2_PLACEMENT_3D ( 'NONE', #35712, #39142, #34979 ) ;
#1504=DIRECTION ( 'NONE',  ( 1.000000000000000000, -0.000000000000000000, 0.000000000000000000 ) ) ;
#1512=ORIENTED_EDGE ( 'NONE', *, *, #36370, .F. ) ;
#1526=CIRCLE ( 'NONE', #9309, 16.00000000000000000 ) ;
#1546=VERTEX_POINT ( 'NONE', #22792 ) ;
#1549=DIRECTION ( 'NONE',  ( -1.000000000000000000, 0.000000000000000000, 0.000000000000000000 ) ) ;
#1551=EDGE_CURVE ( 'NONE', #4753, #40406, #3307, .T. ) ;
#1555=ORIENTED_EDGE ( 'NONE', *, *, #6304, .T. ) ;
#1569=DIRECTION ( 'NONE',  ( -1.000000000000000000, 0.000000000000000000, -0.000000000000000000 ) ) ;
#1578=ORIENTED_EDGE ( 'NONE', *, *, #36315, .T. ) ;
#1579=ADVANCED_FACE ( 'NONE', ( #12512 ), #750, .T. ) ;
#1607=DIRECTION ( 'NONE',  ( -1.000000000000000000, 0.000000000000000000, -0.000000000000000000 ) ) ;
#1614=DIRECTION ( 'NONE',  ( -1.000000000000000000, -0.000000000000000000, -0.000000000000000000 ) ) ;
#1623=DIRECTION ( 'NONE',  ( 0.000000000000000000, 0.9510565162951544194, -0.3090169943749446757 ) ) ;
#1635=AXIS2_PLACEMENT_3D ( 'NONE', #22052, #14967, #14730 ) ;
#1650=ORIENTED_EDGE ( 'NONE', *, *, #46870, .F. ) ;
#1659=AXIS2_PLACEMENT_3D ( 'NONE', #42605, #5164, #30612 ) ;
#1668=AXIS2_PLACEMENT_3D ( 'NONE', #30817, #1188, #34704 ) ;
#1669=EDGE_CURVE ( 'NONE', #17158, #45189, #41661, .T. ) ;
#1674=DIRECTION ( 'NONE',  ( -1.000000000000000000, 0.000000000000000000, 0.000000000000000000 ) ) ;
#1699=FACE_OUTER_BOUND ( 'NONE', #14844, .T. ) ;
#1709=ORIENTED_EDGE ( 'NONE', *, *, #13515, .T. ) ;
#1722=CYLINDRICAL_SURFACE ( 'NONE', #21208, 16.00000000000000000 ) ;
#1727=DIRECTION ( 'NONE',  ( -1.000000000000000000, 0.000000000000000000, 0.000000000000000000 ) ) ;
#1740=EDGE_CURVE ( 'NONE', #17387, #44456, #31511, .T. ) ;
#1742=VERTEX_POINT ( 'NONE', #16657 ) ;
#1744=CYLINDRICAL_SURFACE ( 'NONE', #9183, 16.00000000000000000 ) ;
#1748=CYLINDRICAL_SURFACE ( 'NONE', #28369, 16.00000000000000000 ) ;
#1760=CARTESIAN_POINT ( 'NONE',  ( 0.000000000000000000, -40.68715046381937128, 10.41901085202062660 ) ) ;
#1770=LINE ( 'NONE', #12079, #42258 ) ;
#1771=ORIENTED_EDGE ( 'NONE', *, *, #7716, .T. ) ;
#1782=ORIENTED_EDGE ( 'NONE', *, *, #1344, .T. ) ;
#1783=CARTESIAN_POINT ( 'NONE',  ( 10.00000000000000000, 0.000000000000000000, 0.000000000000000000 ) ) ;
#1786=EDGE_CURVE ( 'NONE', #32422, #1423, #2532, .T. ) ;
#1791=CARTESIAN_POINT ( 'NONE',  ( 0.000000000000000000, 4.992566952385522505, -37.16516213103271582 ) ) ;
#1803=DIRECTION ( 'NONE',  ( -1.000000000000000000, 0.000000000000000000, 0.000000000000000000 ) ) ;
#1807=DIRECTION ( 'NONE',  ( 0.000000000000000000, 0.000000000000000000, 1.000000000000000000 ) ) ;
#1814=ORIENTED_EDGE ( 'NONE', *, *, #30206, .T. ) ;
#1832=CIRCLE ( 'NONE', #47928, 16.00000000000000000 ) ;
#1863=EDGE_CURVE ( 'NONE', #14446, #12027, #33270, .T. ) ;
#1876=DIRECTION ( 'NONE',  ( -1.000000000000000000, -0.000000000000000000, -0.000000000000000000 ) ) ;
#1878=CIRCLE ( 'NONE', #33094, 15.99999999999999822 ) ;
#1893=AXIS2_PLACEMENT_3D ( 'NONE', #47498, #23248, #38180 ) ;
#1894=VECTOR ( 'NONE', #10151, 1000.000000000000000 ) ;
#1904=VERTEX_POINT ( 'NONE', #32771 ) ;
#1913=ORIENTED_EDGE ( 'NONE', *, *, #40170, .T. ) ;
#1916=AXIS2_PLACEMENT_3D ( 'NONE', #11727, #30565, #26658 ) ;
#1925=LINE ( 'NONE', #47175, #20453 ) ;
#1930=FACE_OUTER_BOUND ( 'NONE', #36547, .T. ) ;
#1931=ORIENTED_EDGE ( 'NONE', *, *, #7229, .F. ) ;
#1932=AXIS2_PLACEMENT_3D ( 'NONE', #20050, #1218, #9275 ) ;
#1938=CARTESIAN_POINT ( 'NONE',  ( 0.000000000000000000, -38.55633173626998911, -16.65560815589452304 ) ) ;
#1939=EDGE_LOOP ( 'NONE', ( #28039, #5808, #34501, #32987 ) ) ;
#1950=AXIS2_PLACEMENT_3D ( 'NONE', #23134, #30982, #41990 ) ;
#1962=VERTEX_POINT ( 'NONE', #1191 ) ;
#1981=CARTESIAN_POINT ( 'NONE',  ( 0.000000000000000000, 0.000000000000000000, 0.000000000000000000 ) ) ;
#1989=CARTESIAN_POINT ( 'NONE',  ( 10.00000000000000000, -17.80606268964563554, 33.00180498840040855 ) ) ;
#1990=DIRECTION ( 'NONE',  ( 0.000000000000000000, 0.000000000000000000, 1.000000000000000000 ) ) ;
#2015=ORIENTED_EDGE ( 'NONE', *, *, #11271, .F. ) ;
#2016=EDGE_CURVE ( 'NONE', #4600, #9305, #29864, .T. ) ;
#2017=ADVANCED_FACE ( 'NONE', ( #22732 ), #27148, .T. ) ;
#2028=CARTESIAN_POINT ( 'NONE',  ( 4.999999999999999112, -10.41901085202107247, 40.68715046381925049 ) ) ;
#2029=ORIENTED_EDGE ( 'NONE', *, *, #26470, .T. ) ;
#2057=CARTESIAN_POINT ( 'NONE',  ( 10.00000000000000000, -37.16516213103280108, 4.992566952384862589 ) ) ;
#2063=ORIENTED_EDGE ( 'NONE', *, *, #40414, .F. ) ;
#2078=EDGE_CURVE ( 'NONE', #20399, #7360, #12694, .T. ) ;
#2096=CARTESIAN_POINT ( 'NONE',  ( 10.00000000000000000, -30.80686688397025108, 21.53537804866070715 ) ) ;
#2099=FACE_OUTER_BOUND ( 'NONE', #23007, .T. ) ;
#2103=DIRECTION ( 'NONE',  ( 0.000000000000000000, 0.000000000000000000, 1.000000000000000000 ) ) ;
#2112=LINE ( 'NONE', #39305, #31826 ) ;
#2124=ORIENTED_EDGE ( 'NONE', *, *, #31457, .T. ) ;
#2131=ORIENTED_EDGE ( 'NONE', *, *, #23541, .F. ) ;
#2136=DIRECTION ( 'NONE',  ( 0.000000000000000000, 0.000000000000000000, 1.000000000000000000 ) ) ;
#2144=EDGE_CURVE ( 'NONE', #18005, #9046, #43272, .T. ) ;
#2147=ORIENTED_EDGE ( 'NONE', *, *, #24145, .F. ) ;
#2153=CARTESIAN_POINT ( 'NONE',  ( 0.000000000000000000, 0.000000000000000000, 0.000000000000000000 ) ) ;
#2160=DIRECTION ( 'NONE',  ( 0.000000000000000000, 1.000000000000000000, -9.787530781167596740E-16 ) ) ;
#2163=CIRCLE ( 'NONE', #3726, 16.00000000000000000 ) ;
#2166=CARTESIAN_POINT ( 'NONE',  ( 0.000000000000000000, -30.80686688397025108, 21.53537804866070715 ) ) ;
#2168=EDGE_CURVE ( 'NONE', #30556, #30938, #7704, .T. ) ;
#2174=EDGE_CURVE ( 'NONE', #19451, #30139, #42559, .T. ) ;
#2179=ORIENTED_EDGE ( 'NONE', *, *, #915, .T. ) ;
#2185=ADVANCED_FACE ( 'NONE', ( #1930 ), #23696, .T. ) ;
#2191=AXIS2_PLACEMENT_3D ( 'NONE', #17774, #25113, #43966 ) ;
#2203=DIRECTION ( 'NONE',  ( -1.000000000000000000, 0.000000000000000000, 0.000000000000000000 ) ) ;
#2233=AXIS2_PLACEMENT_3D ( 'NONE', #23529, #8371, #1010 ) ;
#2241=LINE ( 'NONE', #47040, #17217 ) ;
#2247=AXIS2_PLACEMENT_3D ( 'NONE', #27407, #16623, #38675 ) ;
#2255=FACE_OUTER_BOUND ( 'NONE', #46402, .T. ) ;
#2260=DIRECTION ( 'NONE',  ( 0.000000000000000000, 0.000000000000000000, -1.000000000000000000 ) ) ;
#2268=CARTESIAN_POINT ( 'NONE',  ( 10.00000000000000000, 31.52238457039638320, -27.75498641678709788 ) ) ;
#2274=CARTESIAN_POINT ( 'NONE',  ( 4.999999999999999112, 40.68715046381943523, -10.41901085202036370 ) ) ;
#2283=FACE_OUTER_BOUND ( 'NONE', #46818, .T. ) ;
#2326=CARTESIAN_POINT ( 'NONE',  ( 10.00000000000000000, 17.80606268964585226, -33.00180498840028775 ) ) ;
#2332=DIRECTION ( 'NONE',  ( -1.000000000000000000, -0.000000000000000000, 0.000000000000000000 ) ) ;
#2362=CARTESIAN_POINT ( 'NONE',  ( -10.00000000000000000, 0.000000000000000000, 0.000000000000000000 ) ) ;
#2375=CIRCLE ( 'NONE', #44593, 42.00000000000000000 ) ;
#2376=DIRECTION ( 'NONE',  ( 0.000000000000000000, 0.9876883405951372152, 0.1564344650402347547 ) ) ;
#2377=ORIENTED_EDGE ( 'NONE', *, *, #24833, .T. ) ;
#2384=CARTESIAN_POINT ( 'NONE',  ( 10.00000000000000000, 0.000000000000000000, 0.000000000000000000 ) ) ;
#2385=CARTESIAN_POINT ( 'NONE',  ( 10.00000000000000000, 33.17418723428307459, 17.67226234102837878 ) ) ;
#2389=DIRECTION ( 'NONE',  ( 0.000000000000000000, 0.000000000000000000, 1.000000000000000000 ) ) ;
#2393=AXIS2_PLACEMENT_3D ( 'NONE', #2429, #31848, #46521 ) ;
#2400=DIRECTION ( 'NONE',  ( -1.000000000000000000, 0.000000000000000000, 0.000000000000000000 ) ) ;
#2408=CIRCLE ( 'NONE', #35224, 42.00000000000000000 ) ;
#2420=ORIENTED_EDGE ( 'NONE', *, *, #13114, .F. ) ;
#2429=CARTESIAN_POINT ( 'NONE',  ( 10.00000000000000000, 26.08949754953024325, 27.05870788708241648 ) ) ;
#2430=CARTESIAN_POINT ( 'NONE',  ( 10.00000000000000000, 0.000000000000000000, 0.000000000000000000 ) ) ;
#2431=ORIENTED_EDGE ( 'NONE', *, *, #6410, .T. ) ;
#2435=CARTESIAN_POINT ( 'NONE',  ( 10.00000000000000000, 37.58145647212453611, 0.6853352020791767529 ) ) ;
#2442=MANIFOLD_SOLID_BREP ( 'Cut-Extrude-Thin1', #16878 ) ;
#2444=AXIS2_PLACEMENT_3D ( 'NONE', #43405, #2751, #17684 ) ;
#2445=EDGE_CURVE ( 'NONE', #36248, #6463, #16891, .T. ) ;
#2456=VECTOR ( 'NONE', #28329, 1000.000000000000000 ) ;
#2457=VERTEX_POINT ( 'NONE', #16795 ) ;
#2458=ORIENTED_EDGE ( 'NONE', *, *, #31194, .F. ) ;
#2472=EDGE_CURVE ( 'NONE', #22056, #34741, #12989, .T. ) ;
#2483=ORIENTED_EDGE ( 'NONE', *, *, #34708, .F. ) ;
#2501=ORIENTED_EDGE ( 'NONE', *, *, #9994, .T. ) ;
#2507=CARTESIAN_POINT ( 'NONE',  ( 10.00000000000000000, 37.22597642581158084, 10.79786254984347593 ) ) ;
#2509=CARTESIAN_POINT ( 'NONE',  ( 10.00000000000000000, 33.79645857604513992, 16.45098606841138178 ) ) ;
#2532=CIRCLE ( 'NONE', #47890, 37.49900000000000233 ) ;
#2552=CARTESIAN_POINT ( 'NONE',  ( 10.00000000000000000, 0.000000000000000000, 0.000000000000000000 ) ) ;
#2578=ORIENTED_EDGE ( 'NONE', *, *, #27544, .F. ) ;
#2579=ORIENTED_EDGE ( 'NONE', *, *, #14247, .F. ) ;
#2605=DIRECTION ( 'NONE',  ( -1.000000000000000000, 0.000000000000000000, 0.000000000000000000 ) ) ;
#2634=VERTEX_POINT ( 'NONE', #47122 ) ;
#2637=CARTESIAN_POINT ( 'NONE',  ( 10.00000000000000000, -30.80686688397025108, 21.53537804866070715 ) ) ;
#2654=CARTESIAN_POINT ( 'NONE',  ( 10.00000000000000000, 38.55633173627010990, 16.65560815589424593 ) ) ;
#2662=CARTESIAN_POINT ( 'NONE',  ( 0.000000000000000000, -35.38097989696520074, 12.42422080174625520 ) ) ;
#2663=LINE ( 'NONE', #3382, #4109 ) ;
#2665=ORIENTED_EDGE ( 'NONE', *, *, #27099, .F. ) ;
#2673=FACE_OUTER_BOUND ( 'NONE', #4889, .T. ) ;
#2675=EDGE_LOOP ( 'NONE', ( #36426, #6545, #28197, #36081 ) ) ;
#2680=FACE_OUTER_BOUND ( 'NONE', #8736, .T. ) ;
#2693=CARTESIAN_POINT ( 'NONE',  ( 0.000000000000000000, 0.000000000000000000, 0.000000000000000000 ) ) ;
#2700=AXIS2_PLACEMENT_3D ( 'NONE', #32093, #39688, #43351 ) ;
#2710=ADVANCED_FACE ( 'NONE', ( #15045 ), #26777, .T. ) ;
#2711=LINE ( 'NONE', #14217, #21010 ) ;
#2714=CARTESIAN_POINT ( 'NONE',  ( 0.000000000000000000, 0.000000000000000000, 0.000000000000000000 ) ) ;
#2715=ORIENTED_EDGE ( 'NONE', *, *, #36049, .F. ) ;
#2726=ORIENTED_EDGE ( 'NONE', *, *, #10122, .T. ) ;
#2731=CARTESIAN_POINT ( 'NONE',  ( 0.000000000000000000, 0.000000000000000000, 0.000000000000000000 ) ) ;
#2751=DIRECTION ( 'NONE',  ( -1.000000000000000000, 0.000000000000000000, -0.000000000000000000 ) ) ;
#2760=VERTEX_POINT ( 'NONE', #44900 ) ;
#2764=EDGE_CURVE ( 'NONE', #19937, #13075, #48223, .T. ) ;
#2767=CARTESIAN_POINT ( 'NONE',  ( 0.000000000000000000, 12.26510123303308752, -35.53030884539072787 ) ) ;
#2773=CIRCLE ( 'NONE', #12965, 37.49900000000000944 ) ;
#2777=ORIENTED_EDGE ( 'NONE', *, *, #7716, .F. ) ;
#2779=AXIS2_PLACEMENT_3D ( 'NONE', #32071, #13221, #27668 ) ;
#2784=ORIENTED_EDGE ( 'NONE', *, *, #42154, .F. ) ;
#2798=CARTESIAN_POINT ( 'NONE',  ( 0.000000000000000000, 3.925862922256769583, -41.81611651403857621 ) ) ;
#2810=AXIS2_PLACEMENT_3D ( 'NONE', #35956, #6352, #39660 ) ;
#2815=DIRECTION ( 'NONE',  ( 0.000000000000000000, 0.000000000000000000, 1.000000000000000000 ) ) ;
#2843=AXIS2_PLACEMENT_3D ( 'NONE', #759, #37983, #23289 ) ;
#2845=VERTEX_POINT ( 'NONE', #23838 ) ;
#2859=CYLINDRICAL_SURFACE ( 'NONE', #6123, 16.00000000000000000 ) ;
#2862=FACE_OUTER_BOUND ( 'NONE', #40045, .T. ) ;
#2872=CARTESIAN_POINT ( 'NONE',  ( 10.00000000000000000, 0.000000000000000000, 0.000000000000000000 ) ) ;
#2875=EDGE_CURVE ( 'NONE', #2760, #26919, #28001, .T. ) ;
#2876=EDGE_LOOP ( 'NONE', ( #10804, #35963, #16596, #630 ) ) ;
#2885=AXIS2_PLACEMENT_3D ( 'NONE', #23459, #1449, #38402 ) ;
#2886=DIRECTION ( 'NONE',  ( 0.000000000000000000, 0.5877852522924684742, 0.8090169943749506709 ) ) ;
#2899=ORIENTED_EDGE ( 'NONE', *, *, #33085, .T. ) ;
#2903=EDGE_CURVE ( 'NONE', #35831, #42467, #7939, .T. ) ;
#2910=CIRCLE ( 'NONE', #37334, 42.00000000000000000 ) ;
#2912=CARTESIAN_POINT ( 'NONE',  ( 10.00000000000000000, 17.80606268964540462, 33.00180498840053644 ) ) ;
#2918=DIRECTION ( 'NONE',  ( -1.000000000000000000, 0.000000000000000000, -0.000000000000000000 ) ) ;
#2923=DIRECTION ( 'NONE',  ( -1.000000000000000000, 0.000000000000000000, -0.000000000000000000 ) ) ;
#2933=AXIS2_PLACEMENT_3D ( 'NONE', #25449, #40403, #6862 ) ;
#2934=CARTESIAN_POINT ( 'NONE',  ( 0.000000000000000000, -15.48615015657556171, -39.04073710021360455 ) ) ;
#2949=CARTESIAN_POINT ( 'NONE',  ( 0.000000000000000000, 16.23288003029497162, 33.80338159004289622 ) ) ;
#2956=CARTESIAN_POINT ( 'NONE',  ( 5.000000000000000000, 26.79245525562762253, -32.34446384429941901 ) ) ;
#2968=AXIS2_PLACEMENT_3D ( 'NONE', #44954, #21942, #11439 ) ;
#2987=EDGE_CURVE ( 'NONE', #35465, #17019, #42641, .T. ) ;
#2990=CARTESIAN_POINT ( 'NONE',  ( 10.00000000000000000, 0.000000000000000000, 0.000000000000000000 ) ) ;
#2996=DIRECTION ( 'NONE',  ( -1.000000000000000000, -0.000000000000000000, -0.000000000000000000 ) ) ;
#3002=EDGE_CURVE ( 'NONE', #26893, #20243, #36046, .T. ) ;
#3005=ORIENTED_EDGE ( 'NONE', *, *, #42514, .F. ) ;
#3010=EDGE_CURVE ( 'NONE', #37417, #9289, #43436, .T. ) ;
#3018=LINE ( 'NONE', #18181, #11722 ) ;
#3026=DIRECTION ( 'NONE',  ( -1.000000000000000000, -0.000000000000000000, 0.000000000000000000 ) ) ;
#3028=DIRECTION ( 'NONE',  ( -1.000000000000000000, 0.000000000000000000, 0.000000000000000000 ) ) ;
#3033=ORIENTED_EDGE ( 'NONE', *, *, #10122, .F. ) ;
#3039=DIRECTION ( 'NONE',  ( -1.000000000000000000, 0.000000000000000000, -0.000000000000000000 ) ) ;
#3043=CARTESIAN_POINT ( 'NONE',  ( 10.00000000000000000, 0.000000000000000000, 0.000000000000000000 ) ) ;
#3057=EDGE_LOOP ( 'NONE', ( #18396, #24074, #32245, #32297 ) ) ;
#3079=CYLINDRICAL_SURFACE ( 'NONE', #19589, 42.00000000000000000 ) ;
#3085=DIRECTION ( 'NONE',  ( 0.000000000000000000, 0.8090169943749487835, -0.5877852522924713607 ) ) ;
#3094=DIRECTION ( 'NONE',  ( 0.000000000000000000, 0.000000000000000000, 1.000000000000000000 ) ) ;
#3109=CIRCLE ( 'NONE', #5469, 15.99999999999999822 ) ;
#3115=ORIENTED_EDGE ( 'NONE', *, *, #19580, .F. ) ;
#3117=AXIS2_PLACEMENT_3D ( 'NONE', #23505, #3948, #19823 ) ;
#3126=EDGE_CURVE ( 'NONE', #2457, #30556, #23794, .T. ) ;
#3128=EDGE_CURVE ( 'NONE', #23303, #17771, #36305, .T. ) ;
#3135=EDGE_LOOP ( 'NONE', ( #40906, #2458, #14966, #16279 ) ) ;
#3150=AXIS2_PLACEMENT_3D ( 'NONE', #24004, #42608, #13461 ) ;
#3157=DIRECTION ( 'NONE',  ( -1.000000000000000000, 0.000000000000000000, -0.000000000000000000 ) ) ;
#3162=CARTESIAN_POINT ( 'NONE',  ( 4.999999999999999112, 10.41901085202135491, -40.68715046381917944 ) ) ;
#3167=ORIENTED_EDGE ( 'NONE', *, *, #3588, .T. ) ;
#3170=VECTOR ( 'NONE', #9899, 1000.000000000000000 ) ;
#3179=EDGE_CURVE ( 'NONE', #27388, #4066, #15762, .T. ) ;
#3195=ORIENTED_EDGE ( 'NONE', *, *, #9994, .F. ) ;
#3208=ORIENTED_EDGE ( 'NONE', *, *, #20823, .F. ) ;
#3215=LINE ( 'NONE', #21342, #8642 ) ;
#3217=EDGE_LOOP ( 'NONE', ( #2015, #40552, #32867, #25486 ) ) ;
#3238=LINE ( 'NONE', #14273, #29209 ) ;
#3261=VERTEX_POINT ( 'NONE', #32035 ) ;
#3266=DIRECTION ( 'NONE',  ( -1.000000000000000000, 0.000000000000000000, -0.000000000000000000 ) ) ;
#3276=DIRECTION ( 'NONE',  ( -1.000000000000000000, 0.000000000000000000, 0.000000000000000000 ) ) ;
#3284=AXIS2_PLACEMENT_3D ( 'NONE', #45795, #22777, #18851 ) ;
#3289=DIRECTION ( 'NONE',  ( 1.000000000000000000, -0.000000000000000000, -0.000000000000000000 ) ) ;
#3301=ORIENTED_EDGE ( 'NONE', *, *, #3582, .F. ) ;
#3306=AXIS2_PLACEMENT_3D ( 'NONE', #44125, #47324, #25259 ) ;
#3307=CIRCLE ( 'NONE', #36917, 16.00000000000000000 ) ;
#3310=EDGE_CURVE ( 'NONE', #24385, #34476, #34560, .T. ) ;
#3312=VECTOR ( 'NONE', #40845, 1000.000000000000000 ) ;
#3318=ORIENTED_EDGE ( 'NONE', *, *, #25893, .T. ) ;
#3321=CYLINDRICAL_SURFACE ( 'NONE', #2191, 37.49900000000000233 ) ;
#3332=CYLINDRICAL_SURFACE ( 'NONE', #4548, 16.00000000000000000 ) ;
#3338=ADVANCED_FACE ( 'NONE', ( #10467 ), #44479, .T. ) ;
#3361=ORIENTED_EDGE ( 'NONE', *, *, #38679, .T. ) ;
#3372=VECTOR ( 'NONE', #31147, 1000.000000000000000 ) ;
#3376=VERTEX_POINT ( 'NONE', #22208 ) ;
#3378=CIRCLE ( 'NONE', #47929, 37.49900000000000944 ) ;
#3381=DIRECTION ( 'NONE',  ( 0.000000000000000000, -0.8910065241883722287, 0.4539904997395382558 ) ) ;
#3382=CARTESIAN_POINT ( 'NONE',  ( 10.00000000000000000, -0.8828120875898013420, -37.48860685352291711 ) ) ;
#3384=ORIENTED_EDGE ( 'NONE', *, *, #1786, .T. ) ;
#3397=CARTESIAN_POINT ( 'NONE',  ( 10.00000000000000000, -12.42422080174614862, -35.38097989696524337 ) ) ;
#3404=ADVANCED_FACE ( 'NONE', ( #25388 ), #25144, .T. ) ;
#3407=VERTEX_POINT ( 'NONE', #25628 ) ;
#3448=DIRECTION ( 'NONE',  ( 1.000000000000000000, -0.000000000000000000, -0.000000000000000000 ) ) ;
#3449=ORIENTED_EDGE ( 'NONE', *, *, #10331, .T. ) ;
#3451=FACE_OUTER_BOUND ( 'NONE', #39530, .T. ) ;
#3458=LINE ( 'NONE', #21592, #35763 ) ;
#3462=CARTESIAN_POINT ( 'NONE',  ( -10.00000000000000000, 0.000000000000000000, 0.000000000000000000 ) ) ;
#3465=EDGE_CURVE ( 'NONE', #39693, #12539, #43541, .T. ) ;
#3488=EDGE_CURVE ( 'NONE', #27073, #16066, #23196, .T. ) ;
#3490=CIRCLE ( 'NONE', #7364, 42.00000000000000000 ) ;
#3496=VERTEX_POINT ( 'NONE', #23646 ) ;
#3529=ORIENTED_EDGE ( 'NONE', *, *, #42664, .F. ) ;
#3531=ADVANCED_FACE ( 'NONE', ( #19476 ), #41783, .T. ) ;
#3540=VECTOR ( 'NONE', #44889, 1000.000000000000000 ) ;
#3549=DIRECTION ( 'NONE',  ( 0.000000000000000000, 0.000000000000000000, 1.000000000000000000 ) ) ;
#3553=AXIS2_PLACEMENT_3D ( 'NONE', #27076, #5036, #19953 ) ;
#3554=AXIS2_PLACEMENT_3D ( 'NONE', #29583, #36446, #33492 ) ;
#3560=VECTOR ( 'NONE', #13337, 1000.000000000000000 ) ;
#3570=EDGE_LOOP ( 'NONE', ( #17424, #665, #3936, #21252 ) ) ;
#3577=VERTEX_POINT ( 'NONE', #418 ) ;
#3582=EDGE_CURVE ( 'NONE', #15492, #39405, #39644, .T. ) ;
#3584=CARTESIAN_POINT ( 'NONE',  ( 10.00000000000000000, -27.05870788708213226, -26.08949754953053102 ) ) ;
#3588=EDGE_CURVE ( 'NONE', #21447, #15966, #2112, .T. ) ;
#3590=CARTESIAN_POINT ( 'NONE',  ( 0.000000000000000000, -16.23288003029473359, -33.80338159004301701 ) ) ;
#3602=AXIS2_PLACEMENT_3D ( 'NONE', #20362, #20135, #9355 ) ;
#3630=AXIS2_PLACEMENT_3D ( 'NONE', #16180, #19345, #34759 ) ;
#3633=EDGE_LOOP ( 'NONE', ( #28091, #37120, #25456, #4239 ) ) ;
#3640=DIRECTION ( 'NONE',  ( -1.000000000000000000, -0.000000000000000000, -0.000000000000000000 ) ) ;
#3643=EDGE_CURVE ( 'NONE', #47876, #27745, #24775, .T. ) ;
#3649=ORIENTED_EDGE ( 'NONE', *, *, #45761, .F. ) ;
#3652=LINE ( 'NONE', #18582, #13691 ) ;
#3664=LINE ( 'NONE', #15176, #46557 ) ;
#3667=DIRECTION ( 'NONE',  ( 1.000000000000000000, 0.000000000000000000, 0.000000000000000000 ) ) ;
#3686=VERTEX_POINT ( 'NONE', #13359 ) ;
#3699=DIRECTION ( 'NONE',  ( -1.000000000000000000, 0.000000000000000000, 0.000000000000000000 ) ) ;
#3702=DIRECTION ( 'NONE',  ( 0.000000000000000000, -0.7071067811865535679, 0.7071067811865413555 ) ) ;
#3705=ORIENTED_EDGE ( 'NONE', *, *, #12403, .F. ) ;
#3709=EDGE_CURVE ( 'NONE', #21714, #6290, #24016, .T. ) ;
#3712=CYLINDRICAL_SURFACE ( 'NONE', #28490, 42.00000000000000000 ) ;
#3713=EDGE_CURVE ( 'NONE', #20060, #11606, #11510, .T. ) ;
#3718=DIRECTION ( 'NONE',  ( -1.000000000000000000, 0.000000000000000000, 0.000000000000000000 ) ) ;
#3721=FACE_OUTER_BOUND ( 'NONE', #27692, .T. ) ;
#3722=DIRECTION ( 'NONE',  ( -1.000000000000000000, -0.000000000000000000, -0.000000000000000000 ) ) ;
#3725=ADVANCED_FACE ( 'NONE', ( #23900 ), #5302, .T. ) ;
#3726=AXIS2_PLACEMENT_3D ( 'NONE', #37620, #1136, #15587 ) ;
#3728=CYLINDRICAL_SURFACE ( 'NONE', #15160, 42.00000000000000000 ) ;
#3746=CARTESIAN_POINT ( 'NONE',  ( 10.00000000000000000, -3.925862922256464493, 41.81611651403861174 ) ) ;
#3765=DIRECTION ( 'NONE',  ( -1.000000000000000000, -0.000000000000000000, 0.000000000000000000 ) ) ;
#3768=CARTESIAN_POINT ( 'NONE',  ( 10.00000000000000000, 35.38097989696528600, -12.42422080174602605 ) ) ;
#3773=DIRECTION ( 'NONE',  ( -1.000000000000000000, -0.000000000000000000, 0.000000000000000000 ) ) ;
#3783=LINE ( 'NONE', #30700, #28598 ) ;
#3786=DIRECTION ( 'NONE',  ( 0.000000000000000000, 0.000000000000000000, -1.000000000000000000 ) ) ;
#3799=EDGE_LOOP ( 'NONE', ( #1084, #12084, #25830, #4015 ) ) ;
#3812=ORIENTED_EDGE ( 'NONE', *, *, #8759, .T. ) ;
#3814=ORIENTED_EDGE ( 'NONE', *, *, #38294, .T. ) ;
#3815=EDGE_CURVE ( 'NONE', #18791, #43612, #32507, .T. ) ;
#3819=DIRECTION ( 'NONE',  ( -1.000000000000000000, 0.000000000000000000, -0.000000000000000000 ) ) ;
#3821=ORIENTED_EDGE ( 'NONE', *, *, #45248, .F. ) ;
#3824=CARTESIAN_POINT ( 'NONE',  ( 0.000000000000000000, -21.53537804866103045, 30.80686688397002371 ) ) ;
#3825=ORIENTED_EDGE ( 'NONE', *, *, #40768, .F. ) ;
#3826=DIRECTION ( 'NONE',  ( -1.000000000000000000, 0.000000000000000000, 0.000000000000000000 ) ) ;
#3828=DIRECTION ( 'NONE',  ( 0.000000000000000000, 0.000000000000000000, 1.000000000000000000 ) ) ;
#3834=AXIS2_PLACEMENT_3D ( 'NONE', #7185, #44876, #19397 ) ;
#3843=CARTESIAN_POINT ( 'NONE',  ( 0.000000000000000000, 35.47612816024556537, -22.48208911017461631 ) ) ;
#3858=VECTOR ( 'NONE', #34524, 1000.000000000000000 ) ;
#3871=EDGE_CURVE ( 'NONE', #42217, #21692, #3783, .T. ) ;
#3874=CARTESIAN_POINT ( 'NONE',  ( 0.000000000000000000, 22.74946021919175720, -29.81001611430984255 ) ) ;
#3893=VERTEX_POINT ( 'NONE', #102 ) ;
#3903=CARTESIAN_POINT ( 'NONE',  ( 0.000000000000000000, 21.53537804866126137, -30.80686688396986028 ) ) ;
#3907=CARTESIAN_POINT ( 'NONE',  ( 0.000000000000000000, -36.88895765772628010, -6.736453364083947015 ) ) ;
#3917=EDGE_CURVE ( 'NONE', #14446, #11050, #46596, .T. ) ;
#3922=EDGE_CURVE ( 'NONE', #13075, #13054, #45378, .T. ) ;
#3927=ORIENTED_EDGE ( 'NONE', *, *, #28049, .F. ) ;
#3930=ORIENTED_EDGE ( 'NONE', *, *, #27422, .T. ) ;
#3936=ORIENTED_EDGE ( 'NONE', *, *, #20497, .F. ) ;
#3939=DIRECTION ( 'NONE',  ( -1.000000000000000000, -0.000000000000000000, -0.000000000000000000 ) ) ;
#3948=DIRECTION ( 'NONE',  ( -1.000000000000000000, 0.000000000000000000, 0.000000000000000000 ) ) ;
#3951=CARTESIAN_POINT ( 'NONE',  ( 10.00000000000000000, -17.80606268964563554, 33.00180498840040855 ) ) ;
#3955=ORIENTED_EDGE ( 'NONE', *, *, #931, .F. ) ;
#3963=DIRECTION ( 'NONE',  ( 0.000000000000000000, -0.1564344650402380854, 0.9876883405951365491 ) ) ;
#3965=DIRECTION ( 'NONE',  ( 0.000000000000000000, -0.5877852522924801315, 0.8090169943749421222 ) ) ;
#3969=CARTESIAN_POINT ( 'NONE',  ( 5.000000000000000000, -26.79245525562690844, -32.34446384430000876 ) ) ;
#3979=AXIS2_PLACEMENT_3D ( 'NONE', #41632, #11306, #8098 ) ;
#3989=EDGE_CURVE ( 'NONE', #37838, #23605, #39576, .T. ) ;
#3990=CARTESIAN_POINT ( 'NONE',  ( 0.000000000000000000, 0.000000000000000000, 0.000000000000000000 ) ) ;
#3994=CARTESIAN_POINT ( 'NONE',  ( 0.000000000000000000, -4.992566952385247170, 37.16516213103275845 ) ) ;
#3996=CIRCLE ( 'NONE', #6338, 42.00000000000000000 ) ;
#4000=CARTESIAN_POINT ( 'NONE',  ( 10.00000000000000000, 0.000000000000000000, 0.000000000000000000 ) ) ;
#4006=DIRECTION ( 'NONE',  ( 0.000000000000000000, 0.000000000000000000, 1.000000000000000000 ) ) ;
#4010=CARTESIAN_POINT ( 'NONE',  ( 0.000000000000000000, -35.92658777277502935, -10.74501242461320594 ) ) ;
#4015=ORIENTED_EDGE ( 'NONE', *, *, #34966, .F. ) ;
#4023=DIRECTION ( 'NONE',  ( -1.000000000000000000, 0.000000000000000000, 0.000000000000000000 ) ) ;
#4024=LINE ( 'NONE', #19186, #23518 ) ;
#4033=DIRECTION ( 'NONE',  ( -1.000000000000000000, -0.000000000000000000, -0.000000000000000000 ) ) ;
#4034=VECTOR ( 'NONE', #30035, 1000.000000000000000 ) ;
#4050=FACE_OUTER_BOUND ( 'NONE', #41755, .T. ) ;
#4066=VERTEX_POINT ( 'NONE', #23323 ) ;
#4077=AXIS2_PLACEMENT_3D ( 'NONE', #10397, #33627, #14071 ) ;
#4079=ORIENTED_EDGE ( 'NONE', *, *, #27813, .F. ) ;
#4081=DIRECTION ( 'NONE',  ( 1.000000000000000000, 0.000000000000000000, 0.000000000000000000 ) ) ;
#4101=( LENGTH_UNIT ( ) NAMED_UNIT ( * ) SI_UNIT ( .MILLI., .METRE. ) );
#4109=VECTOR ( 'NONE', #28632, 1000.000000000000000 ) ;
#4114=EDGE_CURVE ( 'NONE', #43888, #24385, #40368, .T. ) ;
#4122=ORIENTED_EDGE ( 'NONE', *, *, #4208, .T. ) ;
#4124=FACE_OUTER_BOUND ( 'NONE', #1301, .T. ) ;
#4135=DIRECTION ( 'NONE',  ( -1.000000000000000000, 0.000000000000000000, 0.000000000000000000 ) ) ;
#4172=FACE_OUTER_BOUND ( 'NONE', #23018, .T. ) ;
#4174=VECTOR ( 'NONE', #47882, 1000.000000000000000 ) ;
#4175=ORIENTED_EDGE ( 'NONE', *, *, #32777, .T. ) ;
#4177=CIRCLE ( 'NONE', #236, 42.00000000000000000 ) ;
#4181=AXIS2_PLACEMENT_3D ( 'NONE', #33462, #14866, #29784 ) ;
#4182=CYLINDRICAL_SURFACE ( 'NONE', #40, 16.00000000000000000 ) ;
#4188=DIRECTION ( 'NONE',  ( 0.000000000000000000, 0.1564344650402312298, -0.9876883405951375483 ) ) ;
#4193=ORIENTED_EDGE ( 'NONE', *, *, #24021, .F. ) ;
#4208=EDGE_CURVE ( 'NONE', #16066, #29887, #46815, .T. ) ;
#4216=EDGE_CURVE ( 'NONE', #6463, #24385, #6414, .T. ) ;
#4239=ORIENTED_EDGE ( 'NONE', *, *, #16396, .T. ) ;
#4248=CARTESIAN_POINT ( 'NONE',  ( 10.00000000000000000, 26.08949754953024325, 27.05870788708241648 ) ) ;
#4250=AXIS2_PLACEMENT_3D ( 'NONE', #44664, #48098, #3786 ) ;
#4265=AXIS2_PLACEMENT_3D ( 'NONE', #12951, #701, #45992 ) ;
#4274=CYLINDRICAL_SURFACE ( 'NONE', #41734, 37.49900000000000233 ) ;
#4281=CARTESIAN_POINT ( 'NONE',  ( 4.999999999999999112, -36.13751322684434797, 21.40280677340357940 ) ) ;
#4297=ORIENTED_EDGE ( 'NONE', *, *, #18834, .F. ) ;
#4303=AXIS2_PLACEMENT_3D ( 'NONE', #34770, #31120, #46043 ) ;
#4312=VERTEX_POINT ( 'NONE', #18128 ) ;
#4318=EDGE_LOOP ( 'NONE', ( #29922, #37525, #7279, #34533 ) ) ;
#4320=DIRECTION ( 'NONE',  ( 0.000000000000000000, 0.4539904997395479702, -0.8910065241883673437 ) ) ;
#4322=EDGE_CURVE ( 'NONE', #26338, #45549, #11539, .T. ) ;
#4326=CARTESIAN_POINT ( 'NONE',  ( 10.00000000000000000, -35.53030884539094103, 12.26510123303246935 ) ) ;
#4331=CARTESIAN_POINT ( 'NONE',  ( 0.000000000000000000, 0.000000000000000000, 0.000000000000000000 ) ) ;
#4363=CARTESIAN_POINT ( 'NONE',  ( 0.000000000000000000, -22.48208911017525580, 35.47612816024516036 ) ) ;
#4380=CARTESIAN_POINT ( 'NONE',  ( -10.00000000000000000, 0.000000000000000000, 0.000000000000000000 ) ) ;
#4391=ADVANCED_FACE ( 'NONE', ( #3451 ), #44572, .T. ) ;
#4400=CARTESIAN_POINT ( 'NONE',  ( 0.000000000000000000, -10.96151621346461447, -35.95386929396268272 ) ) ;
#4402=CARTESIAN_POINT ( 'NONE',  ( 0.000000000000000000, 17.80606268964585226, -33.00180498840028775 ) ) ;
#4403=CARTESIAN_POINT ( 'NONE',  ( 0.000000000000000000, 16.95692799528845640, -1.176623242955009039E-14 ) ) ;
#4431=CARTESIAN_POINT ( 'NONE',  ( 10.00000000000000000, -33.17418723428294669, -17.67226234102862747 ) ) ;
#4434=CARTESIAN_POINT ( 'NONE',  ( 10.00000000000000000, -27.13269053701078448, -25.88420570971428702 ) ) ;
#4438=CARTESIAN_POINT ( 'NONE',  ( 10.00000000000000000, 17.67226234102874116, -33.17418723428288274 ) ) ;
#4440=EDGE_CURVE ( 'NONE', #28690, #40406, #45856, .T. ) ;
#4442=EDGE_CURVE ( 'NONE', #24728, #1214, #31019, .T. ) ;
#4458=EDGE_CURVE ( 'NONE', #7133, #3407, #42325, .T. ) ;
#4463=CARTESIAN_POINT ( 'NONE',  ( 10.00000000000000000, -6.555932627142143865, -37.01155633439065440 ) ) ;
#4465=FACE_OUTER_BOUND ( 'NONE', #23033, .T. ) ;
#4482=EDGE_CURVE ( 'NONE', #19357, #46202, #25095, .T. ) ;
#4503=CARTESIAN_POINT ( 'NONE',  ( 10.00000000000000000, 0.000000000000000000, 0.000000000000000000 ) ) ;
#4505=ORIENTED_EDGE ( 'NONE', *, *, #37871, .T. ) ;
#4509=CARTESIAN_POINT ( 'NONE',  ( 10.00000000000000000, -27.13269053701078448, -25.88420570971428702 ) ) ;
#4517=DIRECTION ( 'NONE',  ( -1.000000000000000000, 0.000000000000000000, -0.000000000000000000 ) ) ;
#4531=EDGE_CURVE ( 'NONE', #41093, #39281, #15932, .T. ) ;
#4535=ADVANCED_FACE ( 'NONE', ( #4902 ), #1722, .T. ) ;
#4541=ORIENTED_EDGE ( 'NONE', *, *, #14278, .F. ) ;
#4546=DIRECTION ( 'NONE',  ( -1.000000000000000000, 0.000000000000000000, -0.000000000000000000 ) ) ;
#4548=AXIS2_PLACEMENT_3D ( 'NONE', #3584, #44227, #3828 ) ;
#4573=VECTOR ( 'NONE', #16287, 1000.000000000000000 ) ;
#4578=CARTESIAN_POINT ( 'NONE',  ( 10.00000000000000000, -27.05870788708213226, -26.08949754953053102 ) ) ;
#4594=ORIENTED_EDGE ( 'NONE', *, *, #19715, .F. ) ;
#4600=VERTEX_POINT ( 'NONE', #28635 ) ;
#4615=DIRECTION ( 'NONE',  ( -1.000000000000000000, 0.000000000000000000, 0.000000000000000000 ) ) ;
#4632=DIRECTION ( 'NONE',  ( -1.000000000000000000, -0.000000000000000000, -0.000000000000000000 ) ) ;
#4643=ORIENTED_EDGE ( 'NONE', *, *, #44488, .T. ) ;
#4653=AXIS2_PLACEMENT_3D ( 'NONE', #30400, #45310, #41903 ) ;
#4655=ORIENTED_EDGE ( 'NONE', *, *, #21828, .F. ) ;
#4657=LINE ( 'NONE', #4894, #479 ) ;
#4658=ORIENTED_EDGE ( 'NONE', *, *, #660, .T. ) ;
#4661=CIRCLE ( 'NONE', #26546, 15.99999999999999822 ) ;
#4670=DIRECTION ( 'NONE',  ( -1.000000000000000000, -0.000000000000000000, 0.000000000000000000 ) ) ;
#4695=EDGE_CURVE ( 'NONE', #31823, #8701, #43099, .T. ) ;
#4698=DIRECTION ( 'NONE',  ( 0.000000000000000000, -0.9510565162951565288, 0.3090169943749383474 ) ) ;
#4701=CARTESIAN_POINT ( 'NONE',  ( 10.00000000000000000, -35.95386929396264009, 10.96151621346475658 ) ) ;
#4705=ORIENTED_EDGE ( 'NONE', *, *, #12030, .T. ) ;
#4709=AXIS2_PLACEMENT_3D ( 'NONE', #2731, #40195, #6892 ) ;
#4715=LINE ( 'NONE', #31405, #16439 ) ;
#4721=DIRECTION ( 'NONE',  ( 0.000000000000000000, 0.9876883405951382144, -0.1564344650402276493 ) ) ;
#4735=CARTESIAN_POINT ( 'NONE',  ( 0.000000000000000000, -12.26510123303234501, -35.53030884539098366 ) ) ;
#4739=VECTOR ( 'NONE', #1727, 1000.000000000000000 ) ;
#4753=VERTEX_POINT ( 'NONE', #30021 ) ;
#4754=ORIENTED_EDGE ( 'NONE', *, *, #243, .F. ) ;
#4767=AXIS2_PLACEMENT_3D ( 'NONE', #336, #41701, #7451 ) ;
#4773=CIRCLE ( 'NONE', #32146, 37.49900000000001654 ) ;
#4792=CARTESIAN_POINT ( 'NONE',  ( 10.00000000000000000, -9.188173127307592836, 40.98264845739746676 ) ) ;
#4820=( LENGTH_UNIT ( ) NAMED_UNIT ( * ) SI_UNIT ( .MILLI., .METRE. ) );
#4823=EDGE_CURVE ( 'NONE', #34476, #39757, #10279, .T. ) ;
#4824=ORIENTED_EDGE ( 'NONE', *, *, #6916, .T. ) ;
#4837=VECTOR ( 'NONE', #6489, 1000.000000000000000 ) ;
#4844=ORIENTED_EDGE ( 'NONE', *, *, #8392, .F. ) ;
#4864=CARTESIAN_POINT ( 'NONE',  ( 10.00000000000000000, -6.736453364083292428, -36.88895765772640800 ) ) ;
#4865=CARTESIAN_POINT ( 'NONE',  ( 10.00000000000000000, -29.81001611431024756, 22.74946021919122785 ) ) ;
#4871=AXIS2_PLACEMENT_3D ( 'NONE', #16549, #43695, #2815 ) ;
#4873=DIRECTION ( 'NONE',  ( -1.000000000000000000, 0.000000000000000000, 0.000000000000000000 ) ) ;
#4875=AXIS2_PLACEMENT_3D ( 'NONE', #9527, #5391, #9065 ) ;
#4882=CYLINDRICAL_SURFACE ( 'NONE', #1932, 16.00000000000000000 ) ;
#4886=ORIENTED_EDGE ( 'NONE', *, *, #41076, .F. ) ;
#4889=EDGE_LOOP ( 'NONE', ( #10513, #1409, #16048, #42720 ) ) ;
#4890=ORIENTED_EDGE ( 'NONE', *, *, #7931, .T. ) ;
#4891=AXIS2_PLACEMENT_3D ( 'NONE', #39505, #47777, #5977 ) ;
#4894=CARTESIAN_POINT ( 'NONE',  ( 10.00000000000000000, 33.80338159004307386, -16.23288003029461279 ) ) ;
#4902=FACE_OUTER_BOUND ( 'NONE', #44494, .T. ) ;
#4906=CARTESIAN_POINT ( 'NONE',  ( 10.00000000000000000, -37.22597642581161637, 5.202137450156258502 ) ) ;
#4910=ORIENTED_EDGE ( 'NONE', *, *, #32592, .F. ) ;
#4920=FACE_OUTER_BOUND ( 'NONE', #15500, .T. ) ;
#4928=ADVANCED_FACE ( 'NONE', ( #5519 ), #42972, .T. ) ;
#4940=AXIS2_PLACEMENT_3D ( 'NONE', #41287, #18985, #11903 ) ;
#4943=EDGE_CURVE ( 'NONE', #409, #47967, #28268, .T. ) ;
#4945=ORIENTED_EDGE ( 'NONE', *, *, #31457, .F. ) ;
#4989=CARTESIAN_POINT ( 'NONE',  ( 0.000000000000000000, -16.65560815589383381, -38.55633173627028754 ) ) ;
#4994=CARTESIAN_POINT ( 'NONE',  ( 0.000000000000000000, -37.22597642581153821, 10.79786254984320415 ) ) ;
#5002=FACE_OUTER_BOUND ( 'NONE', #22421, .T. ) ;
#5005=AXIS2_PLACEMENT_3D ( 'NONE', #46124, #16501, #31696 ) ;
#5015=CYLINDRICAL_SURFACE ( 'NONE', #40909, 16.00000000000000000 ) ;
#5022=ORIENTED_EDGE ( 'NONE', *, *, #14302, .T. ) ;
#5028=DIRECTION ( 'NONE',  ( 0.000000000000000000, 0.000000000000000000, 1.000000000000000000 ) ) ;
#5035=EDGE_CURVE ( 'NONE', #26639, #46150, #40019, .T. ) ;
#5036=DIRECTION ( 'NONE',  ( -1.000000000000000000, -0.000000000000000000, -0.000000000000000000 ) ) ;
#5039=DIRECTION ( 'NONE',  ( -1.000000000000000000, -0.000000000000000000, 0.000000000000000000 ) ) ;
#5042=CARTESIAN_POINT ( 'NONE',  ( 10.00000000000000000, 30.84782396557248418, -21.32104025579081252 ) ) ;
#5049=AXIS2_PLACEMENT_3D ( 'NONE', #43091, #31858, #42366 ) ;
#5052=SURFACE_SIDE_STYLE ('',( #23638 ) ) ;
#5057=FACE_OUTER_BOUND ( 'NONE', #9709, .T. ) ;
#5062=ORIENTED_EDGE ( 'NONE', *, *, #20283, .F. ) ;
#5064=CIRCLE ( 'NONE', #25336, 16.00000000000000355 ) ;
#5068=CIRCLE ( 'NONE', #27632, 42.00000000000000000 ) ;
#5072=AXIS2_PLACEMENT_3D ( 'NONE', #32900, #14070, #14312 ) ;
#5079=VECTOR ( 'NONE', #35197, 1000.000000000000000 ) ;
#5081=AXIS2_PLACEMENT_3D ( 'NONE', #41460, #33859, #15285 ) ;
#5082=FACE_OUTER_BOUND ( 'NONE', #24638, .T. ) ;
#5101=ORIENTED_EDGE ( 'NONE', *, *, #17391, .T. ) ;
#5104=CARTESIAN_POINT ( 'NONE',  ( 10.00000000000000000, 35.92658777277511462, 10.74501242461295014 ) ) ;
#5107=ORIENTED_EDGE ( 'NONE', *, *, #660, .F. ) ;
#5127=DIRECTION ( 'NONE',  ( 0.000000000000000000, 0.000000000000000000, 1.000000000000000000 ) ) ;
#5136=DIRECTION ( 'NONE',  ( 0.000000000000000000, 0.000000000000000000, -1.000000000000000000 ) ) ;
#5157=CARTESIAN_POINT ( 'NONE',  ( 10.00000000000000000, -21.32104025579135964, 30.84782396557210760 ) ) ;
#5161=CARTESIAN_POINT ( 'NONE',  ( 0.000000000000000000, -17.67226234102801286, -33.17418723428327354 ) ) ;
#5163=ORIENTED_EDGE ( 'NONE', *, *, #21586, .F. ) ;
#5164=DIRECTION ( 'NONE',  ( -1.000000000000000000, -0.000000000000000000, -0.000000000000000000 ) ) ;
#5165=ORIENTED_EDGE ( 'NONE', *, *, #34918, .T. ) ;
#5166=DIRECTION ( 'NONE',  ( 0.000000000000000000, -0.8090169943749531134, 0.5877852522924653655 ) ) ;
#5181=DIRECTION ( 'NONE',  ( -1.000000000000000000, -0.000000000000000000, -0.000000000000000000 ) ) ;
#5198=DIRECTION ( 'NONE',  ( -1.000000000000000000, -0.000000000000000000, -0.000000000000000000 ) ) ;
#5201=EDGE_LOOP ( 'NONE', ( #47018, #15746, #13501, #36436 ) ) ;
#5203=EDGE_CURVE ( 'NONE', #46629, #9112, #14898, .T. ) ;
#5205=DIRECTION ( 'NONE',  ( 0.000000000000000000, 0.000000000000000000, 1.000000000000000000 ) ) ;
#5214=ADVANCED_FACE ( 'NONE', ( #14793 ), #23335, .T. ) ;
#5228=DIRECTION ( 'NONE',  ( -1.000000000000000000, 0.000000000000000000, -0.000000000000000000 ) ) ;
#5236=ORIENTED_EDGE ( 'NONE', *, *, #808, .T. ) ;
#5245=DIRECTION ( 'NONE',  ( 0.000000000000000000, 0.000000000000000000, 1.000000000000000000 ) ) ;
#5246=AXIS2_PLACEMENT_3D ( 'NONE', #24682, #42570, #17087 ) ;
#5250=ORIENTED_EDGE ( 'NONE', *, *, #33958, .T. ) ;
#5252=AXIS2_PLACEMENT_3D ( 'NONE', #46347, #27514, #5245 ) ;
#5256=AXIS2_PLACEMENT_3D ( 'NONE', #16315, #35383, #8964 ) ;
#5266=CIRCLE ( 'NONE', #17759, 37.49900000000000944 ) ;
#5302=CYLINDRICAL_SURFACE ( 'NONE', #45113, 42.00000000000000000 ) ;
#5308=CARTESIAN_POINT ( 'NONE',  ( 10.00000000000000000, 33.79645857604513992, -16.45098606841138178 ) ) ;
#5320=EDGE_LOOP ( 'NONE', ( #14797, #43749, #7077, #45314 ) ) ;
#5327=ORIENTED_EDGE ( 'NONE', *, *, #4322, .F. ) ;
#5328=ORIENTED_EDGE ( 'NONE', *, *, #44382, .T. ) ;
#5339=CARTESIAN_POINT ( 'NONE',  ( 10.00000000000000000, 21.32104025579114648, 30.84782396557224970 ) ) ;
#5344=CARTESIAN_POINT ( 'NONE',  ( 0.000000000000000000, 0.000000000000000000, 0.000000000000000000 ) ) ;
#5351=VERTEX_POINT ( 'NONE', #19899 ) ;
#5369=VERTEX_POINT ( 'NONE', #1791 ) ;
#5378=EDGE_CURVE ( 'NONE', #32480, #4066, #22718, .T. ) ;
#5391=DIRECTION ( 'NONE',  ( -1.000000000000000000, 0.000000000000000000, 0.000000000000000000 ) ) ;
#5400=ORIENTED_EDGE ( 'NONE', *, *, #19635, .F. ) ;
#5419=CARTESIAN_POINT ( 'NONE',  ( 10.00000000000000000, -33.80338159004296017, 16.23288003029484727 ) ) ;
#5436=FACE_OUTER_BOUND ( 'NONE', #12838, .T. ) ;
#5454=CARTESIAN_POINT ( 'NONE',  ( 0.000000000000000000, 6.736453364083555329, 36.88895765772635116 ) ) ;
#5459=CARTESIAN_POINT ( 'NONE',  ( 0.000000000000000000, 22.74946021919133088, 29.81001611431016229 ) ) ;
#5467=CARTESIAN_POINT ( 'NONE',  ( 0.000000000000000000, -16.45098606841102651, -33.79645857604531045 ) ) ;
#5469=AXIS2_PLACEMENT_3D ( 'NONE', #39769, #43903, #6229 ) ;
#5480=ORIENTED_EDGE ( 'NONE', *, *, #3126, .F. ) ;
#5481=EDGE_LOOP ( 'NONE', ( #39773, #8652, #11031, #42965 ) ) ;
#5483=CIRCLE ( 'NONE', #46916, 37.49900000000000944 ) ;
#5493=ORIENTED_EDGE ( 'NONE', *, *, #9658, .F. ) ;
#5500=AXIS2_PLACEMENT_3D ( 'NONE', #30135, #3, #41875 ) ;
#5517=CARTESIAN_POINT ( 'NONE',  ( 0.000000000000000000, 27.13269053701096922, 25.88420570971410228 ) ) ;
#5519=FACE_OUTER_BOUND ( 'NONE', #968, .T. ) ;
#5534=EDGE_CURVE ( 'NONE', #29887, #23982, #29997, .T. ) ;
#5539=EDGE_CURVE ( 'NONE', #6962, #11527, #29197, .T. ) ;
#5553=ORIENTED_EDGE ( 'NONE', *, *, #21102, .F. ) ;
#5554=VERTEX_POINT ( 'NONE', #37490 ) ;
#5564=CIRCLE ( 'NONE', #30579, 16.00000000000000000 ) ;
#5586=DIRECTION ( 'NONE',  ( -1.000000000000000000, 0.000000000000000000, 0.000000000000000000 ) ) ;
#5611=CIRCLE ( 'NONE', #19665, 16.00000000000000355 ) ;
#5616=FACE_OUTER_BOUND ( 'NONE', #30990, .T. ) ;
#5626=VERTEX_POINT ( 'NONE', #36992 ) ;
#5631=AXIS2_PLACEMENT_3D ( 'NONE', #14868, #18036, #37136 ) ;
#5637=ORIENTED_EDGE ( 'NONE', *, *, #26568, .T. ) ;
#5641=DIRECTION ( 'NONE',  ( 1.000000000000000000, 0.000000000000000000, -0.000000000000000000 ) ) ;
#5648=CYLINDRICAL_SURFACE ( 'NONE', #39975, 37.49900000000000233 ) ;
#5653=CARTESIAN_POINT ( 'NONE',  ( 10.00000000000000000, 0.000000000000000000, 0.000000000000000000 ) ) ;
#5669=FACE_OUTER_BOUND ( 'NONE', #47908, .T. ) ;
#5674=CARTESIAN_POINT ( 'NONE',  ( 10.00000000000000000, 4.992566952384984269, 37.16516213103279398 ) ) ;
#5702=DIRECTION ( 'NONE',  ( 0.000000000000000000, 0.000000000000000000, 1.000000000000000000 ) ) ;
#5705=CARTESIAN_POINT ( 'NONE',  ( 10.00000000000000000, -35.92658777277502935, -10.74501242461320594 ) ) ;
#5709=EDGE_CURVE ( 'NONE', #15060, #34499, #20592, .T. ) ;
#5722=VECTOR ( 'NONE', #13180, 1000.000000000000000 ) ;
#5767=CARTESIAN_POINT ( 'NONE',  ( 10.00000000000000000, 37.48860685352291000, -0.8828120875901940279 ) ) ;
#5771=CARTESIAN_POINT ( 'NONE',  ( 4.999999999999999112, -40.68715046381937128, 10.41901085202062660 ) ) ;
#5773=LINE ( 'NONE', #6022, #30083 ) ;
#5781=DIRECTION ( 'NONE',  ( 0.000000000000000000, 0.000000000000000000, 1.000000000000000000 ) ) ;
#5782=CARTESIAN_POINT ( 'NONE',  ( 10.00000000000000000, 37.22597642581150268, 5.202137450157037435 ) ) ;
#5791=CIRCLE ( 'NONE', #44871, 15.99999999999999467 ) ;
#5792=CIRCLE ( 'NONE', #22963, 42.00000000000000000 ) ;
#5808=ORIENTED_EDGE ( 'NONE', *, *, #3989, .T. ) ;
#5815=ORIENTED_EDGE ( 'NONE', *, *, #30132, .F. ) ;
#5820=FACE_OUTER_BOUND ( 'NONE', #30672, .T. ) ;
#5833=CARTESIAN_POINT ( 'NONE',  ( 10.00000000000000000, -10.96151621346514382, 35.95386929396252640 ) ) ;
#5836=VERTEX_POINT ( 'NONE', #35256 ) ;
#5837=ORIENTED_EDGE ( 'NONE', *, *, #25334, .T. ) ;
#5854=CARTESIAN_POINT ( 'NONE',  ( 0.000000000000000000, -29.81001611430991360, -22.74946021919165418 ) ) ;
#5860=CIRCLE ( 'NONE', #41806, 16.00000000000000000 ) ;
#5866=CARTESIAN_POINT ( 'NONE',  ( 10.00000000000000000, 33.00180498840072829, -17.80606268964504935 ) ) ;
#5870=AXIS2_PLACEMENT_3D ( 'NONE', #28544, #29007, #28290 ) ;
#5872=ORIENTED_EDGE ( 'NONE', *, *, #45236, .F. ) ;
#5892=VECTOR ( 'NONE', #13069, 1000.000000000000000 ) ;
#5924=ADVANCED_FACE ( 'NONE', ( #32558 ), #13950, .T. ) ;
#5940=LINE ( 'NONE', #2028, #36757 ) ;
#5941=VERTEX_POINT ( 'NONE', #7807 ) ;
#5944=ORIENTED_EDGE ( 'NONE', *, *, #25904, .F. ) ;
#5947=CIRCLE ( 'NONE', #44997, 15.99999999999999822 ) ;
#5956=ORIENTED_EDGE ( 'NONE', *, *, #1034, .F. ) ;
#5958=DIRECTION ( 'NONE',  ( 1.000000000000000000, 0.000000000000000000, 0.000000000000000000 ) ) ;
#5977=DIRECTION ( 'NONE',  ( 0.000000000000000000, 0.000000000000000000, 1.000000000000000000 ) ) ;
#5983=ORIENTED_EDGE ( 'NONE', *, *, #16758, .T. ) ;
#5990=AXIS2_PLACEMENT_3D ( 'NONE', #41713, #26778, #23113 ) ;
#5995=VERTEX_POINT ( 'NONE', #11252 ) ;
#6009=CARTESIAN_POINT ( 'NONE',  ( 10.00000000000000000, -21.40280677340398441, 36.13751322684410638 ) ) ;
#6017=CARTESIAN_POINT ( 'NONE',  ( 10.00000000000000000, -37.48860685352290290, -0.8828120875904512665 ) ) ;
#6022=CARTESIAN_POINT ( 'NONE',  ( 10.00000000000000000, -21.32104025579091910, -30.84782396557241313 ) ) ;
#6027=PRESENTATION_STYLE_ASSIGNMENT (( #16547 ) ) ;
#6039=ORIENTED_EDGE ( 'NONE', *, *, #25522, .T. ) ;
#6048=EDGE_CURVE ( 'NONE', #21073, #19357, #19061, .T. ) ;
#6049=CIRCLE ( 'NONE', #44324, 16.00000000000000000 ) ;
#6055=CARTESIAN_POINT ( 'NONE',  ( 0.000000000000000000, 0.000000000000000000, 0.000000000000000000 ) ) ;
#6104=CYLINDRICAL_SURFACE ( 'NONE', #15535, 42.00000000000000000 ) ;
#6111=ORIENTED_EDGE ( 'NONE', *, *, #32777, .F. ) ;
#6114=ORIENTED_EDGE ( 'NONE', *, *, #36049, .T. ) ;
#6123=AXIS2_PLACEMENT_3D ( 'NONE', #29297, #10702, #33445 ) ;
#6127=VERTEX_POINT ( 'NONE', #4402 ) ;
#6131=EDGE_CURVE ( 'NONE', #20243, #30855, #18291, .T. ) ;
#6133=FACE_OUTER_BOUND ( 'NONE', #37331, .T. ) ;
#6149=EDGE_CURVE ( 'NONE', #18061, #5554, #25338, .T. ) ;
#6153=CARTESIAN_POINT ( 'NONE',  ( 10.00000000000000000, 35.92658777277525672, -10.74501242461245809 ) ) ;
#6159=AXIS2_PLACEMENT_3D ( 'NONE', #38469, #11571, #34066 ) ;
#6161=ORIENTED_EDGE ( 'NONE', *, *, #33289, .F. ) ;
#6171=ORIENTED_EDGE ( 'NONE', *, *, #14198, .T. ) ;
#6179=CARTESIAN_POINT ( 'NONE',  ( 5.000000000000000000, 35.47612816024556537, -22.48208911017461631 ) ) ;
#6184=ORIENTED_EDGE ( 'NONE', *, *, #25293, .T. ) ;
#6192=CARTESIAN_POINT ( 'NONE',  ( 10.00000000000000000, 35.95386929396241271, 10.96151621346552751 ) ) ;
#6196=EDGE_CURVE ( 'NONE', #47392, #34754, #28477, .T. ) ;
#6207=CARTESIAN_POINT ( 'NONE',  ( 0.000000000000000000, 21.32104025579114648, 30.84782396557224970 ) ) ;
#6229=DIRECTION ( 'NONE',  ( 0.000000000000000000, 0.3090169943749410120, 0.9510565162951557516 ) ) ;
#6234=EDGE_LOOP ( 'NONE', ( #33759, #39607, #4754, #4705 ) ) ;
#6239=EDGE_CURVE ( 'NONE', #6864, #27731, #10475, .T. ) ;
#6240=ORIENTED_EDGE ( 'NONE', *, *, #48178, .F. ) ;
#6273=VERTEX_POINT ( 'NONE', #20764 ) ;
#6276=EDGE_LOOP ( 'NONE', ( #38206, #21022, #47282, #39099 ) ) ;
#6290=VERTEX_POINT ( 'NONE', #40085 ) ;
#6292=DIRECTION ( 'NONE',  ( -1.000000000000000000, -0.000000000000000000, 0.000000000000000000 ) ) ;
#6296=ORIENTED_EDGE ( 'NONE', *, *, #22115, .T. ) ;
#6298=CARTESIAN_POINT ( 'NONE',  ( 10.00000000000000000, -37.22597642581153821, -5.202137450156795850 ) ) ;
#6301=FACE_OUTER_BOUND ( 'NONE', #16047, .T. ) ;
#6304=EDGE_CURVE ( 'NONE', #1546, #7292, #43362, .T. ) ;
#6316=CARTESIAN_POINT ( 'NONE',  ( 50.00005079999999680, 12.24744871391589207, -2.499999999999994671 ) ) ;
#6317=CYLINDRICAL_SURFACE ( 'NONE', #27091, 42.00000000000000000 ) ;
#6336=CARTESIAN_POINT ( 'NONE',  ( 10.00000000000000178, 0.000000000000000000, 0.000000000000000000 ) ) ;
#6338=AXIS2_PLACEMENT_3D ( 'NONE', #15946, #31371, #24018 ) ;
#6348=AXIS2_PLACEMENT_3D ( 'NONE', #44049, #28395, #21046 ) ;
#6352=DIRECTION ( 'NONE',  ( -1.000000000000000000, 0.000000000000000000, -0.000000000000000000 ) ) ;
#6353=ORIENTED_EDGE ( 'NONE', *, *, #45997, .T. ) ;
#6356=CARTESIAN_POINT ( 'NONE',  ( -10.00000000000000000, 0.000000000000000000, 0.000000000000000000 ) ) ;
#6369=DIRECTION ( 'NONE',  ( -1.000000000000000000, 0.000000000000000000, -0.000000000000000000 ) ) ;
#6373=DIRECTION ( 'NONE',  ( -1.000000000000000000, -0.000000000000000000, 0.000000000000000000 ) ) ;
#6377=AXIS2_PLACEMENT_3D ( 'NONE', #12519, #35019, #31127 ) ;
#6405=EDGE_CURVE ( 'NONE', #47714, #15972, #18532, .T. ) ;
#6410=EDGE_CURVE ( 'NONE', #19329, #21447, #15998, .T. ) ;
#6414=LINE ( 'NONE', #6179, #19254 ) ;
#6418=ORIENTED_EDGE ( 'NONE', *, *, #20389, .T. ) ;
#6436=CARTESIAN_POINT ( 'NONE',  ( 10.00000000000000000, 0.000000000000000000, 0.000000000000000000 ) ) ;
#6443=ORIENTED_EDGE ( 'NONE', *, *, #26048, .F. ) ;
#6444=VERTEX_POINT ( 'NONE', #32968 ) ;
#6451=VERTEX_POINT ( 'NONE', #47892 ) ;
#6452=EDGE_CURVE ( 'NONE', #9450, #17448, #7264, .T. ) ;
#6456=EDGE_LOOP ( 'NONE', ( #18719, #29465, #34263, #24472 ) ) ;
#6463=VERTEX_POINT ( 'NONE', #3843 ) ;
#6485=VECTOR ( 'NONE', #48386, 1000.000000000000000 ) ;
#6488=CARTESIAN_POINT ( 'NONE',  ( 10.00000000000000000, 0.000000000000000000, 0.000000000000000000 ) ) ;
#6489=DIRECTION ( 'NONE',  ( 1.000000000000000000, -0.000000000000000000, -0.000000000000000000 ) ) ;
#6510=CIRCLE ( 'NONE', #40888, 42.00000000000000000 ) ;
#6518=CYLINDRICAL_SURFACE ( 'NONE', #39468, 37.49900000000000233 ) ;
#6536=ORIENTED_EDGE ( 'NONE', *, *, #10271, .F. ) ;
#6544=DIRECTION ( 'NONE',  ( -1.000000000000000000, -0.000000000000000000, 0.000000000000000000 ) ) ;
#6545=ORIENTED_EDGE ( 'NONE', *, *, #37260, .T. ) ;
#6548=VECTOR ( 'NONE', #19462, 1000.000000000000000 ) ;
#6553=FACE_OUTER_BOUND ( 'NONE', #4318, .T. ) ;
#6559=DIRECTION ( 'NONE',  ( 0.000000000000000000, 0.000000000000000000, 1.000000000000000000 ) ) ;
#6562=VECTOR ( 'NONE', #19546, 1000.000000000000000 ) ;
#6566=ORIENTED_EDGE ( 'NONE', *, *, #32592, .T. ) ;
#6573=CIRCLE ( 'NONE', #26105, 42.00000000000000000 ) ;
#6583=DIRECTION ( 'NONE',  ( 0.000000000000000000, 0.000000000000000000, 1.000000000000000000 ) ) ;
#6586=DIRECTION ( 'NONE',  ( 0.000000000000000000, -0.8090169943749402348, -0.5877852522924830181 ) ) ;
#6589=AXIS2_PLACEMENT_3D ( 'NONE', #31311, #20032, #30568 ) ;
#6592=FACE_OUTER_BOUND ( 'NONE', #235, .T. ) ;
#6600=DIRECTION ( 'NONE',  ( 0.000000000000000000, 0.9876883405951381034, -0.1564344650402276216 ) ) ;
#6619=DIRECTION ( 'NONE',  ( 0.000000000000000000, 0.000000000000000000, 1.000000000000000000 ) ) ;
#6623=VERTEX_POINT ( 'NONE', #19251 ) ;
#6626=EDGE_CURVE ( 'NONE', #26799, #41107, #35562, .T. ) ;
#6633=ORIENTED_EDGE ( 'NONE', *, *, #31194, .T. ) ;
#6642=EDGE_LOOP ( 'NONE', ( #43292, #15147, #23849, #11945 ) ) ;
#6643=DIRECTION ( 'NONE',  ( 0.000000000000000000, 1.000000000000000000, 3.491481338843133750E-15 ) ) ;
#6660=CARTESIAN_POINT ( 'NONE',  ( 0.000000000000000000, -3.925862922255855647, -41.81611651403866858 ) ) ;
#6686=CYLINDRICAL_SURFACE ( 'NONE', #4891, 42.00000000000000000 ) ;
#6699=ORIENTED_EDGE ( 'NONE', *, *, #46549, .F. ) ;
#6712=DIRECTION ( 'NONE',  ( 1.000000000000000000, 0.000000000000000000, 0.000000000000000000 ) ) ;
#6717=DIRECTION ( 'NONE',  ( 0.000000000000000000, 0.000000000000000000, 1.000000000000000000 ) ) ;
#6718=CIRCLE ( 'NONE', #14521, 37.49900000000000233 ) ;
#6728=CARTESIAN_POINT ( 'NONE',  ( 0.000000000000000000, -26.08949754953005495, -27.05870788708258701 ) ) ;
#6729=COLOUR_RGB ( '', 0.09019608, 0.27058824, 0.51372549) ;
#6730=DIRECTION ( 'NONE',  ( 0.000000000000000000, 0.000000000000000000, 1.000000000000000000 ) ) ;
#6748=AXIS2_PLACEMENT_3D ( 'NONE', #2509, #28476, #43413 ) ;
#6756=CIRCLE ( 'NONE', #13025, 15.99999999999999645 ) ;
#6768=AXIS2_PLACEMENT_3D ( 'NONE', #9087, #12289, #27211 ) ;
#6770=ORIENTED_EDGE ( 'NONE', *, *, #36065, .F. ) ;
#6778=CIRCLE ( 'NONE', #41171, 16.00000000000000000 ) ;
#6787=DIRECTION ( 'NONE',  ( 0.000000000000000000, -0.8910065241883721177, 0.4539904997395382003 ) ) ;
#6798=ADVANCED_FACE ( 'NONE', ( #47071 ), #13537, .T. ) ;
#6811=CARTESIAN_POINT ( 'NONE',  ( 0.000000000000000000, -35.53030884539077050, -12.26510123303296851 ) ) ;
#6825=ORIENTED_EDGE ( 'NONE', *, *, #40363, .F. ) ;
#6830=DIRECTION ( 'NONE',  ( 0.000000000000000000, 0.000000000000000000, 1.000000000000000000 ) ) ;
#6835=CYLINDRICAL_SURFACE ( 'NONE', #43276, 16.00000000000000000 ) ;
#6856=CARTESIAN_POINT ( 'NONE',  ( 10.00000000000000000, -15.48615015657610883, 39.04073710021339139 ) ) ;
#6857=ORIENTED_EDGE ( 'NONE', *, *, #4823, .T. ) ;
#6862=DIRECTION ( 'NONE',  ( 0.000000000000000000, 0.000000000000000000, 1.000000000000000000 ) ) ;
#6864=VERTEX_POINT ( 'NONE', #34293 ) ;
#6866=EDGE_CURVE ( 'NONE', #2845, #39728, #30170, .T. ) ;
#6868=AXIS2_PLACEMENT_3D ( 'NONE', #1783, #5228, #17176 ) ;
#6869=ADVANCED_FACE ( 'NONE', ( #11565 ), #7872, .T. ) ;
#6877=CARTESIAN_POINT ( 'NONE',  ( 0.000000000000000000, 12.24744871391588852, 2.500000000000003553 ) ) ;
#6892=DIRECTION ( 'NONE',  ( 0.000000000000000000, -8.881784197001252323E-16, -1.000000000000000000 ) ) ;
#6899=CARTESIAN_POINT ( 'NONE',  ( 10.00000000000000000, -26.79245525562738095, 32.34446384429961796 ) ) ;
#6916=EDGE_CURVE ( 'NONE', #8858, #11527, #11450, .T. ) ;
#6934=EDGE_CURVE ( 'NONE', #14862, #5941, #38959, .T. ) ;
#6945=ORIENTED_EDGE ( 'NONE', *, *, #34805, .T. ) ;
#6948=LINE ( 'NONE', #32427, #38181 ) ;
#6958=DIRECTION ( 'NONE',  ( 0.000000000000000000, -0.5877852522924624790, -0.8090169943749550008 ) ) ;
#6962=VERTEX_POINT ( 'NONE', #19843 ) ;
#6983=CARTESIAN_POINT ( 'NONE',  ( 10.00000000000000000, 0.000000000000000000, 0.000000000000000000 ) ) ;
#6984=ORIENTED_EDGE ( 'NONE', *, *, #43713, .T. ) ;
#6993=CARTESIAN_POINT ( 'NONE',  ( 10.00000000000000000, -22.64427369931148348, -30.00120703465229965 ) ) ;
#7018=CARTESIAN_POINT ( 'NONE',  ( 10.00000000000000000, 17.80606268964585226, -33.00180498840028775 ) ) ;
#7023=ADVANCED_FACE ( 'NONE', ( #42377 ), #8831, .T. ) ;
#7028=DIRECTION ( 'NONE',  ( 0.000000000000000000, 0.000000000000000000, 1.000000000000000000 ) ) ;
#7036=DIRECTION ( 'NONE',  ( 0.000000000000000000, -0.7071067811865536790, 0.7071067811865413555 ) ) ;
#7044=ORIENTED_EDGE ( 'NONE', *, *, #30562, .T. ) ;
#7054=VERTEX_POINT ( 'NONE', #45819 ) ;
#7067=ORIENTED_EDGE ( 'NONE', *, *, #9430, .F. ) ;
#7068=AXIS2_PLACEMENT_3D ( 'NONE', #15693, #44350, #10823 ) ;
#7076=EDGE_LOOP ( 'NONE', ( #32430, #31340, #43338, #11702 ) ) ;
#7077=ORIENTED_EDGE ( 'NONE', *, *, #30409, .T. ) ;
#7081=DIRECTION ( 'NONE',  ( -1.000000000000000000, 0.000000000000000000, 0.000000000000000000 ) ) ;
#7133=VERTEX_POINT ( 'NONE', #14445 ) ;
#7139=CARTESIAN_POINT ( 'NONE',  ( 10.00000000000000000, 0.000000000000000000, 0.000000000000000000 ) ) ;
#7142=CIRCLE ( 'NONE', #22752, 16.00000000000000355 ) ;
#7148=AXIS2_PLACEMENT_3D ( 'NONE', #37660, #7796, #36916 ) ;
#7152=DIRECTION ( 'NONE',  ( -1.000000000000000000, 0.000000000000000000, -0.000000000000000000 ) ) ;
#7157=CARTESIAN_POINT ( 'NONE',  ( 10.00000000000000000, 0.000000000000000000, 0.000000000000000000 ) ) ;
#7181=ORIENTED_EDGE ( 'NONE', *, *, #19829, .F. ) ;
#7185=CARTESIAN_POINT ( 'NONE',  ( 10.00000000000000000, 0.000000000000000000, 0.000000000000000000 ) ) ;
#7190=CARTESIAN_POINT ( 'NONE',  ( 10.00000000000000000, 0.000000000000000000, 0.000000000000000000 ) ) ;
#7199=DIRECTION ( 'NONE',  ( 0.000000000000000000, 0.000000000000000000, 1.000000000000000000 ) ) ;
#7200=DIRECTION ( 'NONE',  ( -1.000000000000000000, 0.000000000000000000, 0.000000000000000000 ) ) ;
#7213=ORIENTED_EDGE ( 'NONE', *, *, #21667, .F. ) ;
#7220=AXIS2_PLACEMENT_3D ( 'NONE', #6983, #40524, #25810 ) ;
#7222=ORIENTED_EDGE ( 'NONE', *, *, #12178, .T. ) ;
#7223=ORIENTED_EDGE ( 'NONE', *, *, #33533, .T. ) ;
#7229=EDGE_CURVE ( 'NONE', #37417, #34741, #3664, .T. ) ;
#7251=CARTESIAN_POINT ( 'NONE',  ( 10.00000000000000000, -21.53537804866103045, 30.80686688397002371 ) ) ;
#7264=LINE ( 'NONE', #36875, #16763 ) ;
#7273=AXIS2_PLACEMENT_3D ( 'NONE', #33919, #30499, #7971 ) ;
#7279=ORIENTED_EDGE ( 'NONE', *, *, #3922, .F. ) ;
#7284=CARTESIAN_POINT ( 'NONE',  ( 0.000000000000000000, -35.95386929396248377, -10.96151621346525751 ) ) ;
#7288=ORIENTED_EDGE ( 'NONE', *, *, #14705, .T. ) ;
#7292=VERTEX_POINT ( 'NONE', #33281 ) ;
#7295=AXIS2_PLACEMENT_3D ( 'NONE', #15893, #4632, #30832 ) ;
#7306=DIRECTION ( 'NONE',  ( -1.000000000000000000, 0.000000000000000000, 0.000000000000000000 ) ) ;
#7325=CARTESIAN_POINT ( 'NONE',  ( 10.00000000000000000, 33.80338159004283938, 16.23288003029508886 ) ) ;
#7331=EDGE_LOOP ( 'NONE', ( #41774, #13448, #24399, #20068 ) ) ;
#7336=ADVANCED_FACE ( 'NONE', ( #18347 ), #19310, .T. ) ;
#7345=EDGE_CURVE ( 'NONE', #48195, #9112, #34235, .T. ) ;
#7348=ADVANCED_FACE ( 'NONE', ( #20279 ), #12960, .T. ) ;
#7360=VERTEX_POINT ( 'NONE', #16611 ) ;
#7364=AXIS2_PLACEMENT_3D ( 'NONE', #12877, #23392, #19465 ) ;
#7365=LINE ( 'NONE', #33543, #45357 ) ;
#7371=CYLINDRICAL_SURFACE ( 'NONE', #47315, 37.49900000000000233 ) ;
#7404=AXIS2_PLACEMENT_3D ( 'NONE', #14864, #10713, #29782 ) ;
#7423=VECTOR ( 'NONE', #95, 1000.000000000000000 ) ;
#7429=AXIS2_PLACEMENT_3D ( 'NONE', #9169, #47350, #13329 ) ;
#7451=DIRECTION ( 'NONE',  ( 0.000000000000000000, -0.5877852522924801315, 0.8090169943749421222 ) ) ;
#7457=CIRCLE ( 'NONE', #34799, 16.00000000000000000 ) ;
#7483=AXIS2_PLACEMENT_3D ( 'NONE', #16523, #23616, #28260 ) ;
#7487=ADVANCED_FACE ( 'NONE', ( #31081 ), #46002, .T. ) ;
#7499=LINE ( 'NONE', #19226, #17826 ) ;
#7505=DIRECTION ( 'NONE',  ( 0.000000000000000000, -0.3090169943749548342, 0.9510565162951511997 ) ) ;
#7506=ORIENTED_EDGE ( 'NONE', *, *, #35798, .T. ) ;
#7523=DIRECTION ( 'NONE',  ( -1.000000000000000000, 0.000000000000000000, 0.000000000000000000 ) ) ;
#7525=LINE ( 'NONE', #33694, #4034 ) ;
#7538=ORIENTED_EDGE ( 'NONE', *, *, #46610, .F. ) ;
#7541=ORIENTED_EDGE ( 'NONE', *, *, #26320, .F. ) ;
#7550=ORIENTED_EDGE ( 'NONE', *, *, #6048, .T. ) ;
#7553=DIRECTION ( 'NONE',  ( -1.000000000000000000, 0.000000000000000000, 0.000000000000000000 ) ) ;
#7556=DIRECTION ( 'NONE',  ( 1.000000000000000000, -0.000000000000000000, 0.000000000000000000 ) ) ;
#7558=DIRECTION ( 'NONE',  ( -1.000000000000000000, 0.000000000000000000, -0.000000000000000000 ) ) ;
#7568=DIRECTION ( 'NONE',  ( 0.000000000000000000, -0.3090169943749549453, 0.9510565162951511997 ) ) ;
#7571=EDGE_CURVE ( 'NONE', #17448, #20243, #36409, .T. ) ;
#7577=DIRECTION ( 'NONE',  ( -1.000000000000000000, 0.000000000000000000, 0.000000000000000000 ) ) ;
#7579=CARTESIAN_POINT ( 'NONE',  ( 10.00000000000000000, -10.74501242461258244, -35.92658777277521409 ) ) ;
#7596=ORIENTED_EDGE ( 'NONE', *, *, #39522, .F. ) ;
#7620=AXIS2_PLACEMENT_3D ( 'NONE', #2693, #32570, #43816 ) ;
#7621=CARTESIAN_POINT ( 'NONE',  ( 10.00000000000000000, 38.55633173627034438, -16.65560815589369881 ) ) ;
#7622=LINE ( 'NONE', #10813, #10989 ) ;
#7628=DIRECTION ( 'NONE',  ( -1.000000000000000000, 0.000000000000000000, 0.000000000000000000 ) ) ;
#7634=DIRECTION ( 'NONE',  ( -1.000000000000000000, 0.000000000000000000, 0.000000000000000000 ) ) ;
#7639=CARTESIAN_POINT ( 'NONE',  ( 10.00000000000000000, 0.6853352020795618893, -37.58145647212453611 ) ) ;
#7648=DIRECTION ( 'NONE',  ( 0.000000000000000000, 0.1564344650402242354, 0.9876883405951387696 ) ) ;
#7677=DIRECTION ( 'NONE',  ( 0.000000000000000000, 0.000000000000000000, 1.000000000000000000 ) ) ;
#7680=CYLINDRICAL_SURFACE ( 'NONE', #18435, 42.00000000000000000 ) ;
#7704=CIRCLE ( 'NONE', #41326, 42.00000000000000000 ) ;
#7707=ORIENTED_EDGE ( 'NONE', *, *, #25293, .F. ) ;
#7714=EDGE_CURVE ( 'NONE', #11606, #25587, #35612, .T. ) ;
#7716=EDGE_CURVE ( 'NONE', #34741, #47392, #30943, .T. ) ;
#7721=ADVANCED_FACE ( 'NONE', ( #8451 ), #31467, .T. ) ;
#7730=CARTESIAN_POINT ( 'NONE',  ( 0.000000000000000000, 0.000000000000000000, 0.000000000000000000 ) ) ;
#7738=CARTESIAN_POINT ( 'NONE',  ( 0.000000000000000000, 10.74501242461282757, 35.92658777277515014 ) ) ;
#7747=CYLINDRICAL_SURFACE ( 'NONE', #21187, 16.00000000000000000 ) ;
#7760=FACE_OUTER_BOUND ( 'NONE', #21647, .T. ) ;
#7790=CARTESIAN_POINT ( 'NONE',  ( -1.200000000000000030E-05, 0.9569279952884557350, -2.499999999999984457 ) ) ;
#7791=ORIENTED_EDGE ( 'NONE', *, *, #18880, .T. ) ;
#7796=DIRECTION ( 'NONE',  ( -1.000000000000000000, 0.000000000000000000, 0.000000000000000000 ) ) ;
#7799=ORIENTED_EDGE ( 'NONE', *, *, #40807, .F. ) ;
#7807=CARTESIAN_POINT ( 'NONE',  ( 10.00000000000000000, 16.95692799528845640, -2.500000000000000000 ) ) ;
#7817=FACE_OUTER_BOUND ( 'NONE', #31953, .T. ) ;
#7837=EDGE_CURVE ( 'NONE', #15162, #20655, #41366, .T. ) ;
#7842=ORIENTED_EDGE ( 'NONE', *, *, #9449, .F. ) ;
#7849=ORIENTED_EDGE ( 'NONE', *, *, #17449, .T. ) ;
#7852=EDGE_LOOP ( 'NONE', ( #14082, #15206, #39587, #46868 ) ) ;
#7872=CYLINDRICAL_SURFACE ( 'NONE', #48148, 16.00000000000000000 ) ;
#7880=VERTEX_POINT ( 'NONE', #22112 ) ;
#7887=CARTESIAN_POINT ( 'NONE',  ( 0.000000000000000000, 30.80686688397010542, 21.53537804866092387 ) ) ;
#7903=ORIENTED_EDGE ( 'NONE', *, *, #42623, .F. ) ;
#7908=DIRECTION ( 'NONE',  ( -1.000000000000000000, 0.000000000000000000, 0.000000000000000000 ) ) ;
#7914=DIRECTION ( 'NONE',  ( -1.000000000000000000, -0.000000000000000000, 0.000000000000000000 ) ) ;
#7926=DIRECTION ( 'NONE',  ( -1.000000000000000000, -0.000000000000000000, -0.000000000000000000 ) ) ;
#7931=EDGE_CURVE ( 'NONE', #11606, #18781, #8500, .T. ) ;
#7939=CIRCLE ( 'NONE', #32958, 42.00000000000000000 ) ;
#7942=AXIS2_PLACEMENT_3D ( 'NONE', #39356, #43517, #2376 ) ;
#7959=CIRCLE ( 'NONE', #8770, 37.49900000000000233 ) ;
#7963=CARTESIAN_POINT ( 'NONE',  ( 50.00005079999999680, 0.000000000000000000, 0.000000000000000000 ) ) ;
#7968=DIRECTION ( 'NONE',  ( 0.000000000000000000, 0.000000000000000000, 1.000000000000000000 ) ) ;
#7971=DIRECTION ( 'NONE',  ( 0.000000000000000000, 0.000000000000000000, 1.000000000000000000 ) ) ;
#7972=AXIS2_PLACEMENT_3D ( 'NONE', #44896, #10652, #36343 ) ;
#7973=CARTESIAN_POINT ( 'NONE',  ( 10.00000000000000000, -30.84782396557233142, 21.32104025579104345 ) ) ;
#7998=ORIENTED_EDGE ( 'NONE', *, *, #46549, .T. ) ;
#8001=VERTEX_POINT ( 'NONE', #33721 ) ;
#8009=AXIS2_PLACEMENT_3D ( 'NONE', #17490, #20689, #32439 ) ;
#8016=EDGE_CURVE ( 'NONE', #24152, #15492, #36660, .T. ) ;
#8020=ORIENTED_EDGE ( 'NONE', *, *, #20827, .T. ) ;
#8031=CIRCLE ( 'NONE', #33048, 16.00000000000000000 ) ;
#8035=ORIENTED_EDGE ( 'NONE', *, *, #48112, .F. ) ;
#8041=DIRECTION ( 'NONE',  ( 0.000000000000000000, -0.8910065241883722287, 0.4539904997395382003 ) ) ;
#8043=CYLINDRICAL_SURFACE ( 'NONE', #15382, 16.00000000000000000 ) ;
#8063=DIRECTION ( 'NONE',  ( 0.000000000000000000, 0.000000000000000000, 1.000000000000000000 ) ) ;
#8073=CIRCLE ( 'NONE', #37781, 16.00000000000000000 ) ;
#8075=VERTEX_POINT ( 'NONE', #30314 ) ;
#8076=ORIENTED_EDGE ( 'NONE', *, *, #30132, .T. ) ;
#8086=PLANE ( 'NONE',  #42338 ) ;
#8092=VERTEX_POINT ( 'NONE', #679 ) ;
#8098=DIRECTION ( 'NONE',  ( 0.000000000000000000, 0.000000000000000000, 1.000000000000000000 ) ) ;
#8101=ORIENTED_EDGE ( 'NONE', *, *, #5035, .F. ) ;
#8110=CYLINDRICAL_SURFACE ( 'NONE', #2843, 16.00000000000000000 ) ;
#8128=CARTESIAN_POINT ( 'NONE',  ( 10.00000000000000000, -16.23288003029521320, 33.80338159004277543 ) ) ;
#8138=CIRCLE ( 'NONE', #28432, 16.00000000000000000 ) ;
#8145=VECTOR ( 'NONE', #43632, 1000.000000000000000 ) ;
#8167=CYLINDRICAL_SURFACE ( 'NONE', #5081, 16.00000000000000000 ) ;
#8177=DIRECTION ( 'NONE',  ( 0.000000000000000000, 0.000000000000000000, 1.000000000000000000 ) ) ;
#8184=CARTESIAN_POINT ( 'NONE',  ( 10.00000000000000000, 0.000000000000000000, 0.000000000000000000 ) ) ;
#8185=CARTESIAN_POINT ( 'NONE',  ( 10.00000000000000000, -10.96151621346461447, -35.95386929396268272 ) ) ;
#8203=AXIS2_PLACEMENT_3D ( 'NONE', #6488, #17741, #10154 ) ;
#8204=VECTOR ( 'NONE', #25480, 1000.000000000000000 ) ;
#8223=CYLINDRICAL_SURFACE ( 'NONE', #28378, 16.00000000000000000 ) ;
#8226=CARTESIAN_POINT ( 'NONE',  ( 4.999999999999999112, -9.188173127307004862, -40.98264845739759465 ) ) ;
#8268=AXIS2_PLACEMENT_3D ( 'NONE', #40026, #36345, #17970 ) ;
#8278=CYLINDRICAL_SURFACE ( 'NONE', #27071, 37.49900000000000233 ) ;
#8284=DIRECTION ( 'NONE',  ( 0.000000000000000000, -9.787530781167598712E-16, -1.000000000000000000 ) ) ;
#8285=ADVANCED_FACE ( 'NONE', ( #47160 ), #10921, .F. ) ;
#8291=VERTEX_POINT ( 'NONE', #10692 ) ;
#8304=CIRCLE ( 'NONE', #12233, 16.00000000000000000 ) ;
#8312=ADVANCED_FACE ( 'NONE', ( #25599 ), #3321, .T. ) ;
#8315=ORIENTED_EDGE ( 'NONE', *, *, #43498, .F. ) ;
#8338=VERTEX_POINT ( 'NONE', #40778 ) ;
#8339=DIRECTION ( 'NONE',  ( 0.000000000000000000, 0.000000000000000000, 1.000000000000000000 ) ) ;
#8341=LINE ( 'NONE', #19571, #47694 ) ;
#8344=VECTOR ( 'NONE', #31310, 1000.000000000000000 ) ;
#8348=DIRECTION ( 'NONE',  ( 1.000000000000000000, 0.000000000000000000, 0.000000000000000000 ) ) ;
#8357=DIRECTION ( 'NONE',  ( 0.000000000000000000, 0.000000000000000000, -1.000000000000000000 ) ) ;
#8366=ORIENTED_EDGE ( 'NONE', *, *, #40414, .T. ) ;
#8369=DIRECTION ( 'NONE',  ( 0.000000000000000000, 0.4539904997395477482, -0.8910065241883673437 ) ) ;
#8371=DIRECTION ( 'NONE',  ( -1.000000000000000000, 0.000000000000000000, -0.000000000000000000 ) ) ;
#8389=VERTEX_POINT ( 'NONE', #17284 ) ;
#8392=EDGE_CURVE ( 'NONE', #26170, #48358, #32704, .T. ) ;
#8401=FACE_OUTER_BOUND ( 'NONE', #683, .T. ) ;
#8407=CARTESIAN_POINT ( 'NONE',  ( 10.00000000000000000, 29.81001611431009479, 22.74946021919143391 ) ) ;
#8412=LINE ( 'NONE', #30449, #17447 ) ;
#8417=FACE_OUTER_BOUND ( 'NONE', #44005, .T. ) ;
#8425=EDGE_CURVE ( 'NONE', #6273, #5369, #7499, .T. ) ;
#8429=ORIENTED_EDGE ( 'NONE', *, *, #22345, .T. ) ;
#8444=DIRECTION ( 'NONE',  ( -1.000000000000000000, 0.000000000000000000, -0.000000000000000000 ) ) ;
#8446=DIRECTION ( 'NONE',  ( -1.000000000000000000, -0.000000000000000000, 0.000000000000000000 ) ) ;
#8449=EDGE_CURVE ( 'NONE', #30139, #8092, #1431, .T. ) ;
#8451=FACE_OUTER_BOUND ( 'NONE', #12170, .T. ) ;
#8461=CARTESIAN_POINT ( 'NONE',  ( 0.000000000000000000, -37.58145647212455032, 0.6853352020789044152 ) ) ;
#8462=DIRECTION ( 'NONE',  ( 0.000000000000000000, -0.8090169943749403458, -0.5877852522924830181 ) ) ;
#8468=DIRECTION ( 'NONE',  ( 0.000000000000000000, 0.000000000000000000, 1.000000000000000000 ) ) ;
#8469=DIRECTION ( 'NONE',  ( -1.000000000000000000, -0.000000000000000000, 0.000000000000000000 ) ) ;
#8471=ORIENTED_EDGE ( 'NONE', *, *, #23193, .T. ) ;
#8478=AXIS2_PLACEMENT_3D ( 'NONE', #40259, #3026, #21389 ) ;
#8486=CARTESIAN_POINT ( 'NONE',  ( 0.000000000000000000, 16.23288003029543347, -33.80338159004267595 ) ) ;
#8490=CARTESIAN_POINT ( 'NONE',  ( 10.00000000000000000, 10.74501242461282757, 35.92658777277515014 ) ) ;
#8500=CIRCLE ( 'NONE', #3834, 37.49900000000000944 ) ;
#8511=VERTEX_POINT ( 'NONE', #12149 ) ;
#8517=AXIS2_PLACEMENT_3D ( 'NONE', #17378, #39690, #39442 ) ;
#8519=CARTESIAN_POINT ( 'NONE',  ( 10.00000000000000000, 0.000000000000000000, 0.000000000000000000 ) ) ;
#8520=ORIENTED_EDGE ( 'NONE', *, *, #43101, .T. ) ;
#8534=DIRECTION ( 'NONE',  ( 0.000000000000000000, 0.4539904997395414754, 0.8910065241883706744 ) ) ;
#8548=ORIENTED_EDGE ( 'NONE', *, *, #42664, .T. ) ;
#8552=EDGE_CURVE ( 'NONE', #28265, #25548, #40523, .T. ) ;
#8556=DIRECTION ( 'NONE',  ( -1.000000000000000000, -0.000000000000000000, 0.000000000000000000 ) ) ;
#8557=ORIENTED_EDGE ( 'NONE', *, *, #33912, .F. ) ;
#8558=DIRECTION ( 'NONE',  ( -1.000000000000000000, 0.000000000000000000, 0.000000000000000000 ) ) ;
#8559=ORIENTED_EDGE ( 'NONE', *, *, #9658, .T. ) ;
#8560=DIRECTION ( 'NONE',  ( -1.000000000000000000, -0.000000000000000000, 0.000000000000000000 ) ) ;
#8570=DIRECTION ( 'NONE',  ( -1.000000000000000000, 0.000000000000000000, 0.000000000000000000 ) ) ;
#8571=FACE_OUTER_BOUND ( 'NONE', #44955, .T. ) ;
#8573=LINE ( 'NONE', #37483, #35021 ) ;
#8580=FACE_OUTER_BOUND ( 'NONE', #44449, .T. ) ;
#8583=DIRECTION ( 'NONE',  ( -1.000000000000000000, 0.000000000000000000, 0.000000000000000000 ) ) ;
#8589=DIRECTION ( 'NONE',  ( 0.000000000000000000, 0.000000000000000000, 1.000000000000000000 ) ) ;
#8595=AXIS2_PLACEMENT_3D ( 'NONE', #14191, #13951, #44295 ) ;
#8601=CIRCLE ( 'NONE', #42123, 42.00000000000000000 ) ;
#8613=ORIENTED_EDGE ( 'NONE', *, *, #39477, .T. ) ;
#8618=VERTEX_POINT ( 'NONE', #12860 ) ;
#8619=DIRECTION ( 'NONE',  ( -1.000000000000000000, 0.000000000000000000, 0.000000000000000000 ) ) ;
#8623=AXIS2_PLACEMENT_3D ( 'NONE', #27064, #8446, #30987 ) ;
#8642=VECTOR ( 'NONE', #39731, 1000.000000000000000 ) ;
#8652=ORIENTED_EDGE ( 'NONE', *, *, #915, .F. ) ;
#8656=CARTESIAN_POINT ( 'NONE',  ( 10.00000000000000000, 30.00120703465205452, 22.64427369931179967 ) ) ;
#8668=EDGE_CURVE ( 'NONE', #45189, #29506, #8932, .T. ) ;
#8686=ORIENTED_EDGE ( 'NONE', *, *, #42994, .F. ) ;
#8689=CYLINDRICAL_SURFACE ( 'NONE', #40093, 16.00000000000000000 ) ;
#8701=VERTEX_POINT ( 'NONE', #41998 ) ;
#8703=( NAMED_UNIT ( * ) SI_UNIT ( $, .STERADIAN. ) SOLID_ANGLE_UNIT ( ) );
#8705=AXIS2_PLACEMENT_3D ( 'NONE', #7730, #22657, #389 ) ;
#8711=DIRECTION ( 'NONE',  ( -1.000000000000000000, 0.000000000000000000, -0.000000000000000000 ) ) ;
#8719=ORIENTED_EDGE ( 'NONE', *, *, #281, .T. ) ;
#8730=AXIS2_PLACEMENT_3D ( 'NONE', #2872, #40342, #10714 ) ;
#8736=EDGE_LOOP ( 'NONE', ( #15542, #21317, #6633, #23146 ) ) ;
#8742=EDGE_CURVE ( 'NONE', #38437, #34100, #16314, .T. ) ;
#8746=LINE ( 'NONE', #34211, #34881 ) ;
#8747=ORIENTED_EDGE ( 'NONE', *, *, #6304, .F. ) ;
#8755=DIRECTION ( 'NONE',  ( 1.000000000000000000, 0.000000000000000000, 0.000000000000000000 ) ) ;
#8759=EDGE_CURVE ( 'NONE', #4600, #11933, #6948, .T. ) ;
#8768=DIRECTION ( 'NONE',  ( 0.000000000000000000, 0.000000000000000000, 1.000000000000000000 ) ) ;
#8770=AXIS2_PLACEMENT_3D ( 'NONE', #28536, #2332, #28997 ) ;
#8772=CARTESIAN_POINT ( 'NONE',  ( -10.00000000000000000, 0.000000000000000000, 0.000000000000000000 ) ) ;
#8790=VERTEX_POINT ( 'NONE', #47356 ) ;
#8791=ORIENTED_EDGE ( 'NONE', *, *, #18676, .F. ) ;
#8793=CIRCLE ( 'NONE', #38547, 16.00000000000000000 ) ;
#8801=CARTESIAN_POINT ( 'NONE',  ( 0.000000000000000000, -10.74501242461258244, -35.92658777277521409 ) ) ;
#8814=CARTESIAN_POINT ( 'NONE',  ( 5.000000000000000000, -27.75498641678720446, -31.52238457039628727 ) ) ;
#8831=CYLINDRICAL_SURFACE ( 'NONE', #31016, 16.00000000000000000 ) ;
#8847=CIRCLE ( 'NONE', #21356, 37.49900000000001654 ) ;
#8858=VERTEX_POINT ( 'NONE', #25773 ) ;
#8875=ADVANCED_FACE ( 'NONE', ( #15274 ), #23085, .T. ) ;
#8877=DIRECTION ( 'NONE',  ( 0.000000000000000000, 0.000000000000000000, -1.000000000000000000 ) ) ;
#8885=DIRECTION ( 'NONE',  ( 0.000000000000000000, 1.000000000000000000, 3.469446951953614189E-15 ) ) ;
#8886=FACE_OUTER_BOUND ( 'NONE', #6456, .T. ) ;
#8901=FACE_OUTER_BOUND ( 'NONE', #34835, .T. ) ;
#8904=ADVANCED_FACE ( 'NONE', ( #15023 ), #26756, .T. ) ;
#8930=VERTEX_POINT ( 'NONE', #22111 ) ;
#8931=CIRCLE ( 'NONE', #10508, 42.00000000000000000 ) ;
#8932=LINE ( 'NONE', #42721, #4573 ) ;
#8939=DIRECTION ( 'NONE',  ( -1.000000000000000000, 0.000000000000000000, 0.000000000000000000 ) ) ;
#8947=AXIS2_PLACEMENT_3D ( 'NONE', #7639, #25742, #22569 ) ;
#8954=VECTOR ( 'NONE', #10520, 1000.000000000000000 ) ;
#8959=AXIS2_PLACEMENT_3D ( 'NONE', #29834, #44764, #43064 ) ;
#8961=CARTESIAN_POINT ( 'NONE',  ( 0.000000000000000000, -21.53537804866058991, -30.80686688397033635 ) ) ;
#8964=DIRECTION ( 'NONE',  ( 0.000000000000000000, -0.9510565162951565288, 0.3090169943749382364 ) ) ;
#8966=CIRCLE ( 'NONE', #1137, 42.00000000000000000 ) ;
#8967=VECTOR ( 'NONE', #34786, 1000.000000000000000 ) ;
#8978=ORIENTED_EDGE ( 'NONE', *, *, #40977, .F. ) ;
#9016=CARTESIAN_POINT ( 'NONE',  ( 10.00000000000000000, -16.45098606841102651, -33.79645857604531045 ) ) ;
#9027=DIRECTION ( 'NONE',  ( -1.000000000000000000, 0.000000000000000000, 0.000000000000000000 ) ) ;
#9042=AXIS2_PLACEMENT_3D ( 'NONE', #25080, #17494, #2103 ) ;
#9046=VERTEX_POINT ( 'NONE', #13048 ) ;
#9059=DIRECTION ( 'NONE',  ( 0.000000000000000000, -0.8910065241883721177, 0.4539904997395382003 ) ) ;
#9060=ORIENTED_EDGE ( 'NONE', *, *, #9603, .T. ) ;
#9065=DIRECTION ( 'NONE',  ( 0.000000000000000000, -6.982962677686267499E-15, 1.000000000000000000 ) ) ;
#9066=AXIS2_PLACEMENT_3D ( 'NONE', #43214, #34902, #46410 ) ;
#9069=CARTESIAN_POINT ( 'NONE',  ( 0.000000000000000000, 0.000000000000000000, 0.000000000000000000 ) ) ;
#9070=VERTEX_POINT ( 'NONE', #24285 ) ;
#9071=CARTESIAN_POINT ( 'NONE',  ( 10.00000000000000000, -37.58145647212455032, 0.6853352020789044152 ) ) ;
#9079=CARTESIAN_POINT ( 'NONE',  ( 0.000000000000000000, 0.000000000000000000, 0.000000000000000000 ) ) ;
#9081=AXIS2_PLACEMENT_3D ( 'NONE', #5467, #39006, #20385 ) ;
#9087=CARTESIAN_POINT ( 'NONE',  ( 0.000000000000000000, -37.22597642581153821, -5.202137450156795850 ) ) ;
#9091=SHAPE_REPRESENTATION ( 'small gear_ISO - Spur gear 2M 40T 20PA 10FW ---S40A75H50L20.0N', ( #11636 ), #10100 ) ;
#9096=DIRECTION ( 'NONE',  ( 1.000000000000000000, -0.000000000000000000, -0.000000000000000000 ) ) ;
#9104=ORIENTED_EDGE ( 'NONE', *, *, #29018, .F. ) ;
#9111=DIRECTION ( 'NONE',  ( 0.000000000000000000, 0.000000000000000000, -1.000000000000000000 ) ) ;
#9112=VERTEX_POINT ( 'NONE', #1304 ) ;
#9125=EDGE_CURVE ( 'NONE', #21677, #17728, #27011, .T. ) ;
#9130=VERTEX_POINT ( 'NONE', #31168 ) ;
#9133=DIRECTION ( 'NONE',  ( -1.000000000000000000, -0.000000000000000000, 0.000000000000000000 ) ) ;
#9144=AXIS2_PLACEMENT_3D ( 'NONE', #7963, #8939, #41515 ) ;
#9157=LINE ( 'NONE', #20170, #47912 ) ;
#9159=AXIS2_PLACEMENT_3D ( 'NONE', #8185, #26784, #25806 ) ;
#9169=CARTESIAN_POINT ( 'NONE',  ( 10.00000000000000000, 0.000000000000000000, 0.000000000000000000 ) ) ;
#9170=ORIENTED_EDGE ( 'NONE', *, *, #14104, .T. ) ;
#9171=ORIENTED_EDGE ( 'NONE', *, *, #11785, .F. ) ;
#9173=FACE_OUTER_BOUND ( 'NONE', #21336, .T. ) ;
#9183=AXIS2_PLACEMENT_3D ( 'NONE', #1003, #31619, #23521 ) ;
#9221=LINE ( 'NONE', #28072, #35121 ) ;
#9239=ORIENTED_EDGE ( 'NONE', *, *, #11271, .T. ) ;
#9253=DIRECTION ( 'NONE',  ( -1.000000000000000000, 0.000000000000000000, -0.000000000000000000 ) ) ;
#9273=VECTOR ( 'NONE', #2160, 1000.000000000000000 ) ;
#9275=DIRECTION ( 'NONE',  ( 0.000000000000000000, 0.000000000000000000, 1.000000000000000000 ) ) ;
#9289=VERTEX_POINT ( 'NONE', #26223 ) ;
#9298=ORIENTED_EDGE ( 'NONE', *, *, #46610, .T. ) ;
#9305=VERTEX_POINT ( 'NONE', #26462 ) ;
#9309=AXIS2_PLACEMENT_3D ( 'NONE', #7284, #22228, #37153 ) ;
#9315=DIRECTION ( 'NONE',  ( 0.000000000000000000, 0.000000000000000000, 1.000000000000000000 ) ) ;
#9318=DIRECTION ( 'NONE',  ( -1.000000000000000000, -0.000000000000000000, 0.000000000000000000 ) ) ;
#9323=DIRECTION ( 'NONE',  ( -1.000000000000000000, 0.000000000000000000, -0.000000000000000000 ) ) ;
#9355=DIRECTION ( 'NONE',  ( 0.000000000000000000, 0.000000000000000000, 1.000000000000000000 ) ) ;
#9364=DIRECTION ( 'NONE',  ( -1.000000000000000000, 0.000000000000000000, 0.000000000000000000 ) ) ;
#9374=DIRECTION ( 'NONE',  ( 0.000000000000000000, -6.938893903907228378E-15, 1.000000000000000000 ) ) ;
#9382=DIRECTION ( 'NONE',  ( -1.000000000000000000, 0.000000000000000000, 0.000000000000000000 ) ) ;
#9383=VECTOR ( 'NONE', #41398, 1000.000000000000000 ) ;
#9392=ORIENTED_EDGE ( 'NONE', *, *, #41507, .F. ) ;
#9407=AXIS2_PLACEMENT_3D ( 'NONE', #24612, #32664, #39787 ) ;
#9420=CARTESIAN_POINT ( 'NONE',  ( 4.999999999999999112, -9.188173127307592836, 40.98264845739746676 ) ) ;
#9430=EDGE_CURVE ( 'NONE', #12321, #7133, #44571, .T. ) ;
#9434=DIRECTION ( 'NONE',  ( -1.000000000000000000, 0.000000000000000000, -0.000000000000000000 ) ) ;
#9438=DIRECTION ( 'NONE',  ( -1.000000000000000000, 0.000000000000000000, 0.000000000000000000 ) ) ;
#9449=EDGE_CURVE ( 'NONE', #17019, #39073, #46936, .T. ) ;
#9450=VERTEX_POINT ( 'NONE', #5104 ) ;
#9457=ORIENTED_EDGE ( 'NONE', *, *, #6131, .T. ) ;
#9462=ORIENTED_EDGE ( 'NONE', *, *, #13042, .T. ) ;
#9468=CARTESIAN_POINT ( 'NONE',  ( 10.00000000000000000, 21.53537804866126137, -30.80686688396986028 ) ) ;
#9473=CYLINDRICAL_SURFACE ( 'NONE', #23603, 37.49900000000000233 ) ;
#9476=LINE ( 'NONE', #23686, #28349 ) ;
#9483=CARTESIAN_POINT ( 'NONE',  ( 10.00000000000000000, -22.64427369931191336, 30.00120703465197280 ) ) ;
#9485=EDGE_CURVE ( 'NONE', #36993, #43390, #3378, .T. ) ;
#9488=EDGE_LOOP ( 'NONE', ( #40490, #37692, #35106, #4824 ) ) ;
#9495=EDGE_CURVE ( 'NONE', #40832, #26882, #8847, .T. ) ;
#9522=ORIENTED_EDGE ( 'NONE', *, *, #43101, .F. ) ;
#9527=CARTESIAN_POINT ( 'NONE',  ( 10.00000000000000000, 0.000000000000000000, 0.000000000000000000 ) ) ;
#9541=EDGE_CURVE ( 'NONE', #41064, #36905, #34612, .T. ) ;
#9561=LINE ( 'NONE', #6153, #42454 ) ;
#9564=ORIENTED_EDGE ( 'NONE', *, *, #41029, .T. ) ;
#9565=EDGE_CURVE ( 'NONE', #5351, #908, #6510, .T. ) ;
#9568=CARTESIAN_POINT ( 'NONE',  ( -10.00000000000000000, 0.000000000000000000, 0.000000000000000000 ) ) ;
#9596=EDGE_CURVE ( 'NONE', #7880, #13054, #19009, .T. ) ;
#9603=EDGE_CURVE ( 'NONE', #18852, #11835, #44230, .T. ) ;
#9611=ADVANCED_FACE ( 'NONE', ( #2862 ), #25845, .T. ) ;
#9628=ORIENTED_EDGE ( 'NONE', *, *, #17391, .F. ) ;
#9632=ADVANCED_FACE ( 'NONE', ( #6301 ), #18264, .T. ) ;
#9636=CYLINDRICAL_SURFACE ( 'NONE', #37506, 37.49900000000000233 ) ;
#9642=CARTESIAN_POINT ( 'NONE',  ( 4.999999999999999112, -2.663952781845850826, -41.91543099594819921 ) ) ;
#9649=CARTESIAN_POINT ( 'NONE',  ( 0.000000000000000000, 36.13751322684449008, -21.40280677340332716 ) ) ;
#9656=ORIENTED_EDGE ( 'NONE', *, *, #8742, .T. ) ;
#9658=EDGE_CURVE ( 'NONE', #19451, #13273, #15956, .T. ) ;
#9674=EDGE_CURVE ( 'NONE', #32864, #33539, #24544, .T. ) ;
#9675=LINE ( 'NONE', #25084, #25154 ) ;
#9678=CIRCLE ( 'NONE', #37031, 15.99999999999999645 ) ;
#9702=DIRECTION ( 'NONE',  ( 0.000000000000000000, -0.1564344650402170189, -0.9876883405951399908 ) ) ;
#9709=EDGE_LOOP ( 'NONE', ( #34156, #33064, #14652, #14902 ) ) ;
#9718=VECTOR ( 'NONE', #9382, 1000.000000000000000 ) ;
#9727=DIRECTION ( 'NONE',  ( 0.000000000000000000, 0.000000000000000000, 1.000000000000000000 ) ) ;
#9759=LINE ( 'NONE', #5866, #25339 ) ;
#9773=ORIENTED_EDGE ( 'NONE', *, *, #35172, .F. ) ;
#9785=CARTESIAN_POINT ( 'NONE',  ( 10.00000000000000000, 27.13269053701096922, 25.88420570971410228 ) ) ;
#9795=CARTESIAN_POINT ( 'NONE',  ( 10.00000000000000000, 33.79645857604513992, -16.45098606841138178 ) ) ;
#9808=FACE_OUTER_BOUND ( 'NONE', #40547, .T. ) ;
#9822=CARTESIAN_POINT ( 'NONE',  ( 10.00000000000000000, -33.00180498840035170, -17.80606268964575278 ) ) ;
#9829=AXIS2_PLACEMENT_3D ( 'NONE', #32756, #43319, #6586 ) ;
#9831=DIRECTION ( 'NONE',  ( -1.000000000000000000, 0.000000000000000000, 0.000000000000000000 ) ) ;
#9841=DIRECTION ( 'NONE',  ( 1.000000000000000000, -0.000000000000000000, 0.000000000000000000 ) ) ;
#9842=EDGE_CURVE ( 'NONE', #842, #45536, #19040, .T. ) ;
#9846=VECTOR ( 'NONE', #44427, 1000.000000000000000 ) ;
#9872=STYLED_ITEM ( 'NONE', ( #6027 ), #2442 ) ;
#9890=ORIENTED_EDGE ( 'NONE', *, *, #1740, .F. ) ;
#9893=EDGE_CURVE ( 'NONE', #26166, #11716, #18743, .T. ) ;
#9899=DIRECTION ( 'NONE',  ( -1.000000000000000000, 0.000000000000000000, -0.000000000000000000 ) ) ;
#9900=VERTEX_POINT ( 'NONE', #5767 ) ;
#9905=EDGE_CURVE ( 'NONE', #46331, #8930, #31003, .T. ) ;
#9908=EDGE_LOOP ( 'NONE', ( #263, #23972, #17455, #46178 ) ) ;
#9928=CARTESIAN_POINT ( 'NONE',  ( 0.000000000000000000, 27.75498641678786527, -31.52238457039571173 ) ) ;
#9930=AXIS2_PLACEMENT_3D ( 'NONE', #30037, #46172, #5781 ) ;
#9985=DIRECTION ( 'NONE',  ( -1.000000000000000000, 0.000000000000000000, 0.000000000000000000 ) ) ;
#9992=ORIENTED_EDGE ( 'NONE', *, *, #12922, .T. ) ;
#9994=EDGE_CURVE ( 'NONE', #4312, #25302, #5791, .T. ) ;
#10018=CARTESIAN_POINT ( 'NONE',  ( 10.00000000000000000, 37.01155633439059756, 6.555932627142549762 ) ) ;
#10020=DIRECTION ( 'NONE',  ( 1.000000000000000000, -0.000000000000000000, -0.000000000000000000 ) ) ;
#10047=CYLINDRICAL_SURFACE ( 'NONE', #31995, 42.00000000000000000 ) ;
#10066=DIRECTION ( 'NONE',  ( -1.000000000000000000, -0.000000000000000000, 0.000000000000000000 ) ) ;
#10072=DIRECTION ( 'NONE',  ( 1.000000000000000000, -0.000000000000000000, 0.000000000000000000 ) ) ;
#10085=ORIENTED_EDGE ( 'NONE', *, *, #42785, .T. ) ;
#10089=DIRECTION ( 'NONE',  ( -1.000000000000000000, 0.000000000000000000, -0.000000000000000000 ) ) ;
#10093=CARTESIAN_POINT ( 'NONE',  ( 10.00000000000000000, -38.55633173626998911, -16.65560815589452304 ) ) ;
#10100=( GEOMETRIC_REPRESENTATION_CONTEXT ( 3 ) GLOBAL_UNCERTAINTY_ASSIGNED_CONTEXT ( ( #11989 ) ) GLOBAL_UNIT_ASSIGNED_CONTEXT ( ( #4101, #15371, #27109 ) ) REPRESENTATION_CONTEXT ( 'NONE', 'WORKASPACE' ) );
#10111=EDGE_CURVE ( 'NONE', #1904, #41511, #19640, .T. ) ;
#10121=ORIENTED_EDGE ( 'NONE', *, *, #23197, .T. ) ;
#10122=EDGE_CURVE ( 'NONE', #36840, #12477, #40732, .T. ) ;
#10139=AXIS2_PLACEMENT_3D ( 'NONE', #18589, #13721, #22266 ) ;
#10140=EDGE_LOOP ( 'NONE', ( #7067, #23923, #45046, #35225 ) ) ;
#10151=DIRECTION ( 'NONE',  ( 1.000000000000000000, -0.000000000000000000, -0.000000000000000000 ) ) ;
#10154=DIRECTION ( 'NONE',  ( 0.000000000000000000, 0.000000000000000000, 1.000000000000000000 ) ) ;
#10157=ORIENTED_EDGE ( 'NONE', *, *, #978, .F. ) ;
#10160=EDGE_CURVE ( 'NONE', #10554, #34876, #21158, .T. ) ;
#10174=ORIENTED_EDGE ( 'NONE', *, *, #9495, .F. ) ;
#10176=EDGE_CURVE ( 'NONE', #22407, #43729, #47111, .T. ) ;
#10188=CARTESIAN_POINT ( 'NONE',  ( 0.000000000000000000, -35.53030884539094103, 12.26510123303246935 ) ) ;
#10198=ORIENTED_EDGE ( 'NONE', *, *, #26210, .F. ) ;
#10213=ORIENTED_EDGE ( 'NONE', *, *, #43219, .T. ) ;
#10226=DIRECTION ( 'NONE',  ( -1.000000000000000000, -0.000000000000000000, -0.000000000000000000 ) ) ;
#10244=ORIENTED_EDGE ( 'NONE', *, *, #456, .T. ) ;
#10258=ORIENTED_EDGE ( 'NONE', *, *, #4216, .T. ) ;
#10266=EDGE_LOOP ( 'NONE', ( #36371, #28776, #40455, #29392 ) ) ;
#10269=CARTESIAN_POINT ( 'NONE',  ( 10.00000000000000000, 0.000000000000000000, 0.000000000000000000 ) ) ;
#10271=EDGE_CURVE ( 'NONE', #5836, #47967, #37548, .T. ) ;
#10274=AXIS2_PLACEMENT_3D ( 'NONE', #23173, #14865, #15827 ) ;
#10278=EDGE_CURVE ( 'NONE', #13273, #47647, #35207, .T. ) ;
#10279=CIRCLE ( 'NONE', #111, 37.49900000000000944 ) ;
#10280=AXIS2_PLACEMENT_3D ( 'NONE', #11425, #3819, #18734 ) ;
#10290=VECTOR ( 'NONE', #12262, 1000.000000000000000 ) ;
#10308=DIRECTION ( 'NONE',  ( -1.000000000000000000, 0.000000000000000000, 0.000000000000000000 ) ) ;
#10331=EDGE_CURVE ( 'NONE', #47530, #12539, #30215, .T. ) ;
#10341=ORIENTED_EDGE ( 'NONE', *, *, #42452, .F. ) ;
#10357=CIRCLE ( 'NONE', #25193, 16.00000000000000000 ) ;
#10361=CARTESIAN_POINT ( 'NONE',  ( 10.00000000000000000, -22.48208911017525580, 35.47612816024516036 ) ) ;
#10366=ORIENTED_EDGE ( 'NONE', *, *, #19208, .F. ) ;
#10367=DIRECTION ( 'NONE',  ( 0.000000000000000000, 0.000000000000000000, 1.000000000000000000 ) ) ;
#10370=EDGE_CURVE ( 'NONE', #451, #20, #13290, .T. ) ;
#10383=VERTEX_POINT ( 'NONE', #42677 ) ;
#10392=DIRECTION ( 'NONE',  ( -1.000000000000000000, 0.000000000000000000, 0.000000000000000000 ) ) ;
#10397=CARTESIAN_POINT ( 'NONE',  ( 0.000000000000000000, -33.79645857604501913, -16.45098606841161626 ) ) ;
#10410=VERTEX_POINT ( 'NONE', #5459 ) ;
#10414=ORIENTED_EDGE ( 'NONE', *, *, #19943, .F. ) ;
#10416=ORIENTED_EDGE ( 'NONE', *, *, #30802, .F. ) ;
#10417=VECTOR ( 'NONE', #20203, 1000.000000000000000 ) ;
#10419=DIRECTION ( 'NONE',  ( -1.000000000000000000, -0.000000000000000000, 0.000000000000000000 ) ) ;
#10421=CIRCLE ( 'NONE', #4181, 16.00000000000000000 ) ;
#10423=ADVANCED_FACE ( 'NONE', ( #30944 ), #38999, .T. ) ;
#10428=CYLINDRICAL_SURFACE ( 'NONE', #45287, 42.00000000000000000 ) ;
#10440=DIRECTION ( 'NONE',  ( 0.000000000000000000, 0.000000000000000000, 1.000000000000000000 ) ) ;
#10448=DIRECTION ( 'NONE',  ( -1.000000000000000000, -0.000000000000000000, 0.000000000000000000 ) ) ;
#10451=DIRECTION ( 'NONE',  ( -1.000000000000000000, -0.000000000000000000, -0.000000000000000000 ) ) ;
#10467=FACE_OUTER_BOUND ( 'NONE', #1160, .T. ) ;
#10468=CARTESIAN_POINT ( 'NONE',  ( 10.00000000000000000, -6.555932627142676772, 37.01155633439056203 ) ) ;
#10474=CARTESIAN_POINT ( 'NONE',  ( 0.000000000000000000, 41.81611651403868990, -3.925862922255709542 ) ) ;
#10475=CIRCLE ( 'NONE', #16738, 16.00000000000000000 ) ;
#10488=ADVANCED_FACE ( 'NONE', ( #8886 ), #16724, .T. ) ;
#10504=DIRECTION ( 'NONE',  ( -1.000000000000000000, 0.000000000000000000, 0.000000000000000000 ) ) ;
#10508=AXIS2_PLACEMENT_3D ( 'NONE', #29857, #30115, #45040 ) ;
#10510=ORIENTED_EDGE ( 'NONE', *, *, #37028, .T. ) ;
#10513=ORIENTED_EDGE ( 'NONE', *, *, #41227, .T. ) ;
#10520=DIRECTION ( 'NONE',  ( -1.000000000000000000, -0.000000000000000000, 0.000000000000000000 ) ) ;
#10528=CYLINDRICAL_SURFACE ( 'NONE', #1278, 42.00000000000000000 ) ;
#10530=CIRCLE ( 'NONE', #30061, 42.00000000000000000 ) ;
#10545=ORIENTED_EDGE ( 'NONE', *, *, #45822, .T. ) ;
#10547=DIRECTION ( 'NONE',  ( 1.000000000000000000, -0.000000000000000000, -0.000000000000000000 ) ) ;
#10553=CARTESIAN_POINT ( 'NONE',  ( 0.000000000000000000, -4.992566952384716927, -37.16516213103282951 ) ) ;
#10554=VERTEX_POINT ( 'NONE', #10093 ) ;
#10581=EDGE_LOOP ( 'NONE', ( #25840, #22171, #3812, #19930 ) ) ;
#10595=CARTESIAN_POINT ( 'NONE',  ( 5.000000000000000000, -16.65560815589439159, 38.55633173627004595 ) ) ;
#10603=FACE_OUTER_BOUND ( 'NONE', #19809, .T. ) ;
#10607=ORIENTED_EDGE ( 'NONE', *, *, #39431, .F. ) ;
#10609=EDGE_CURVE ( 'NONE', #25493, #19520, #3215, .T. ) ;
#10617=CIRCLE ( 'NONE', #8268, 16.00000000000000000 ) ;
#10625=EDGE_CURVE ( 'NONE', #45724, #47714, #35229, .T. ) ;
#10637=AXIS2_PLACEMENT_3D ( 'NONE', #6436, #40932, #25987 ) ;
#10641=ORIENTED_EDGE ( 'NONE', *, *, #38509, .T. ) ;
#10652=DIRECTION ( 'NONE',  ( 0.000000000000000000, -9.787530781167598712E-16, -1.000000000000000000 ) ) ;
#10662=CARTESIAN_POINT ( 'NONE',  ( 5.000000000000000000, -15.48615015657610705, 39.04073710021338428 ) ) ;
#10665=ORIENTED_EDGE ( 'NONE', *, *, #45855, .F. ) ;
#10673=AXIS2_PLACEMENT_3D ( 'NONE', #27395, #42571, #13422 ) ;
#10692=CARTESIAN_POINT ( 'NONE',  ( 0.000000000000000000, -41.81611651403859042, -3.925862922256606602 ) ) ;
#10693=EDGE_CURVE ( 'NONE', #8092, #8291, #47690, .T. ) ;
#10702=DIRECTION ( 'NONE',  ( -1.000000000000000000, 0.000000000000000000, -0.000000000000000000 ) ) ;
#10705=DIRECTION ( 'NONE',  ( 0.000000000000000000, 0.000000000000000000, 1.000000000000000000 ) ) ;
#10713=DIRECTION ( 'NONE',  ( -1.000000000000000000, -0.000000000000000000, -0.000000000000000000 ) ) ;
#10714=DIRECTION ( 'NONE',  ( 0.000000000000000000, 0.000000000000000000, 1.000000000000000000 ) ) ;
#10717=DIRECTION ( 'NONE',  ( 0.000000000000000000, 0.000000000000000000, 1.000000000000000000 ) ) ;
#10727=ADVANCED_FACE ( 'NONE', ( #34283 ), #754, .T. ) ;
#10734=CARTESIAN_POINT ( 'NONE',  ( -10.00000000000000000, 0.000000000000000000, 0.000000000000000000 ) ) ;
#10735=DIRECTION ( 'NONE',  ( 0.000000000000000000, 8.881784197001252323E-16, 1.000000000000000000 ) ) ;
#10746=ORIENTED_EDGE ( 'NONE', *, *, #44968, .F. ) ;
#10750=AXIS2_PLACEMENT_3D ( 'NONE', #884, #15831, #30763 ) ;
#10763=ORIENTED_EDGE ( 'NONE', *, *, #34708, .T. ) ;
#10786=CIRCLE ( 'NONE', #42829, 16.00000000000000000 ) ;
#10796=ORIENTED_EDGE ( 'NONE', *, *, #36365, .F. ) ;
#10797=DIRECTION ( 'NONE',  ( -1.000000000000000000, 0.000000000000000000, 0.000000000000000000 ) ) ;
#10804=ORIENTED_EDGE ( 'NONE', *, *, #26016, .T. ) ;
#10813=CARTESIAN_POINT ( 'NONE',  ( 4.999999999999999112, 2.663952781846732343, -41.91543099594814947 ) ) ;
#10819=DIRECTION ( 'NONE',  ( -1.000000000000000000, -0.000000000000000000, -0.000000000000000000 ) ) ;
#10820=CIRCLE ( 'NONE', #37396, 16.00000000000000000 ) ;
#10823=DIRECTION ( 'NONE',  ( 0.000000000000000000, 0.000000000000000000, 1.000000000000000000 ) ) ;
#10835=ADVANCED_FACE ( 'NONE', ( #24242 ), #5648, .T. ) ;
#10843=AXIS2_PLACEMENT_3D ( 'NONE', #11079, #43882, #25262 ) ;
#10850=DIRECTION ( 'NONE',  ( -1.000000000000000000, 0.000000000000000000, -0.000000000000000000 ) ) ;
#10858=DIRECTION ( 'NONE',  ( -1.000000000000000000, -0.000000000000000000, -0.000000000000000000 ) ) ;
#10859=LINE ( 'NONE', #566, #22643 ) ;
#10861=ORIENTED_EDGE ( 'NONE', *, *, #4440, .T. ) ;
#10863=AXIS2_PLACEMENT_3D ( 'NONE', #12720, #20290, #28365 ) ;
#10876=DIRECTION ( 'NONE',  ( 0.000000000000000000, 1.000000000000000000, 3.491481338843133750E-15 ) ) ;
#10891=DIRECTION ( 'NONE',  ( 0.000000000000000000, 0.000000000000000000, 1.000000000000000000 ) ) ;
#10894=DIRECTION ( 'NONE',  ( -1.000000000000000000, -0.000000000000000000, -0.000000000000000000 ) ) ;
#10906=ADVANCED_FACE ( 'NONE', ( #8580 ), #23513, .T. ) ;
#10908=ORIENTED_EDGE ( 'NONE', *, *, #45855, .T. ) ;
#10912=DIRECTION ( 'NONE',  ( 1.000000000000000000, 0.000000000000000000, 0.000000000000000000 ) ) ;
#10918=VERTEX_POINT ( 'NONE', #36219 ) ;
#10921=CYLINDRICAL_SURFACE ( 'NONE', #13136, 12.50000000000000000 ) ;
#10927=VECTOR ( 'NONE', #12089, 1000.000000000000000 ) ;
#10928=DIRECTION ( 'NONE',  ( 1.000000000000000000, 0.000000000000000000, 0.000000000000000000 ) ) ;
#10929=ORIENTED_EDGE ( 'NONE', *, *, #31578, .F. ) ;
#10931=ADVANCED_FACE ( 'NONE', ( #6133 ), #14189, .T. ) ;
#10944=FACE_OUTER_BOUND ( 'NONE', #30301, .T. ) ;
#10946=ADVANCED_FACE ( 'NONE', ( #40391 ), #17615, .T. ) ;
#10948=ADVANCED_FACE ( 'NONE', ( #32085 ), #13469, .T. ) ;
#10949=CARTESIAN_POINT ( 'NONE',  ( 0.000000000000000000, 0.000000000000000000, 0.000000000000000000 ) ) ;
#10962=EDGE_LOOP ( 'NONE', ( #26455, #34328, #27277, #12216 ) ) ;
#10985=CYLINDRICAL_SURFACE ( 'NONE', #26242, 42.00000000000000000 ) ;
#10989=VECTOR ( 'NONE', #25969, 1000.000000000000000 ) ;
#11001=CARTESIAN_POINT ( 'NONE',  ( 10.00000000000000000, -0.6853352020787742971, -37.58145647212455032 ) ) ;
#11012=CARTESIAN_POINT ( 'NONE',  ( 0.000000000000000000, 21.40280677340421889, -36.13751322684397138 ) ) ;
#11014=ORIENTED_EDGE ( 'NONE', *, *, #29102, .F. ) ;
#11018=PRODUCT_DEFINITION_CONTEXT ( 'detailed design', #40098, 'design' ) ;
#11024=CIRCLE ( 'NONE', #29011, 42.00000000000000000 ) ;
#11026=AXIS2_PLACEMENT_3D ( 'NONE', #9016, #46712, #31546 ) ;
#11031=ORIENTED_EDGE ( 'NONE', *, *, #38591, .T. ) ;
#11039=ADVANCED_FACE ( 'NONE', ( #13719 ), #28648, .T. ) ;
#11050=VERTEX_POINT ( 'NONE', #30095 ) ;
#11056=DIRECTION ( 'NONE',  ( 0.000000000000000000, 0.000000000000000000, 1.000000000000000000 ) ) ;
#11072=VECTOR ( 'NONE', #45359, 1000.000000000000000 ) ;
#11079=CARTESIAN_POINT ( 'NONE',  ( 10.00000000000000000, 22.64427369931212297, -30.00120703465181293 ) ) ;
#11091=EDGE_LOOP ( 'NONE', ( #3821, #20292, #36054, #14889 ) ) ;
#11108=ADVANCED_FACE ( 'NONE', ( #33742 ), #22736, .T. ) ;
#11109=CARTESIAN_POINT ( 'NONE',  ( 0.000000000000000000, 0.8828120875905820508, -37.48860685352290290 ) ) ;
#11115=EDGE_CURVE ( 'NONE', #22715, #13193, #18063, .T. ) ;
#11116=DIRECTION ( 'NONE',  ( 1.000000000000000000, 0.000000000000000000, 0.000000000000000000 ) ) ;
#11122=DIRECTION ( 'NONE',  ( 0.000000000000000000, 0.7071067811865437980, 0.7071067811865512365 ) ) ;
#11124=CARTESIAN_POINT ( 'NONE',  ( 10.00000000000000000, 41.91543099594818500, 2.663952781846293139 ) ) ;
#11143=ADVANCED_FACE ( 'NONE', ( #26660 ), #8043, .T. ) ;
#11146=ORIENTED_EDGE ( 'NONE', *, *, #38509, .F. ) ;
#11152=ORIENTED_EDGE ( 'NONE', *, *, #33361, .T. ) ;
#11154=EDGE_CURVE ( 'NONE', #25587, #14954, #6778, .T. ) ;
#11161=CIRCLE ( 'NONE', #14304, 16.00000000000000000 ) ;
#11171=ORIENTED_EDGE ( 'NONE', *, *, #808, .F. ) ;
#11181=FACE_OUTER_BOUND ( 'NONE', #3135, .T. ) ;
#11185=DIRECTION ( 'NONE',  ( 0.000000000000000000, 0.9510565162951523099, 0.3090169943749517811 ) ) ;
#11190=CYLINDRICAL_SURFACE ( 'NONE', #10274, 37.49900000000000233 ) ;
#11196=ORIENTED_EDGE ( 'NONE', *, *, #6452, .F. ) ;
#11197=LINE ( 'NONE', #42256, #34910 ) ;
#11209=VERTEX_POINT ( 'NONE', #4865 ) ;
#11214=DIRECTION ( 'NONE',  ( -1.000000000000000000, -0.000000000000000000, -0.000000000000000000 ) ) ;
#11233=EDGE_CURVE ( 'NONE', #8001, #13193, #1443, .T. ) ;
#11243=ORIENTED_EDGE ( 'NONE', *, *, #12788, .F. ) ;
#11252=CARTESIAN_POINT ( 'NONE',  ( 0.000000000000000000, -29.81001611431024045, 22.74946021919122430 ) ) ;
#11254=DIRECTION ( 'NONE',  ( -1.000000000000000000, 0.000000000000000000, 0.000000000000000000 ) ) ;
#11271=EDGE_CURVE ( 'NONE', #42124, #43612, #27151, .T. ) ;
#11280=CIRCLE ( 'NONE', #31636, 12.50000000000000000 ) ;
#11282=ORIENTED_EDGE ( 'NONE', *, *, #6934, .T. ) ;
#11296=CARTESIAN_POINT ( 'NONE',  ( 10.00000000000000000, -29.81001611431024756, 22.74946021919122785 ) ) ;
#11306=DIRECTION ( 'NONE',  ( -1.000000000000000000, 0.000000000000000000, -0.000000000000000000 ) ) ;
#11326=CARTESIAN_POINT ( 'NONE',  ( 0.000000000000000000, 0.000000000000000000, 0.000000000000000000 ) ) ;
#11339=ORIENTED_EDGE ( 'NONE', *, *, #30562, .F. ) ;
#11364=DIRECTION ( 'NONE',  ( -1.000000000000000000, 0.000000000000000000, 0.000000000000000000 ) ) ;
#11366=DIRECTION ( 'NONE',  ( 0.000000000000000000, 0.8910065241883688980, -0.4539904997395447506 ) ) ;
#11373=DIRECTION ( 'NONE',  ( 0.000000000000000000, 0.000000000000000000, -1.000000000000000000 ) ) ;
#11383=AXIS2_PLACEMENT_3D ( 'NONE', #43875, #7152, #40218 ) ;
#11385=LINE ( 'NONE', #41240, #44136 ) ;
#11388=FACE_OUTER_BOUND ( 'NONE', #32602, .T. ) ;
#11400=ADVANCED_FACE ( 'NONE', ( #25802 ), #6317, .T. ) ;
#11409=DIRECTION ( 'NONE',  ( 0.000000000000000000, 0.000000000000000000, 1.000000000000000000 ) ) ;
#11424=EDGE_CURVE ( 'NONE', #26639, #22815, #35710, .T. ) ;
#11425=CARTESIAN_POINT ( 'NONE',  ( 10.00000000000000000, 0.000000000000000000, 0.000000000000000000 ) ) ;
#11428=EDGE_LOOP ( 'NONE', ( #9239, #46216, #20540, #46677 ) ) ;
#11439=DIRECTION ( 'NONE',  ( 0.000000000000000000, 0.000000000000000000, 1.000000000000000000 ) ) ;
#11450=CIRCLE ( 'NONE', #38798, 16.00000000000000000 ) ;
#11457=DIRECTION ( 'NONE',  ( 0.000000000000000000, 0.000000000000000000, 1.000000000000000000 ) ) ;
#11465=ADVANCED_FACE ( 'NONE', ( #97 ), #34346, .T. ) ;
#11468=DIRECTION ( 'NONE',  ( -1.000000000000000000, -0.000000000000000000, -0.000000000000000000 ) ) ;
#11475=AXIS2_PLACEMENT_3D ( 'NONE', #32972, #22460, #48387 ) ;
#11478=CIRCLE ( 'NONE', #36479, 16.00000000000000000 ) ;
#11479=DIRECTION ( 'NONE',  ( -1.000000000000000000, 0.000000000000000000, 0.000000000000000000 ) ) ;
#11480=ORIENTED_EDGE ( 'NONE', *, *, #22995, .T. ) ;
#11486=ORIENTED_EDGE ( 'NONE', *, *, #43826, .F. ) ;
#11493=DIRECTION ( 'NONE',  ( 0.000000000000000000, 0.9876883405951372152, 0.1564344650402347547 ) ) ;
#11510=CIRCLE ( 'NONE', #38866, 16.00000000000000000 ) ;
#11516=EDGE_CURVE ( 'NONE', #15480, #42450, #34158, .T. ) ;
#11527=VERTEX_POINT ( 'NONE', #45618 ) ;
#11539=LINE ( 'NONE', #26463, #39614 ) ;
#11551=ORIENTED_EDGE ( 'NONE', *, *, #41609, .T. ) ;
#11554=DIRECTION ( 'NONE',  ( 0.000000000000000000, -0.1564344650402380854, 0.9876883405951365491 ) ) ;
#11560=AXIS2_PLACEMENT_3D ( 'NONE', #31908, #43146, #35560 ) ;
#11562=DIRECTION ( 'NONE',  ( 0.000000000000000000, 0.8090169943749447867, 0.5877852522924769119 ) ) ;
#11563=CARTESIAN_POINT ( 'NONE',  ( 0.000000000000000000, 0.000000000000000000, 0.000000000000000000 ) ) ;
#11564=CARTESIAN_POINT ( 'NONE',  ( 0.000000000000000000, -6.736453364083817341, 36.88895765772630142 ) ) ;
#11565=FACE_OUTER_BOUND ( 'NONE', #43369, .T. ) ;
#11571=DIRECTION ( 'NONE',  ( -1.000000000000000000, 0.000000000000000000, 0.000000000000000000 ) ) ;
#11595=DIRECTION ( 'NONE',  ( 0.000000000000000000, 0.000000000000000000, 1.000000000000000000 ) ) ;
#11606=VERTEX_POINT ( 'NONE', #24082 ) ;
#11628=AXIS2_PLACEMENT_3D ( 'NONE', #20028, #46718, #43034 ) ;
#11636=AXIS2_PLACEMENT_3D ( 'NONE', #13959, #6619, #3667 ) ;
#11653=ORIENTED_EDGE ( 'NONE', *, *, #30664, .T. ) ;
#11660=CARTESIAN_POINT ( 'NONE',  ( 10.00000000000000000, 33.17418723428333749, -17.67226234102790272 ) ) ;
#11665=DIRECTION ( 'NONE',  ( -1.000000000000000000, 0.000000000000000000, -0.000000000000000000 ) ) ;
#11674=DIRECTION ( 'NONE',  ( -1.000000000000000000, 0.000000000000000000, -0.000000000000000000 ) ) ;
#11687=ADVANCED_FACE ( 'NONE', ( #43163 ), #12349, .T. ) ;
#11695=VECTOR ( 'NONE', #3266, 1000.000000000000000 ) ;
#11702=ORIENTED_EDGE ( 'NONE', *, *, #47263, .T. ) ;
#11708=ORIENTED_EDGE ( 'NONE', *, *, #14658, .T. ) ;
#11716=VERTEX_POINT ( 'NONE', #44362 ) ;
#11717=DIRECTION ( 'NONE',  ( 0.000000000000000000, 0.8910065241883688980, -0.4539904997395445840 ) ) ;
#11722=VECTOR ( 'NONE', #25284, 1000.000000000000000 ) ;
#11727=CARTESIAN_POINT ( 'NONE',  ( 10.00000000000000000, -33.17418723428319538, 17.67226234102814431 ) ) ;
#11733=DIRECTION ( 'NONE',  ( 0.000000000000000000, 0.5877852522924685852, 0.8090169943749508930 ) ) ;
#11734=CARTESIAN_POINT ( 'NONE',  ( 10.00000000000000000, -35.53030884539077050, -12.26510123303296851 ) ) ;
#11739=LINE ( 'NONE', #23465, #40929 ) ;
#11754=AXIS2_PLACEMENT_3D ( 'NONE', #35370, #46648, #13111 ) ;
#11755=CIRCLE ( 'NONE', #16442, 12.50000000000000000 ) ;
#11765=ORIENTED_EDGE ( 'NONE', *, *, #14278, .T. ) ;
#11767=DIRECTION ( 'NONE',  ( 0.000000000000000000, 0.000000000000000000, 1.000000000000000000 ) ) ;
#11771=DIRECTION ( 'NONE',  ( -1.000000000000000000, 0.000000000000000000, 0.000000000000000000 ) ) ;
#11772=DIRECTION ( 'NONE',  ( -1.000000000000000000, 0.000000000000000000, -0.000000000000000000 ) ) ;
#11784=DIRECTION ( 'NONE',  ( -1.000000000000000000, -0.000000000000000000, -0.000000000000000000 ) ) ;
#11785=EDGE_CURVE ( 'NONE', #18781, #1295, #25254, .T. ) ;
#11786=CARTESIAN_POINT ( 'NONE',  ( 0.000000000000000000, -35.95386929396264009, 10.96151621346475658 ) ) ;
#11805=AXIS2_PLACEMENT_3D ( 'NONE', #9795, #31859, #21280 ) ;
#11809=LINE ( 'NONE', #299, #24454 ) ;
#11815=ORIENTED_EDGE ( 'NONE', *, *, #4458, .T. ) ;
#11822=ORIENTED_EDGE ( 'NONE', *, *, #26016, .F. ) ;
#11825=ORIENTED_EDGE ( 'NONE', *, *, #33312, .F. ) ;
#11830=DIRECTION ( 'NONE',  ( 0.000000000000000000, 0.000000000000000000, 1.000000000000000000 ) ) ;
#11832=AXIS2_PLACEMENT_3D ( 'NONE', #33507, #14682, #22505 ) ;
#11835=VERTEX_POINT ( 'NONE', #28935 ) ;
#11838=ORIENTED_EDGE ( 'NONE', *, *, #32619, .F. ) ;
#11841=LINE ( 'NONE', #8407, #34000 ) ;
#11863=DIRECTION ( 'NONE',  ( 0.000000000000000000, 0.9510565162951544194, -0.3090169943749446757 ) ) ;
#11864=ORIENTED_EDGE ( 'NONE', *, *, #36579, .T. ) ;
#11869=CIRCLE ( 'NONE', #27492, 37.49900000000000233 ) ;
#11893=ORIENTED_EDGE ( 'NONE', *, *, #21558, .F. ) ;
#11897=CIRCLE ( 'NONE', #944, 16.00000000000000000 ) ;
#11902=CARTESIAN_POINT ( 'NONE',  ( 10.00000000000000000, 0.000000000000000000, 0.000000000000000000 ) ) ;
#11903=DIRECTION ( 'NONE',  ( 0.000000000000000000, 0.000000000000000000, 1.000000000000000000 ) ) ;
#11905=DIRECTION ( 'NONE',  ( -1.000000000000000000, 0.000000000000000000, 0.000000000000000000 ) ) ;
#11908=EDGE_CURVE ( 'NONE', #23982, #6451, #18876, .T. ) ;
#11909=EDGE_LOOP ( 'NONE', ( #12309, #44039, #9170, #14727 ) ) ;
#11915=CARTESIAN_POINT ( 'NONE',  ( 10.00000000000000000, 37.58145647212453611, 0.6853352020791767529 ) ) ;
#11921=ORIENTED_EDGE ( 'NONE', *, *, #10370, .T. ) ;
#11926=SURFACE_STYLE_USAGE ( .BOTH. , #26380 ) ;
#11933=VERTEX_POINT ( 'NONE', #11564 ) ;
#11942=DIRECTION ( 'NONE',  ( 0.000000000000000000, 0.000000000000000000, 1.000000000000000000 ) ) ;
#11945=ORIENTED_EDGE ( 'NONE', *, *, #32980, .F. ) ;
#11960=PLANE ( 'NONE',  #15842 ) ;
#11970=AXIS2_PLACEMENT_3D ( 'NONE', #42238, #34636, #1118 ) ;
#11976=CARTESIAN_POINT ( 'NONE',  ( 10.00000000000000000, -35.38097989696520074, 12.42422080174625520 ) ) ;
#11982=DIRECTION ( 'NONE',  ( -1.000000000000000000, -0.000000000000000000, 0.000000000000000000 ) ) ;
#11989=UNCERTAINTY_MEASURE_WITH_UNIT (LENGTH_MEASURE( 1.000000000000000082E-05 ), #4101, 'distance_accuracy_value', 'NONE');
#12010=AXIS2_PLACEMENT_3D ( 'NONE', #8961, #881, #35138 ) ;
#12011=DIRECTION ( 'NONE',  ( 0.000000000000000000, 0.000000000000000000, 1.000000000000000000 ) ) ;
#12013=AXIS2_PLACEMENT_3D ( 'NONE', #15528, #23115, #19420 ) ;
#12015=DIRECTION ( 'NONE',  ( -1.000000000000000000, 0.000000000000000000, 0.000000000000000000 ) ) ;
#12016=ADVANCED_FACE ( 'NONE', ( #46540 ), #1744, .T. ) ;
#12019=DIRECTION ( 'NONE',  ( 0.000000000000000000, 0.000000000000000000, -1.000000000000000000 ) ) ;
#12027=VERTEX_POINT ( 'NONE', #45818 ) ;
#12030=EDGE_CURVE ( 'NONE', #41330, #12321, #45145, .T. ) ;
#12043=DIRECTION ( 'NONE',  ( 0.000000000000000000, 0.000000000000000000, 1.000000000000000000 ) ) ;
#12046=DIRECTION ( 'NONE',  ( 0.000000000000000000, 0.000000000000000000, 1.000000000000000000 ) ) ;
#12068=CIRCLE ( 'NONE', #8009, 16.00000000000000000 ) ;
#12079=CARTESIAN_POINT ( 'NONE',  ( 10.00000000000000000, -12.42422080174663712, 35.38097989696507994 ) ) ;
#12084=ORIENTED_EDGE ( 'NONE', *, *, #17413, .T. ) ;
#12089=DIRECTION ( 'NONE',  ( -1.000000000000000000, 0.000000000000000000, 0.000000000000000000 ) ) ;
#12104=AXIS2_PLACEMENT_3D ( 'NONE', #34242, #27643, #15899 ) ;
#12143=EDGE_CURVE ( 'NONE', #39399, #6463, #38901, .T. ) ;
#12149=CARTESIAN_POINT ( 'NONE',  ( 0.000000000000000000, 33.00180498840072829, -17.80606268964504935 ) ) ;
#12170=EDGE_LOOP ( 'NONE', ( #30878, #19740, #36368, #19723 ) ) ;
#12174=AXIS2_PLACEMENT_3D ( 'NONE', #29104, #25430, #33014 ) ;
#12178=EDGE_CURVE ( 'NONE', #6290, #15060, #22472, .T. ) ;
#12189=ORIENTED_EDGE ( 'NONE', *, *, #13061, .T. ) ;
#12194=CIRCLE ( 'NONE', #9829, 37.49900000000000233 ) ;
#12198=AXIS2_PLACEMENT_3D ( 'NONE', #44887, #11116, #11373 ) ;
#12201=ORIENTED_EDGE ( 'NONE', *, *, #42968, .T. ) ;
#12207=ORIENTED_EDGE ( 'NONE', *, *, #33958, .F. ) ;
#12216=ORIENTED_EDGE ( 'NONE', *, *, #3922, .T. ) ;
#12227=DIRECTION ( 'NONE',  ( 0.000000000000000000, 0.000000000000000000, -1.000000000000000000 ) ) ;
#12233=AXIS2_PLACEMENT_3D ( 'NONE', #36621, #14847, #3085 ) ;
#12237=DIRECTION ( 'NONE',  ( -1.000000000000000000, 0.000000000000000000, 0.000000000000000000 ) ) ;
#12252=ORIENTED_EDGE ( 'NONE', *, *, #47091, .T. ) ;
#12262=DIRECTION ( 'NONE',  ( -1.000000000000000000, -0.000000000000000000, 0.000000000000000000 ) ) ;
#12264=CIRCLE ( 'NONE', #6768, 16.00000000000000000 ) ;
#12268=CARTESIAN_POINT ( 'NONE',  ( 10.00000000000000000, 0.000000000000000000, 0.000000000000000000 ) ) ;
#12287=CARTESIAN_POINT ( 'NONE',  ( 0.000000000000000000, 38.55633173627010279, 16.65560815589424593 ) ) ;
#12288=AXIS2_PLACEMENT_3D ( 'NONE', #20456, #16088, #42503 ) ;
#12289=DIRECTION ( 'NONE',  ( 1.000000000000000000, 0.000000000000000000, 0.000000000000000000 ) ) ;
#12294=ORIENTED_EDGE ( 'NONE', *, *, #22596, .T. ) ;
#12301=ORIENTED_EDGE ( 'NONE', *, *, #12030, .F. ) ;
#12309=ORIENTED_EDGE ( 'NONE', *, *, #39691, .F. ) ;
#12316=FACE_OUTER_BOUND ( 'NONE', #45403, .T. ) ;
#12321=VERTEX_POINT ( 'NONE', #39803 ) ;
#12327=EDGE_LOOP ( 'NONE', ( #19579, #41452, #26835, #18336 ) ) ;
#12331=EDGE_CURVE ( 'NONE', #21662, #18852, #36277, .T. ) ;
#12345=AXIS2_PLACEMENT_3D ( 'NONE', #26611, #19981, #23650 ) ;
#12349=CYLINDRICAL_SURFACE ( 'NONE', #5252, 16.00000000000000000 ) ;
#12355=DIRECTION ( 'NONE',  ( -1.000000000000000000, 0.000000000000000000, 0.000000000000000000 ) ) ;
#12366=ORIENTED_EDGE ( 'NONE', *, *, #2016, .T. ) ;
#12373=EDGE_LOOP ( 'NONE', ( #7541, #3033, #10763, #46094 ) ) ;
#12383=CYLINDRICAL_SURFACE ( 'NONE', #9144, 12.50000000000000000 ) ;
#12384=ORIENTED_EDGE ( 'NONE', *, *, #38679, .F. ) ;
#12393=DIRECTION ( 'NONE',  ( 0.000000000000000000, -0.4539904997395541320, 0.8910065241883640130 ) ) ;
#12395=CARTESIAN_POINT ( 'NONE',  ( 0.000000000000000000, 9.188173127307290855, 40.98264845739752360 ) ) ;
#12403=EDGE_CURVE ( 'NONE', #9900, #43945, #15957, .T. ) ;
#12410=DIRECTION ( 'NONE',  ( -1.000000000000000000, 0.000000000000000000, 0.000000000000000000 ) ) ;
#12421=ORIENTED_EDGE ( 'NONE', *, *, #24813, .F. ) ;
#12424=DIRECTION ( 'NONE',  ( -1.000000000000000000, 0.000000000000000000, 0.000000000000000000 ) ) ;
#12440=DIRECTION ( 'NONE',  ( 0.000000000000000000, 0.8910065241883688980, -0.4539904997395446951 ) ) ;
#12450=AXIS2_PLACEMENT_3D ( 'NONE', #35518, #27955, #42873 ) ;
#12453=ORIENTED_EDGE ( 'NONE', *, *, #20046, .F. ) ;
#12458=CARTESIAN_POINT ( 'NONE',  ( 0.000000000000000000, 37.22597642581158084, -5.202137450156524068 ) ) ;
#12459=EDGE_CURVE ( 'NONE', #22407, #37035, #5792, .T. ) ;
#12464=AXIS2_PLACEMENT_3D ( 'NONE', #23286, #7634, #30631 ) ;
#12470=ORIENTED_EDGE ( 'NONE', *, *, #3713, .T. ) ;
#12477=VERTEX_POINT ( 'NONE', #17753 ) ;
#12482=ORIENTED_EDGE ( 'NONE', *, *, #6405, .T. ) ;
#12501=EDGE_CURVE ( 'NONE', #36119, #48169, #33931, .T. ) ;
#12508=CARTESIAN_POINT ( 'NONE',  ( 10.00000000000000000, 0.000000000000000000, 0.000000000000000000 ) ) ;
#12512=FACE_OUTER_BOUND ( 'NONE', #32750, .T. ) ;
#12519=CARTESIAN_POINT ( 'NONE',  ( 10.00000000000000000, 0.000000000000000000, 0.000000000000000000 ) ) ;
#12539=VERTEX_POINT ( 'NONE', #43700 ) ;
#12548=DIRECTION ( 'NONE',  ( 0.000000000000000000, 0.8090169943749445647, 0.5877852522924770229 ) ) ;
#12557=EDGE_CURVE ( 'NONE', #9289, #47392, #21671, .T. ) ;
#12559=CIRCLE ( 'NONE', #40704, 37.49900000000001654 ) ;
#12560=CARTESIAN_POINT ( 'NONE',  ( 10.00000000000000000, -0.8828120875903202602, 37.48860685352291000 ) ) ;
#12577=EDGE_CURVE ( 'NONE', #6444, #22246, #37855, .T. ) ;
#12590=CYLINDRICAL_SURFACE ( 'NONE', #5005, 16.00000000000000000 ) ;
#12594=EDGE_CURVE ( 'NONE', #38214, #27745, #30231, .T. ) ;
#12600=VERTEX_POINT ( 'NONE', #44910 ) ;
#12601=EDGE_CURVE ( 'NONE', #3686, #22056, #41721, .T. ) ;
#12602=CIRCLE ( 'NONE', #7148, 15.99999999999999822 ) ;
#12610=FACE_OUTER_BOUND ( 'NONE', #39752, .T. ) ;
#12612=ORIENTED_EDGE ( 'NONE', *, *, #24109, .T. ) ;
#12688=ORIENTED_EDGE ( 'NONE', *, *, #2144, .F. ) ;
#12694=CIRCLE ( 'NONE', #168, 16.00000000000000000 ) ;
#12720=CARTESIAN_POINT ( 'NONE',  ( 10.00000000000000000, 0.000000000000000000, 0.000000000000000000 ) ) ;
#12723=ADVANCED_FACE ( 'NONE', ( #2283 ), #16499, .T. ) ;
#12726=CIRCLE ( 'NONE', #3306, 42.00000000000000000 ) ;
#12727=CIRCLE ( 'NONE', #15066, 37.49900000000001654 ) ;
#12744=ORIENTED_EDGE ( 'NONE', *, *, #34134, .F. ) ;
#12749=CARTESIAN_POINT ( 'NONE',  ( 10.00000000000000000, 37.58145647212455032, -0.6853352020786441789 ) ) ;
#12756=DIRECTION ( 'NONE',  ( -1.000000000000000000, 0.000000000000000000, 0.000000000000000000 ) ) ;
#12759=CARTESIAN_POINT ( 'NONE',  ( 10.00000000000000000, -12.26510123303284594, 35.53030884539080603 ) ) ;
#12766=CARTESIAN_POINT ( 'NONE',  ( -10.00000000000000000, 0.000000000000000000, 0.000000000000000000 ) ) ;
#12771=CARTESIAN_POINT ( 'NONE',  ( 10.00000000000000000, -22.64427369931148348, -30.00120703465229965 ) ) ;
#12772=CARTESIAN_POINT ( 'NONE',  ( 10.00000000000000000, 0.000000000000000000, 0.000000000000000000 ) ) ;
#12788=EDGE_CURVE ( 'NONE', #34798, #30855, #28008, .T. ) ;
#12790=ORIENTED_EDGE ( 'NONE', *, *, #21162, .T. ) ;
#12801=CARTESIAN_POINT ( 'NONE',  ( 10.00000000000000000, -27.13269053701114331, 25.88420570971391754 ) ) ;
#12809=VECTOR ( 'NONE', #30179, 1000.000000000000000 ) ;
#12832=ORIENTED_EDGE ( 'NONE', *, *, #18878, .T. ) ;
#12838=EDGE_LOOP ( 'NONE', ( #39572, #13508, #18455, #2377 ) ) ;
#12840=ADVANCED_FACE ( 'NONE', ( #36055 ), #16269, .T. ) ;
#12848=VECTOR ( 'NONE', #1159, 1000.000000000000000 ) ;
#12853=CIRCLE ( 'NONE', #44888, 16.00000000000000000 ) ;
#12860=CARTESIAN_POINT ( 'NONE',  ( 0.000000000000000000, 12.24744871391589207, -2.499999999999994671 ) ) ;
#12862=CARTESIAN_POINT ( 'NONE',  ( 10.00000000000000000, -35.38097989696503021, -12.42422080174676147 ) ) ;
#12877=CARTESIAN_POINT ( 'NONE',  ( 0.000000000000000000, 0.000000000000000000, 0.000000000000000000 ) ) ;
#12885=EDGE_CURVE ( 'NONE', #3577, #26816, #19872, .T. ) ;
#12917=ORIENTED_EDGE ( 'NONE', *, *, #12885, .F. ) ;
#12922=EDGE_CURVE ( 'NONE', #13574, #29150, #1130, .T. ) ;
#12924=CIRCLE ( 'NONE', #7429, 42.00000000000000000 ) ;
#12925=AXIS2_PLACEMENT_3D ( 'NONE', #48060, #21386, #33131 ) ;
#12930=DIRECTION ( 'NONE',  ( 0.000000000000000000, 0.000000000000000000, 1.000000000000000000 ) ) ;
#12932=ORIENTED_EDGE ( 'NONE', *, *, #45666, .T. ) ;
#12933=AXIS2_PLACEMENT_3D ( 'NONE', #48429, #40143, #23165 ) ;
#12935=DIRECTION ( 'NONE',  ( 0.000000000000000000, -0.9876883405951393247, 0.1564344650402205161 ) ) ;
#12938=ORIENTED_EDGE ( 'NONE', *, *, #32443, .T. ) ;
#12943=VECTOR ( 'NONE', #29436, 1000.000000000000000 ) ;
#12946=CARTESIAN_POINT ( 'NONE',  ( 10.00000000000000000, 0.9569279952884607310, 2.500000000000015543 ) ) ;
#12951=CARTESIAN_POINT ( 'NONE',  ( 0.000000000000000000, 0.000000000000000000, 0.000000000000000000 ) ) ;
#12956=CARTESIAN_POINT ( 'NONE',  ( -10.00000000000000000, 0.000000000000000000, 0.000000000000000000 ) ) ;
#12960=CYLINDRICAL_SURFACE ( 'NONE', #34796, 16.00000000000000000 ) ;
#12962=DIRECTION ( 'NONE',  ( -1.000000000000000000, 0.000000000000000000, 0.000000000000000000 ) ) ;
#12965=AXIS2_PLACEMENT_3D ( 'NONE', #46572, #13041, #27974 ) ;
#12971=CARTESIAN_POINT ( 'NONE',  ( 0.000000000000000000, 16.45098606841173705, -33.79645857604496229 ) ) ;
#12989=CIRCLE ( 'NONE', #20804, 37.49900000000001654 ) ;
#13001=CYLINDRICAL_SURFACE ( 'NONE', #22284, 16.00000000000000000 ) ;
#13024=ORIENTED_EDGE ( 'NONE', *, *, #39065, .T. ) ;
#13025=AXIS2_PLACEMENT_3D ( 'NONE', #1203, #20038, #42316 ) ;
#13030=ORIENTED_EDGE ( 'NONE', *, *, #35049, .T. ) ;
#13041=DIRECTION ( 'NONE',  ( -1.000000000000000000, 0.000000000000000000, 0.000000000000000000 ) ) ;
#13042=EDGE_CURVE ( 'NONE', #15966, #21714, #20699, .T. ) ;
#13048=CARTESIAN_POINT ( 'NONE',  ( 10.00000000000000000, 16.95692799528845995, 2.500000000000000000 ) ) ;
#13054=VERTEX_POINT ( 'NONE', #30647 ) ;
#13061=EDGE_CURVE ( 'NONE', #39405, #19937, #41809, .T. ) ;
#13069=DIRECTION ( 'NONE',  ( 1.000000000000000000, -0.000000000000000000, 0.000000000000000000 ) ) ;
#13075=VERTEX_POINT ( 'NONE', #8128 ) ;
#13079=DIRECTION ( 'NONE',  ( 0.000000000000000000, 0.000000000000000000, 1.000000000000000000 ) ) ;
#13104=VERTEX_POINT ( 'NONE', #37505 ) ;
#13111=DIRECTION ( 'NONE',  ( 0.000000000000000000, 0.000000000000000000, 1.000000000000000000 ) ) ;
#13114=EDGE_CURVE ( 'NONE', #22226, #26939, #33823, .T. ) ;
#13123=FILL_AREA_STYLE ('',( #28279 ) ) ;
#13127=DIRECTION ( 'NONE',  ( -1.000000000000000000, -0.000000000000000000, 0.000000000000000000 ) ) ;
#13132=ORIENTED_EDGE ( 'NONE', *, *, #25564, .T. ) ;
#13134=CIRCLE ( 'NONE', #47497, 16.00000000000000000 ) ;
#13136=AXIS2_PLACEMENT_3D ( 'NONE', #18254, #21198, #29286 ) ;
#13137=DIRECTION ( 'NONE',  ( 0.000000000000000000, 0.4539904997395412534, 0.8910065241883706744 ) ) ;
#13146=DIRECTION ( 'NONE',  ( -1.000000000000000000, -0.000000000000000000, 0.000000000000000000 ) ) ;
#13152=CARTESIAN_POINT ( 'NONE',  ( 0.000000000000000000, -36.13751322684404244, -21.40280677340410165 ) ) ;
#13158=EDGE_CURVE ( 'NONE', #45459, #9046, #20839, .T. ) ;
#13160=LINE ( 'NONE', #31788, #47803 ) ;
#13180=DIRECTION ( 'NONE',  ( 1.000000000000000000, -0.000000000000000000, -0.000000000000000000 ) ) ;
#13183=CIRCLE ( 'NONE', #2233, 16.00000000000000355 ) ;
#13185=EDGE_CURVE ( 'NONE', #44456, #36840, #14337, .T. ) ;
#13188=CARTESIAN_POINT ( 'NONE',  ( 0.000000000000000000, -37.58145647212455032, 16.68533520207890319 ) ) ;
#13191=LINE ( 'NONE', #42818, #37812 ) ;
#13193=VERTEX_POINT ( 'NONE', #46553 ) ;
#13221=DIRECTION ( 'NONE',  ( -1.000000000000000000, 0.000000000000000000, 0.000000000000000000 ) ) ;
#13229=ORIENTED_EDGE ( 'NONE', *, *, #10111, .T. ) ;
#13237=CARTESIAN_POINT ( 'NONE',  ( 10.00000000000000000, -35.95386929396248377, -10.96151621346525751 ) ) ;
#13262=CARTESIAN_POINT ( 'NONE',  ( 10.00000000000000000, 0.000000000000000000, 0.000000000000000000 ) ) ;
#13266=VERTEX_POINT ( 'NONE', #29325 ) ;
#13273=VERTEX_POINT ( 'NONE', #44486 ) ;
#13290=LINE ( 'NONE', #38268, #13309 ) ;
#13291=DIRECTION ( 'NONE',  ( 0.000000000000000000, 0.000000000000000000, -1.000000000000000000 ) ) ;
#13293=DIRECTION ( 'NONE',  ( -1.000000000000000000, -0.000000000000000000, 0.000000000000000000 ) ) ;
#13302=CARTESIAN_POINT ( 'NONE',  ( 10.00000000000000000, -33.79645857604501913, -16.45098606841161626 ) ) ;
#13309=VECTOR ( 'NONE', #23570, 1000.000000000000000 ) ;
#13314=ADVANCED_FACE ( 'NONE', ( #24754 ), #41310, .T. ) ;
#13329=DIRECTION ( 'NONE',  ( 0.000000000000000000, 0.000000000000000000, 1.000000000000000000 ) ) ;
#13332=LINE ( 'NONE', #9642, #3170 ) ;
#13337=DIRECTION ( 'NONE',  ( -1.000000000000000000, 0.000000000000000000, 0.000000000000000000 ) ) ;
#13340=ORIENTED_EDGE ( 'NONE', *, *, #15283, .F. ) ;
#13342=ORIENTED_EDGE ( 'NONE', *, *, #18720, .F. ) ;
#13345=ORIENTED_EDGE ( 'NONE', *, *, #46356, .F. ) ;
#13358=CARTESIAN_POINT ( 'NONE',  ( 10.00000000000000000, 0.000000000000000000, 0.000000000000000000 ) ) ;
#13359=CARTESIAN_POINT ( 'NONE',  ( 10.00000000000000000, 36.88895765772633695, 6.736453364083687667 ) ) ;
#13370=EDGE_CURVE ( 'NONE', #42780, #40355, #8073, .T. ) ;
#13371=ORIENTED_EDGE ( 'NONE', *, *, #17030, .F. ) ;
#13372=EDGE_CURVE ( 'NONE', #1493, #45724, #23727, .T. ) ;
#13377=ORIENTED_EDGE ( 'NONE', *, *, #20654, .T. ) ;
#13392=CIRCLE ( 'NONE', #2444, 16.00000000000000355 ) ;
#13396=VERTEX_POINT ( 'NONE', #8486 ) ;
#13406=ORIENTED_EDGE ( 'NONE', *, *, #2168, .F. ) ;
#13407=FACE_OUTER_BOUND ( 'NONE', #18940, .T. ) ;
#13422=DIRECTION ( 'NONE',  ( 0.000000000000000000, -0.3090169943749349057, -0.9510565162951577500 ) ) ;
#13429=ORIENTED_EDGE ( 'NONE', *, *, #44968, .T. ) ;
#13436=VECTOR ( 'NONE', #1803, 1000.000000000000000 ) ;
#13438=ORIENTED_EDGE ( 'NONE', *, *, #24868, .F. ) ;
#13448=ORIENTED_EDGE ( 'NONE', *, *, #40954, .T. ) ;
#13451=CARTESIAN_POINT ( 'NONE',  ( 0.000000000000000000, 0.000000000000000000, 0.000000000000000000 ) ) ;
#13452=EDGE_LOOP ( 'NONE', ( #44938, #37913, #22032, #22377 ) ) ;
#13461=DIRECTION ( 'NONE',  ( 0.000000000000000000, -0.9876883405951358830, -0.1564344650402420822 ) ) ;
#13469=CYLINDRICAL_SURFACE ( 'NONE', #6348, 16.00000000000000000 ) ;
#13474=CARTESIAN_POINT ( 'NONE',  ( 0.000000000000000000, 0.000000000000000000, 0.000000000000000000 ) ) ;
#13498=AXIS2_PLACEMENT_3D ( 'NONE', #42299, #8755, #27139 ) ;
#13500=CIRCLE ( 'NONE', #45569, 16.00000000000000000 ) ;
#13501=ORIENTED_EDGE ( 'NONE', *, *, #16150, .T. ) ;
#13508=ORIENTED_EDGE ( 'NONE', *, *, #27099, .T. ) ;
#13515=EDGE_CURVE ( 'NONE', #46188, #41093, #29117, .T. ) ;
#13521=ORIENTED_EDGE ( 'NONE', *, *, #38484, .F. ) ;
#13524=CARTESIAN_POINT ( 'NONE',  ( 10.00000000000000000, -37.58145647212455032, 0.6853352020789044152 ) ) ;
#13537=CYLINDRICAL_SURFACE ( 'NONE', #6748, 16.00000000000000000 ) ;
#13543=AXIS2_PLACEMENT_3D ( 'NONE', #19525, #20511, #38161 ) ;
#13573=FACE_OUTER_BOUND ( 'NONE', #6234, .T. ) ;
#13574=VERTEX_POINT ( 'NONE', #35878 ) ;
#13592=ORIENTED_EDGE ( 'NONE', *, *, #21492, .F. ) ;
#13599=CIRCLE ( 'NONE', #15181, 37.49900000000000944 ) ;
#13600=AXIS2_PLACEMENT_3D ( 'NONE', #29896, #42128, #19358 ) ;
#13605=VECTOR ( 'NONE', #13293, 1000.000000000000000 ) ;
#13623=FACE_OUTER_BOUND ( 'NONE', #14786, .T. ) ;
#13632=VERTEX_POINT ( 'NONE', #21430 ) ;
#13646=DIRECTION ( 'NONE',  ( -1.000000000000000000, 0.000000000000000000, 0.000000000000000000 ) ) ;
#13647=VECTOR ( 'NONE', #8619, 1000.000000000000000 ) ;
#13653=VECTOR ( 'NONE', #28167, 1000.000000000000000 ) ;
#13659=LINE ( 'NONE', #6316, #7423 ) ;
#13682=DIRECTION ( 'NONE',  ( 0.000000000000000000, 0.000000000000000000, 1.000000000000000000 ) ) ;
#13684=ORIENTED_EDGE ( 'NONE', *, *, #45691, .F. ) ;
#13691=VECTOR ( 'NONE', #2923, 1000.000000000000000 ) ;
#13693=AXIS2_PLACEMENT_3D ( 'NONE', #7251, #3826, #37357 ) ;
#13703=FACE_OUTER_BOUND ( 'NONE', #21089, .T. ) ;
#13705=ORIENTED_EDGE ( 'NONE', *, *, #27938, .F. ) ;
#13710=VECTOR ( 'NONE', #33091, 1000.000000000000000 ) ;
#13712=ORIENTED_EDGE ( 'NONE', *, *, #18312, .F. ) ;
#13715=DIRECTION ( 'NONE',  ( 0.000000000000000000, 0.4539904997395479702, -0.8910065241883673437 ) ) ;
#13717=VERTEX_POINT ( 'NONE', #26065 ) ;
#13719=FACE_OUTER_BOUND ( 'NONE', #14183, .T. ) ;
#13721=DIRECTION ( 'NONE',  ( -1.000000000000000000, 0.000000000000000000, 0.000000000000000000 ) ) ;
#13738=ADVANCED_FACE ( 'NONE', ( #15058 ), #37329, .T. ) ;
#13742=AXIS2_PLACEMENT_3D ( 'NONE', #19687, #1106, #5028 ) ;
#13745=ORIENTED_EDGE ( 'NONE', *, *, #30357, .T. ) ;
#13746=CIRCLE ( 'NONE', #35654, 15.99999999999999645 ) ;
#13748=CARTESIAN_POINT ( 'NONE',  ( 10.00000000000000000, 0.8828120875905820508, -37.48860685352290290 ) ) ;
#13760=ORIENTED_EDGE ( 'NONE', *, *, #10625, .T. ) ;
#13783=ORIENTED_EDGE ( 'NONE', *, *, #113, .T. ) ;
#13829=DIRECTION ( 'NONE',  ( 0.000000000000000000, 0.5877852522924685852, 0.8090169943749508930 ) ) ;
#13840=DIRECTION ( 'NONE',  ( -1.000000000000000000, -0.000000000000000000, 0.000000000000000000 ) ) ;
#13845=FACE_OUTER_BOUND ( 'NONE', #47608, .T. ) ;
#13877=ORIENTED_EDGE ( 'NONE', *, *, #1551, .F. ) ;
#13880=DIRECTION ( 'NONE',  ( -1.000000000000000000, -0.000000000000000000, -0.000000000000000000 ) ) ;
#13914=CARTESIAN_POINT ( 'NONE',  ( 10.00000000000000000, -15.48615015657555816, -39.04073710021360455 ) ) ;
#13915=EDGE_CURVE ( 'NONE', #17387, #7054, #41726, .T. ) ;
#13916=EDGE_LOOP ( 'NONE', ( #21946, #41736, #34725, #3005 ) ) ;
#13927=FACE_OUTER_BOUND ( 'NONE', #15381, .T. ) ;
#13928=ORIENTED_EDGE ( 'NONE', *, *, #35476, .T. ) ;
#13932=ADVANCED_FACE ( 'NONE', ( #42200 ), #33884, .T. ) ;
#13933=DIRECTION ( 'NONE',  ( 0.000000000000000000, 0.000000000000000000, 1.000000000000000000 ) ) ;
#13950=CYLINDRICAL_SURFACE ( 'NONE', #26899, 16.00000000000000000 ) ;
#13951=DIRECTION ( 'NONE',  ( -1.000000000000000000, 0.000000000000000000, 0.000000000000000000 ) ) ;
#13959=CARTESIAN_POINT ( 'NONE',  ( 0.000000000000000000, 0.000000000000000000, 0.000000000000000000 ) ) ;
#13962=EDGE_LOOP ( 'NONE', ( #2784, #45454, #5553, #48156 ) ) ;
#13971=ORIENTED_EDGE ( 'NONE', *, *, #3582, .T. ) ;
#13974=ORIENTED_EDGE ( 'NONE', *, *, #20449, .T. ) ;
#13986=VERTEX_POINT ( 'NONE', #24325 ) ;
#13997=DIRECTION ( 'NONE',  ( -1.000000000000000000, 0.000000000000000000, -0.000000000000000000 ) ) ;
#14002=CARTESIAN_POINT ( 'NONE',  ( 10.00000000000000000, 37.01155633439068282, -6.555932627142014191 ) ) ;
#14022=FACE_OUTER_BOUND ( 'NONE', #17589, .T. ) ;
#14034=EDGE_CURVE ( 'NONE', #23562, #18326, #9157, .T. ) ;
#14042=DIRECTION ( 'NONE',  ( 0.000000000000000000, 0.000000000000000000, -1.000000000000000000 ) ) ;
#14045=DIRECTION ( 'NONE',  ( -1.000000000000000000, 0.000000000000000000, 0.000000000000000000 ) ) ;
#14052=CYLINDRICAL_SURFACE ( 'NONE', #45456, 16.00000000000000000 ) ;
#14057=DIRECTION ( 'NONE',  ( -1.000000000000000000, 0.000000000000000000, 0.000000000000000000 ) ) ;
#14070=DIRECTION ( 'NONE',  ( -1.000000000000000000, 0.000000000000000000, 0.000000000000000000 ) ) ;
#14071=DIRECTION ( 'NONE',  ( 0.000000000000000000, 0.000000000000000000, -1.000000000000000000 ) ) ;
#14082=ORIENTED_EDGE ( 'NONE', *, *, #8552, .F. ) ;
#14100=AXIS2_PLACEMENT_3D ( 'NONE', #40988, #41230, #45136 ) ;
#14104=EDGE_CURVE ( 'NONE', #19386, #42217, #995, .T. ) ;
#14118=ORIENTED_EDGE ( 'NONE', *, *, #20046, .T. ) ;
#14143=CYLINDRICAL_SURFACE ( 'NONE', #24827, 16.00000000000000000 ) ;
#14171=DIRECTION ( 'NONE',  ( 0.000000000000000000, -0.7071067811865389130, -0.7071067811865563435 ) ) ;
#14172=ORIENTED_EDGE ( 'NONE', *, *, #35172, .T. ) ;
#14175=FACE_OUTER_BOUND ( 'NONE', #31141, .T. ) ;
#14176=DIRECTION ( 'NONE',  ( 0.000000000000000000, 0.000000000000000000, 1.000000000000000000 ) ) ;
#14183=EDGE_LOOP ( 'NONE', ( #33052, #5107, #17798, #14118 ) ) ;
#14189=CYLINDRICAL_SURFACE ( 'NONE', #23532, 37.49900000000000233 ) ;
#14191=CARTESIAN_POINT ( 'NONE',  ( 10.00000000000000000, 10.96151621346540317, -35.95386929396244113 ) ) ;
#14196=FACE_OUTER_BOUND ( 'NONE', #2675, .T. ) ;
#14198=EDGE_CURVE ( 'NONE', #18852, #9070, #38570, .T. ) ;
#14206=ORIENTED_EDGE ( 'NONE', *, *, #11424, .F. ) ;
#14217=CARTESIAN_POINT ( 'NONE',  ( 10.00000000000000000, 10.74501242461282757, 35.92658777277515014 ) ) ;
#14226=CIRCLE ( 'NONE', #4875, 37.49900000000000233 ) ;
#14247=EDGE_CURVE ( 'NONE', #5941, #9046, #15722, .T. ) ;
#14273=CARTESIAN_POINT ( 'NONE',  ( 4.999999999999999112, 21.40280677340371795, 36.13751322684426270 ) ) ;
#14278=EDGE_CURVE ( 'NONE', #38804, #47328, #41715, .T. ) ;
#14282=ORIENTED_EDGE ( 'NONE', *, *, #4482, .T. ) ;
#14288=CARTESIAN_POINT ( 'NONE',  ( 0.000000000000000000, 17.67226234102874116, -33.17418723428288274 ) ) ;
#14302=EDGE_CURVE ( 'NONE', #4753, #17448, #39380, .T. ) ;
#14304=AXIS2_PLACEMENT_3D ( 'NONE', #24178, #35182, #27609 ) ;
#14312=DIRECTION ( 'NONE',  ( 0.000000000000000000, 0.9510565162951521989, 0.3090169943749517256 ) ) ;
#14314=CYLINDRICAL_SURFACE ( 'NONE', #9042, 16.00000000000000000 ) ;
#14324=DIRECTION ( 'NONE',  ( -1.000000000000000000, 0.000000000000000000, 0.000000000000000000 ) ) ;
#14331=AXIS2_PLACEMENT_3D ( 'NONE', #45759, #12237, #8534 ) ;
#14337=CIRCLE ( 'NONE', #21384, 16.00000000000000000 ) ;
#14343=AXIS2_PLACEMENT_3D ( 'NONE', #27476, #41437, #5205 ) ;
#14347=AXIS2_PLACEMENT_3D ( 'NONE', #37274, #32862, #39989 ) ;
#14350=ORIENTED_EDGE ( 'NONE', *, *, #16758, .F. ) ;
#14353=ORIENTED_EDGE ( 'NONE', *, *, #26417, .F. ) ;
#14360=CARTESIAN_POINT ( 'NONE',  ( 10.00000000000000000, -37.22597642581161637, 5.202137450156258502 ) ) ;
#14367=DIRECTION ( 'NONE',  ( -1.000000000000000000, 0.000000000000000000, 0.000000000000000000 ) ) ;
#14368=DIRECTION ( 'NONE',  ( -1.000000000000000000, 0.000000000000000000, 0.000000000000000000 ) ) ;
#14371=CARTESIAN_POINT ( 'NONE',  ( 0.000000000000000000, 0.000000000000000000, 0.000000000000000000 ) ) ;
#14381=VECTOR ( 'NONE', #12355, 1000.000000000000000 ) ;
#14410=AXIS2_PLACEMENT_3D ( 'NONE', #45345, #11364, #4006 ) ;
#14417=AXIS2_PLACEMENT_3D ( 'NONE', #2166, #28819, #17081 ) ;
#14433=DIRECTION ( 'NONE',  ( -1.000000000000000000, 0.000000000000000000, 0.000000000000000000 ) ) ;
#14445=CARTESIAN_POINT ( 'NONE',  ( 0.000000000000000000, -27.75498641678764855, 31.52238457039590358 ) ) ;
#14446=VERTEX_POINT ( 'NONE', #20116 ) ;
#14448=AXIS2_PLACEMENT_3D ( 'NONE', #1014, #29921, #22818 ) ;
#14454=ORIENTED_EDGE ( 'NONE', *, *, #29735, .T. ) ;
#14458=AXIS2_PLACEMENT_3D ( 'NONE', #11915, #11674, #26838 ) ;
#14465=DIRECTION ( 'NONE',  ( -1.000000000000000000, -0.000000000000000000, 0.000000000000000000 ) ) ;
#14471=FACE_OUTER_BOUND ( 'NONE', #375, .T. ) ;
#14496=DIRECTION ( 'NONE',  ( -1.000000000000000000, -0.000000000000000000, -0.000000000000000000 ) ) ;
#14511=CARTESIAN_POINT ( 'NONE',  ( 10.00000000000000000, 27.13269053701096922, 25.88420570971410228 ) ) ;
#14514=DIRECTION ( 'NONE',  ( -1.000000000000000000, -0.000000000000000000, 0.000000000000000000 ) ) ;
#14515=DIRECTION ( 'NONE',  ( 0.000000000000000000, 0.000000000000000000, 1.000000000000000000 ) ) ;
#14517=DIRECTION ( 'NONE',  ( 0.000000000000000000, 0.000000000000000000, 1.000000000000000000 ) ) ;
#14521=AXIS2_PLACEMENT_3D ( 'NONE', #13474, #9318, #27694 ) ;
#14524=DIRECTION ( 'NONE',  ( 0.000000000000000000, 0.000000000000000000, -1.000000000000000000 ) ) ;
#14529=AXIS2_PLACEMENT_3D ( 'NONE', #40593, #14661, #6830 ) ;
#14538=VECTOR ( 'NONE', #37327, 1000.000000000000000 ) ;
#14552=DIRECTION ( 'NONE',  ( -1.000000000000000000, -0.000000000000000000, -0.000000000000000000 ) ) ;
#14554=CYLINDRICAL_SURFACE ( 'NONE', #36700, 37.49900000000000233 ) ;
#14570=CIRCLE ( 'NONE', #41932, 16.00000000000000000 ) ;
#14605=ORIENTED_EDGE ( 'NONE', *, *, #38698, .T. ) ;
#14621=DIRECTION ( 'NONE',  ( -1.000000000000000000, 0.000000000000000000, 0.000000000000000000 ) ) ;
#14628=DIRECTION ( 'NONE',  ( 1.000000000000000000, -0.000000000000000000, 0.000000000000000000 ) ) ;
#14643=DIRECTION ( 'NONE',  ( -1.000000000000000000, -0.000000000000000000, -0.000000000000000000 ) ) ;
#14648=EDGE_CURVE ( 'NONE', #42467, #25752, #25206, .T. ) ;
#14651=ORIENTED_EDGE ( 'NONE', *, *, #15917, .F. ) ;
#14652=ORIENTED_EDGE ( 'NONE', *, *, #38698, .F. ) ;
#14658=EDGE_CURVE ( 'NONE', #46491, #11716, #37823, .T. ) ;
#14661=DIRECTION ( 'NONE',  ( -1.000000000000000000, 0.000000000000000000, 0.000000000000000000 ) ) ;
#14666=AXIS2_PLACEMENT_3D ( 'NONE', #45689, #8711, #45214 ) ;
#14682=DIRECTION ( 'NONE',  ( -1.000000000000000000, -0.000000000000000000, -0.000000000000000000 ) ) ;
#14703=ORIENTED_EDGE ( 'NONE', *, *, #40363, .T. ) ;
#14705=EDGE_CURVE ( 'NONE', #20655, #39405, #229, .T. ) ;
#14719=ORIENTED_EDGE ( 'NONE', *, *, #18556, .T. ) ;
#14727=ORIENTED_EDGE ( 'NONE', *, *, #3871, .T. ) ;
#14730=DIRECTION ( 'NONE',  ( 0.000000000000000000, -0.8910065241883722287, 0.4539904997395382558 ) ) ;
#14745=LINE ( 'NONE', #44592, #34081 ) ;
#14751=CARTESIAN_POINT ( 'NONE',  ( 0.000000000000000000, 0.000000000000000000, 0.000000000000000000 ) ) ;
#14778=ORIENTED_EDGE ( 'NONE', *, *, #10693, .F. ) ;
#14780=VERTEX_POINT ( 'NONE', #33763 ) ;
#14786=EDGE_LOOP ( 'NONE', ( #31787, #18488, #10416, #28571 ) ) ;
#14787=DIRECTION ( 'NONE',  ( -1.000000000000000000, -0.000000000000000000, 0.000000000000000000 ) ) ;
#14793=FACE_OUTER_BOUND ( 'NONE', #29580, .T. ) ;
#14794=ORIENTED_EDGE ( 'NONE', *, *, #4531, .F. ) ;
#14795=DIRECTION ( 'NONE',  ( -1.000000000000000000, 0.000000000000000000, 0.000000000000000000 ) ) ;
#14797=ORIENTED_EDGE ( 'NONE', *, *, #23068, .T. ) ;
#14807=AXIS2_PLACEMENT_3D ( 'NONE', #2637, #2400, #17329 ) ;
#14809=CARTESIAN_POINT ( 'NONE',  ( 0.000000000000000000, 0.000000000000000000, 37.49900000000000233 ) ) ;
#14844=EDGE_LOOP ( 'NONE', ( #21311, #44640, #4844, #47141 ) ) ;
#14845=ORIENTED_EDGE ( 'NONE', *, *, #46870, .T. ) ;
#14847=DIRECTION ( 'NONE',  ( -1.000000000000000000, 0.000000000000000000, -0.000000000000000000 ) ) ;
#14859=EDGE_CURVE ( 'NONE', #18007, #28297, #12853, .T. ) ;
#14862=VERTEX_POINT ( 'NONE', #31827 ) ;
#14864=CARTESIAN_POINT ( 'NONE',  ( 0.000000000000000000, 0.000000000000000000, 0.000000000000000000 ) ) ;
#14865=DIRECTION ( 'NONE',  ( -1.000000000000000000, 0.000000000000000000, -0.000000000000000000 ) ) ;
#14866=DIRECTION ( 'NONE',  ( -1.000000000000000000, 0.000000000000000000, 0.000000000000000000 ) ) ;
#14867=EDGE_CURVE ( 'NONE', #34100, #8511, #9759, .T. ) ;
#14868=CARTESIAN_POINT ( 'NONE',  ( 10.00000000000000000, 37.01155633439068282, -6.555932627142014191 ) ) ;
#14875=CARTESIAN_POINT ( 'NONE',  ( 10.00000000000000000, 16.65560815589464028, -38.55633173626993937 ) ) ;
#14887=CARTESIAN_POINT ( 'NONE',  ( 0.000000000000000000, 0.000000000000000000, 0.000000000000000000 ) ) ;
#14889=ORIENTED_EDGE ( 'NONE', *, *, #37626, .F. ) ;
#14898=CIRCLE ( 'NONE', #4767, 37.49900000000000944 ) ;
#14902=ORIENTED_EDGE ( 'NONE', *, *, #48394, .F. ) ;
#14903=VECTOR ( 'NONE', #16652, 1000.000000000000000 ) ;
#14908=ADVANCED_FACE ( 'NONE', ( #42330 ), #4882, .T. ) ;
#14919=LINE ( 'NONE', #4403, #22094 ) ;
#14921=ADVANCED_FACE ( 'NONE', ( #5616 ), #16624, .F. ) ;
#14925=DIRECTION ( 'NONE',  ( 1.000000000000000000, 0.000000000000000000, 0.000000000000000000 ) ) ;
#14941=ORIENTED_EDGE ( 'NONE', *, *, #10278, .T. ) ;
#14942=CIRCLE ( 'NONE', #26683, 37.49900000000000233 ) ;
#14945=AXIS2_PLACEMENT_3D ( 'NONE', #35627, #31971, #46403 ) ;
#14954=VERTEX_POINT ( 'NONE', #48167 ) ;
#14958=DIRECTION ( 'NONE',  ( 0.000000000000000000, 0.000000000000000000, 1.000000000000000000 ) ) ;
#14966=ORIENTED_EDGE ( 'NONE', *, *, #28590, .T. ) ;
#14967=DIRECTION ( 'NONE',  ( -1.000000000000000000, 0.000000000000000000, 0.000000000000000000 ) ) ;
#14970=DIRECTION ( 'NONE',  ( 1.000000000000000000, 0.000000000000000000, 0.000000000000000000 ) ) ;
#14978=EDGE_CURVE ( 'NONE', #17019, #13986, #11280, .T. ) ;
#15023=FACE_OUTER_BOUND ( 'NONE', #7852, .T. ) ;
#15025=DIRECTION ( 'NONE',  ( 0.000000000000000000, 0.000000000000000000, 1.000000000000000000 ) ) ;
#15038=CARTESIAN_POINT ( 'NONE',  ( 10.00000000000000000, 10.96151621346540317, -35.95386929396244113 ) ) ;
#15045=FACE_OUTER_BOUND ( 'NONE', #33707, .T. ) ;
#15047=CARTESIAN_POINT ( 'NONE',  ( 0.000000000000000000, 10.96151621346487914, 35.95386929396260456 ) ) ;
#15058=FACE_OUTER_BOUND ( 'NONE', #32718, .T. ) ;
#15060=VERTEX_POINT ( 'NONE', #13914 ) ;
#15066=AXIS2_PLACEMENT_3D ( 'NONE', #28042, #10089, #34633 ) ;
#15073=CARTESIAN_POINT ( 'NONE',  ( 0.000000000000000000, 12.42422080174638310, 35.38097989696515810 ) ) ;
#15077=AXIS2_PLACEMENT_3D ( 'NONE', #27389, #42313, #27627 ) ;
#15081=FACE_BOUND ( 'NONE', #19410, .T. ) ;
#15092=DIRECTION ( 'NONE',  ( -1.000000000000000000, -0.000000000000000000, 0.000000000000000000 ) ) ;
#15100=DIRECTION ( 'NONE',  ( -1.000000000000000000, 0.000000000000000000, 0.000000000000000000 ) ) ;
#15101=ORIENTED_EDGE ( 'NONE', *, *, #25334, .F. ) ;
#15116=CIRCLE ( 'NONE', #31551, 37.49900000000000944 ) ;
#15120=DIRECTION ( 'NONE',  ( -1.000000000000000000, -0.000000000000000000, 0.000000000000000000 ) ) ;
#15147=ORIENTED_EDGE ( 'NONE', *, *, #11115, .T. ) ;
#15152=CARTESIAN_POINT ( 'NONE',  ( 10.00000000000000000, 12.26510123303308752, -35.53030884539072787 ) ) ;
#15160=AXIS2_PLACEMENT_3D ( 'NONE', #36765, #2996, #18154 ) ;
#15162=VERTEX_POINT ( 'NONE', #4363 ) ;
#15176=CARTESIAN_POINT ( 'NONE',  ( 10.00000000000000000, 37.16516213103277977, 4.992566952385115719 ) ) ;
#15177=DIRECTION ( 'NONE',  ( 0.000000000000000000, 0.000000000000000000, 1.000000000000000000 ) ) ;
#15181=AXIS2_PLACEMENT_3D ( 'NONE', #40814, #29557, #2886 ) ;
#15187=DIRECTION ( 'NONE',  ( -1.000000000000000000, -0.000000000000000000, -0.000000000000000000 ) ) ;
#15206=ORIENTED_EDGE ( 'NONE', *, *, #34197, .F. ) ;
#15210=CARTESIAN_POINT ( 'NONE',  ( 10.00000000000000000, -32.34446384429951138, -26.79245525562750530 ) ) ;
#15211=DIRECTION ( 'NONE',  ( 0.000000000000000000, 0.000000000000000000, 1.000000000000000000 ) ) ;
#15218=LINE ( 'NONE', #15453, #42229 ) ;
#15256=ORIENTED_EDGE ( 'NONE', *, *, #46092, .T. ) ;
#15274=FACE_OUTER_BOUND ( 'NONE', #24425, .T. ) ;
#15282=ORIENTED_EDGE ( 'NONE', *, *, #34142, .F. ) ;
#15283=EDGE_CURVE ( 'NONE', #13717, #23918, #5068, .T. ) ;
#15285=DIRECTION ( 'NONE',  ( 0.000000000000000000, 0.000000000000000000, 1.000000000000000000 ) ) ;
#15298=CARTESIAN_POINT ( 'NONE',  ( -10.00000000000000000, 0.000000000000000000, 0.000000000000000000 ) ) ;
#15302=CARTESIAN_POINT ( 'NONE',  ( 10.00000000000000000, -16.23288003029521320, 33.80338159004277543 ) ) ;
#15303=ADVANCED_FACE ( 'NONE', ( #25044 ), #20909, .T. ) ;
#15310=AXIS2_PLACEMENT_3D ( 'NONE', #19405, #1549, #15511 ) ;
#15322=AXIS2_PLACEMENT_3D ( 'NONE', #2990, #44118, #37001 ) ;
#15325=EDGE_CURVE ( 'NONE', #26495, #25548, #32635, .T. ) ;
#15337=CIRCLE ( 'NONE', #19228, 16.00000000000000000 ) ;
#15345=FACE_OUTER_BOUND ( 'NONE', #41057, .T. ) ;
#15349=CIRCLE ( 'NONE', #27752, 16.00000000000000000 ) ;
#15371=( NAMED_UNIT ( * ) PLANE_ANGLE_UNIT ( ) SI_UNIT ( $, .RADIAN. ) );
#15381=EDGE_LOOP ( 'NONE', ( #37515, #7791, #8471, #20423 ) ) ;
#15382=AXIS2_PLACEMENT_3D ( 'NONE', #22981, #3157, #18085 ) ;
#15387=ORIENTED_EDGE ( 'NONE', *, *, #43165, .F. ) ;
#15392=DIRECTION ( 'NONE',  ( 0.000000000000000000, 0.000000000000000000, 1.000000000000000000 ) ) ;
#15393=ORIENTED_EDGE ( 'NONE', *, *, #42872, .F. ) ;
#15397=FACE_OUTER_BOUND ( 'NONE', #314, .T. ) ;
#15402=CARTESIAN_POINT ( 'NONE',  ( 0.000000000000000000, 0.8828120875900632436, 37.48860685352291000 ) ) ;
#15415=CARTESIAN_POINT ( 'NONE',  ( 0.000000000000000000, 37.16516213103277266, 4.992566952385114831 ) ) ;
#15418=ORIENTED_EDGE ( 'NONE', *, *, #18592, .F. ) ;
#15435=CYLINDRICAL_SURFACE ( 'NONE', #29603, 16.00000000000000000 ) ;
#15441=FACE_OUTER_BOUND ( 'NONE', #30834, .T. ) ;
#15442=VECTOR ( 'NONE', #22338, 1000.000000000000000 ) ;
#15453=CARTESIAN_POINT ( 'NONE',  ( 5.000000000000000000, 3.925862922256160736, 41.81611651403863306 ) ) ;
#15480=VERTEX_POINT ( 'NONE', #3994 ) ;
#15492=VERTEX_POINT ( 'NONE', #10361 ) ;
#15500=EDGE_LOOP ( 'NONE', ( #19083, #34486, #12366, #10908 ) ) ;
#15503=DIRECTION ( 'NONE',  ( -1.000000000000000000, -0.000000000000000000, -0.000000000000000000 ) ) ;
#15511=DIRECTION ( 'NONE',  ( 0.000000000000000000, 0.5877852522924684742, 0.8090169943749506709 ) ) ;
#15512=DIRECTION ( 'NONE',  ( 0.000000000000000000, 0.000000000000000000, -1.000000000000000000 ) ) ;
#15517=DIRECTION ( 'NONE',  ( -1.000000000000000000, -0.000000000000000000, 0.000000000000000000 ) ) ;
#15528=CARTESIAN_POINT ( 'NONE',  ( 0.000000000000000000, 0.000000000000000000, 0.000000000000000000 ) ) ;
#15535=AXIS2_PLACEMENT_3D ( 'NONE', #10734, #32989, #13682 ) ;
#15542=ORIENTED_EDGE ( 'NONE', *, *, #14648, .T. ) ;
#15544=CARTESIAN_POINT ( 'NONE',  ( 10.00000000000000000, -33.79645857604501913, -16.45098606841161626 ) ) ;
#15559=VERTEX_POINT ( 'NONE', #26998 ) ;
#15577=ORIENTED_EDGE ( 'NONE', *, *, #9485, .T. ) ;
#15578=EDGE_LOOP ( 'NONE', ( #26230, #24985, #26569, #13429 ) ) ;
#15585=ADVANCED_FACE ( 'NONE', ( #45333 ), #26744, .T. ) ;
#15587=DIRECTION ( 'NONE',  ( 0.000000000000000000, -0.9510565162951500895, -0.3090169943749583314 ) ) ;
#15613=LINE ( 'NONE', #45237, #32139 ) ;
#15620=CARTESIAN_POINT ( 'NONE',  ( 10.00000000000000000, 17.67226234102826510, 33.17418723428314564 ) ) ;
#15636=DIRECTION ( 'NONE',  ( 1.000000000000000000, -0.000000000000000000, -0.000000000000000000 ) ) ;
#15642=CIRCLE ( 'NONE', #14945, 37.49900000000000233 ) ;
#15646=CARTESIAN_POINT ( 'NONE',  ( 10.00000000000000000, -30.84782396557201878, -21.32104025579148399 ) ) ;
#15651=DIRECTION ( 'NONE',  ( 0.000000000000000000, -0.8090169943749531134, 0.5877852522924654766 ) ) ;
#15657=VERTEX_POINT ( 'NONE', #17394 ) ;
#15660=DIRECTION ( 'NONE',  ( -1.000000000000000000, 0.000000000000000000, -0.000000000000000000 ) ) ;
#15684=ORIENTED_EDGE ( 'NONE', *, *, #12788, .T. ) ;
#15686=VERTEX_POINT ( 'NONE', #47278 ) ;
#15693=CARTESIAN_POINT ( 'NONE',  ( -10.00000000000000000, 0.000000000000000000, 0.000000000000000000 ) ) ;
#15698=ADVANCED_FACE ( 'NONE', ( #5436 ), #28677, .T. ) ;
#15699=FACE_OUTER_BOUND ( 'NONE', #29139, .T. ) ;
#15722=LINE ( 'NONE', #41431, #28392 ) ;
#15734=CIRCLE ( 'NONE', #44668, 42.00000000000000000 ) ;
#15746=ORIENTED_EDGE ( 'NONE', *, *, #2875, .F. ) ;
#15748=DIRECTION ( 'NONE',  ( -1.000000000000000000, -0.000000000000000000, -0.000000000000000000 ) ) ;
#15757=DIRECTION ( 'NONE',  ( -1.000000000000000000, -0.000000000000000000, 0.000000000000000000 ) ) ;
#15762=CIRCLE ( 'NONE', #26692, 42.00000000000000000 ) ;
#15765=DIRECTION ( 'NONE',  ( 0.000000000000000000, 0.8910065241883656784, 0.4539904997395510788 ) ) ;
#15781=DIRECTION ( 'NONE',  ( -1.000000000000000000, -0.000000000000000000, 0.000000000000000000 ) ) ;
#15787=CYLINDRICAL_SURFACE ( 'NONE', #40612, 37.49900000000000233 ) ;
#15805=CARTESIAN_POINT ( 'NONE',  ( 0.000000000000000000, 37.58145647212453611, 0.6853352020791767529 ) ) ;
#15822=ORIENTED_EDGE ( 'NONE', *, *, #34295, .F. ) ;
#15827=DIRECTION ( 'NONE',  ( 0.000000000000000000, 0.000000000000000000, 1.000000000000000000 ) ) ;
#15831=DIRECTION ( 'NONE',  ( -1.000000000000000000, 0.000000000000000000, -0.000000000000000000 ) ) ;
#15838=ORIENTED_EDGE ( 'NONE', *, *, #11516, .T. ) ;
#15841=ORIENTED_EDGE ( 'NONE', *, *, #10693, .T. ) ;
#15842=AXIS2_PLACEMENT_3D ( 'NONE', #7790, #8284, #18797 ) ;
#15843=ORIENTED_EDGE ( 'NONE', *, *, #27938, .T. ) ;
#15848=CIRCLE ( 'NONE', #22869, 37.49900000000000233 ) ;
#15851=VERTEX_POINT ( 'NONE', #2949 ) ;
#15866=CARTESIAN_POINT ( 'NONE',  ( 0.000000000000000000, 21.40280677340371795, 36.13751322684426270 ) ) ;
#15877=ORIENTED_EDGE ( 'NONE', *, *, #45997, .F. ) ;
#15879=CARTESIAN_POINT ( 'NONE',  ( 10.00000000000000000, -37.58145647212453611, -0.6853352020794456489 ) ) ;
#15886=LINE ( 'NONE', #11976, #36965 ) ;
#15893=CARTESIAN_POINT ( 'NONE',  ( 0.000000000000000000, 0.000000000000000000, 0.000000000000000000 ) ) ;
#15899=DIRECTION ( 'NONE',  ( 0.000000000000000000, 0.000000000000000000, 1.000000000000000000 ) ) ;
#15907=AXIS2_PLACEMENT_3D ( 'NONE', #24353, #32662, #39553 ) ;
#15917=EDGE_CURVE ( 'NONE', #6864, #10410, #28605, .T. ) ;
#15921=ORIENTED_EDGE ( 'NONE', *, *, #28185, .F. ) ;
#15922=DIRECTION ( 'NONE',  ( -1.000000000000000000, 0.000000000000000000, -0.000000000000000000 ) ) ;
#15925=LINE ( 'NONE', #4434, #10290 ) ;
#15932=LINE ( 'NONE', #42115, #30584 ) ;
#15933=ORIENTED_EDGE ( 'NONE', *, *, #37252, .T. ) ;
#15934=LINE ( 'NONE', #37715, #23461 ) ;
#15937=CARTESIAN_POINT ( 'NONE',  ( 0.000000000000000000, -30.00120703465222149, 22.64427369931158296 ) ) ;
#15946=CARTESIAN_POINT ( 'NONE',  ( 0.000000000000000000, 0.000000000000000000, 0.000000000000000000 ) ) ;
#15956=CIRCLE ( 'NONE', #29215, 37.49900000000000233 ) ;
#15957=CIRCLE ( 'NONE', #43309, 16.00000000000000000 ) ;
#15963=EDGE_CURVE ( 'NONE', #3496, #20812, #38649, .T. ) ;
#15966=VERTEX_POINT ( 'NONE', #21490 ) ;
#15972=VERTEX_POINT ( 'NONE', #13188 ) ;
#15975=ORIENTED_EDGE ( 'NONE', *, *, #30357, .F. ) ;
#15998=CIRCLE ( 'NONE', #7404, 42.00000000000000000 ) ;
#16002=DIRECTION ( 'NONE',  ( -1.000000000000000000, -0.000000000000000000, -0.000000000000000000 ) ) ;
#16009=CARTESIAN_POINT ( 'NONE',  ( 10.00000000000000000, 0.000000000000000000, 0.000000000000000000 ) ) ;
#16045=VECTOR ( 'NONE', #11982, 1000.000000000000000 ) ;
#16047=EDGE_LOOP ( 'NONE', ( #13760, #12482, #30302, #40186 ) ) ;
#16048=ORIENTED_EDGE ( 'NONE', *, *, #24217, .T. ) ;
#16053=ORIENTED_EDGE ( 'NONE', *, *, #43851, .F. ) ;
#16066=VERTEX_POINT ( 'NONE', #10474 ) ;
#16069=CARTESIAN_POINT ( 'NONE',  ( 10.00000000000000000, 5.202137450156907761, -37.22597642581151689 ) ) ;
#16070=DIRECTION ( 'NONE',  ( -1.000000000000000000, 0.000000000000000000, 0.000000000000000000 ) ) ;
#16083=DIRECTION ( 'NONE',  ( -1.000000000000000000, -0.000000000000000000, -0.000000000000000000 ) ) ;
#16086=AXIS2_PLACEMENT_3D ( 'NONE', #32843, #43639, #47541 ) ;
#16088=DIRECTION ( 'NONE',  ( -1.000000000000000000, -0.000000000000000000, -0.000000000000000000 ) ) ;
#16122=ORIENTED_EDGE ( 'NONE', *, *, #46924, .F. ) ;
#16150=EDGE_CURVE ( 'NONE', #2760, #4312, #25335, .T. ) ;
#16157=DIRECTION ( 'NONE',  ( 0.000000000000000000, 6.938893903907229364E-16, 1.000000000000000000 ) ) ;
#16159=ADVANCED_FACE ( 'NONE', ( #5082 ), #30130, .T. ) ;
#16160=EDGE_CURVE ( 'NONE', #3407, #1420, #19997, .T. ) ;
#16180=CARTESIAN_POINT ( 'NONE',  ( 0.000000000000000000, 0.000000000000000000, 0.000000000000000000 ) ) ;
#16183=CARTESIAN_POINT ( 'NONE',  ( 10.00000000000000000, -21.32104025579135964, 30.84782396557210760 ) ) ;
#16199=LINE ( 'NONE', #3969, #45787 ) ;
#16217=CARTESIAN_POINT ( 'NONE',  ( 10.00000000000000000, 21.32104025579114648, 30.84782396557224970 ) ) ;
#16244=EDGE_LOOP ( 'NONE', ( #16937, #21607, #37851, #24952 ) ) ;
#16269=CYLINDRICAL_SURFACE ( 'NONE', #31656, 16.00000000000000000 ) ;
#16279=ORIENTED_EDGE ( 'NONE', *, *, #15917, .T. ) ;
#16287=DIRECTION ( 'NONE',  ( -1.000000000000000000, 0.000000000000000000, 0.000000000000000000 ) ) ;
#16299=DIRECTION ( 'NONE',  ( -1.000000000000000000, 0.000000000000000000, 0.000000000000000000 ) ) ;
#16314=CIRCLE ( 'NONE', #8478, 37.49900000000000233 ) ;
#16315=CARTESIAN_POINT ( 'NONE',  ( 10.00000000000000000, 0.000000000000000000, 0.000000000000000000 ) ) ;
#16317=EDGE_CURVE ( 'NONE', #7360, #13104, #8966, .T. ) ;
#16329=CYLINDRICAL_SURFACE ( 'NONE', #46075, 37.49900000000000233 ) ;
#16350=DIRECTION ( 'NONE',  ( -1.000000000000000000, 0.000000000000000000, -0.000000000000000000 ) ) ;
#16355=DIRECTION ( 'NONE',  ( 0.000000000000000000, 0.9876883405951382144, -0.1564344650402276493 ) ) ;
#16359=STYLED_ITEM ( 'NONE', ( #662 ), #37976 ) ;
#16362=ORIENTED_EDGE ( 'NONE', *, *, #77, .T. ) ;
#16366=CARTESIAN_POINT ( 'NONE',  ( 4.999999999999999112, 16.65560815589411092, 38.55633173627015253 ) ) ;
#16377=ORIENTED_EDGE ( 'NONE', *, *, #6452, .T. ) ;
#16385=DIRECTION ( 'NONE',  ( 0.000000000000000000, 1.000000000000000000, -6.938893903907229364E-16 ) ) ;
#16396=EDGE_CURVE ( 'NONE', #35643, #26166, #47266, .T. ) ;
#16402=AXIS2_PLACEMENT_3D ( 'NONE', #9568, #28186, #45640 ) ;
#16404=CARTESIAN_POINT ( 'NONE',  ( 0.000000000000000000, -12.42422080174663712, 35.38097989696507994 ) ) ;
#16414=DIRECTION ( 'NONE',  ( -1.000000000000000000, -0.000000000000000000, -0.000000000000000000 ) ) ;
#16426=CARTESIAN_POINT ( 'NONE',  ( 10.00000000000000000, 0.000000000000000000, 0.000000000000000000 ) ) ;
#16432=CARTESIAN_POINT ( 'NONE',  ( 10.00000000000000000, 37.01155633439059756, 6.555932627142549762 ) ) ;
#16439=VECTOR ( 'NONE', #27726, 1000.000000000000000 ) ;
#16440=CYLINDRICAL_SURFACE ( 'NONE', #43993, 42.00000000000000000 ) ;
#16442=AXIS2_PLACEMENT_3D ( 'NONE', #18845, #44562, #26693 ) ;
#16473=EDGE_CURVE ( 'NONE', #47238, #39281, #27740, .T. ) ;
#16474=DIRECTION ( 'NONE',  ( 0.000000000000000000, 0.000000000000000000, 1.000000000000000000 ) ) ;
#16484=AXIS2_PLACEMENT_3D ( 'NONE', #39936, #28681, #47985 ) ;
#16499=CYLINDRICAL_SURFACE ( 'NONE', #17544, 16.00000000000000000 ) ;
#16501=DIRECTION ( 'NONE',  ( -1.000000000000000000, 0.000000000000000000, 0.000000000000000000 ) ) ;
#16523=CARTESIAN_POINT ( 'NONE',  ( 0.000000000000000000, 35.95386929396256903, -10.96151621346501237 ) ) ;
#16539=ORIENTED_EDGE ( 'NONE', *, *, #24315, .F. ) ;
#16547=SURFACE_STYLE_USAGE ( .BOTH. , #5052 ) ;
#16549=CARTESIAN_POINT ( 'NONE',  ( 10.00000000000000000, 0.000000000000000000, 0.000000000000000000 ) ) ;
#16567=EDGE_CURVE ( 'NONE', #44578, #38804, #45176, .T. ) ;
#16585=DIRECTION ( 'NONE',  ( -1.000000000000000000, 0.000000000000000000, -0.000000000000000000 ) ) ;
#16595=DIRECTION ( 'NONE',  ( 0.000000000000000000, 0.000000000000000000, 1.000000000000000000 ) ) ;
#16596=ORIENTED_EDGE ( 'NONE', *, *, #43552, .T. ) ;
#16599=AXIS2_PLACEMENT_3D ( 'NONE', #27381, #19519, #11493 ) ;
#16611=CARTESIAN_POINT ( 'NONE',  ( 0.000000000000000000, 2.663952781846149254, 41.91543099594818500 ) ) ;
#16616=VECTOR ( 'NONE', #16966, 1000.000000000000000 ) ;
#16617=ORIENTED_EDGE ( 'NONE', *, *, #21492, .T. ) ;
#16623=DIRECTION ( 'NONE',  ( -1.000000000000000000, 0.000000000000000000, -0.000000000000000000 ) ) ;
#16624=PLANE ( 'NONE',  #1096 ) ;
#16626=ORIENTED_EDGE ( 'NONE', *, *, #19580, .T. ) ;
#16643=AXIS2_PLACEMENT_3D ( 'NONE', #17836, #47686, #14176 ) ;
#16645=FACE_OUTER_BOUND ( 'NONE', #21511, .T. ) ;
#16650=ORIENTED_EDGE ( 'NONE', *, *, #48178, .T. ) ;
#16652=DIRECTION ( 'NONE',  ( -1.000000000000000000, 0.000000000000000000, 0.000000000000000000 ) ) ;
#16657=CARTESIAN_POINT ( 'NONE',  ( 10.00000000000000000, -31.52238457039580055, -27.75498641678775869 ) ) ;
#16658=FACE_OUTER_BOUND ( 'NONE', #23319, .T. ) ;
#16659=ORIENTED_EDGE ( 'NONE', *, *, #23193, .F. ) ;
#16660=VECTOR ( 'NONE', #15781, 1000.000000000000000 ) ;
#16675=CARTESIAN_POINT ( 'NONE',  ( 0.000000000000000000, -37.48860685352291711, 0.8828120875899322373 ) ) ;
#16682=CYLINDRICAL_SURFACE ( 'NONE', #19758, 16.00000000000000000 ) ;
#16693=AXIS2_PLACEMENT_3D ( 'NONE', #41717, #4517, #41478 ) ;
#16706=ORIENTED_EDGE ( 'NONE', *, *, #26210, .T. ) ;
#16716=CYLINDRICAL_SURFACE ( 'NONE', #6868, 37.49900000000000233 ) ;
#16724=CYLINDRICAL_SURFACE ( 'NONE', #32109, 42.00000000000000000 ) ;
#16726=ORIENTED_EDGE ( 'NONE', *, *, #4823, .F. ) ;
#16735=LINE ( 'NONE', #2274, #5892 ) ;
#16738=AXIS2_PLACEMENT_3D ( 'NONE', #2385, #47428, #32262 ) ;
#16745=ORIENTED_EDGE ( 'NONE', *, *, #21987, .F. ) ;
#16746=CYLINDRICAL_SURFACE ( 'NONE', #31614, 16.00000000000000000 ) ;
#16758=EDGE_CURVE ( 'NONE', #26166, #20595, #12924, .T. ) ;
#16763=VECTOR ( 'NONE', #7523, 1000.000000000000000 ) ;
#16767=CYLINDRICAL_SURFACE ( 'NONE', #28963, 16.00000000000000000 ) ;
#16776=ORIENTED_EDGE ( 'NONE', *, *, #38753, .F. ) ;
#16786=DIRECTION ( 'NONE',  ( 0.000000000000000000, 0.000000000000000000, 1.000000000000000000 ) ) ;
#16794=VERTEX_POINT ( 'NONE', #39770 ) ;
#16795=CARTESIAN_POINT ( 'NONE',  ( 10.00000000000000000, 16.23288003029543347, -33.80338159004267595 ) ) ;
#16799=CARTESIAN_POINT ( 'NONE',  ( 10.00000000000000000, -21.40280677340345505, -36.13751322684441902 ) ) ;
#16803=DIRECTION ( 'NONE',  ( -1.000000000000000000, 0.000000000000000000, 0.000000000000000000 ) ) ;
#16818=LINE ( 'NONE', #27588, #710 ) ;
#16830=CARTESIAN_POINT ( 'NONE',  ( 10.00000000000000000, -25.88420570971419821, 27.13269053701087330 ) ) ;
#16838=CARTESIAN_POINT ( 'NONE',  ( 4.999999999999999112, -40.68715046381921496, -10.41901085202121280 ) ) ;
#16842=DIRECTION ( 'NONE',  ( 0.000000000000000000, 0.000000000000000000, 1.000000000000000000 ) ) ;
#16844=EDGE_CURVE ( 'NONE', #26882, #929, #31702, .T. ) ;
#16859=CYLINDRICAL_SURFACE ( 'NONE', #214, 16.00000000000000000 ) ;
#16861=CYLINDRICAL_SURFACE ( 'NONE', #22422, 42.00000000000000000 ) ;
#16878=CLOSED_SHELL ( 'NONE', ( #10423, #4928, #7023, #25276, #9632, #24969, #27645, #41572, #17514, #8285, #7721, #2710, #5214, #36224, #22918, #37860, #36838, #44751, #44433, #47601, #7487, #7336, #31517, #604, #39078, #10727, #31185, #32795, #39911, #8875, #11108, #30147, #28740, #13314, #47025, #3725, #46327, #10488, #34753, #41554, #29569, #29054, #29280, #3338, #11400, #31121, #26123, #24641, #29771, #32534, #10946, #6798, #28765, #9611, #616, #20498, #19173, #47791, #29452, #11143, #19875, #28842, #12840, #45517, #31899, #34249, #20693, #45834, #37176, #42335, #4391, #40120, #23808, #17941, #12723, #20011, #1579, #25402, #33148, #25618, #22561, #27155, #275, #30681, #1381, #18146, #31146, #15698, #48154, #20120, #47781, #28737, #33529, #17452, #40460, #2017, #37830, #3404, #12016, #26517, #37574, #11687, #20907, #3531, #11039, #44375, #31944, #4535, #26754, #45893, #40760, #6869, #46760, #15303, #14908, #27048, #553, #17723, #10931, #35039, #43664, #8312, #39643, #1104, #11465, #21938, #42024, #24541, #19222, #41168, #20346, #22283, #16, #36816, #27924, #35869, #10835, #36239, #5924, #45982, #35964, #36680, #13738, #713, #796, #26369, #10948, #28021, #24409, #2185, #30694, #10906, #7348, #29880, #43745, #13932, #15585, #36514, #36947, #27351, #42801, #17106, #16159, #38300, #48346, #39548, #8904, #33071, #19442, #43210, #14921, #21193, #42402 ) ) ;
#16891=CIRCLE ( 'NONE', #9066, 16.00000000000000000 ) ;
#16912=CARTESIAN_POINT ( 'NONE',  ( -1.200000000000000030E-05, 16.95692799528845640, -2.500000000000000000 ) ) ;
#16933=AXIS2_PLACEMENT_3D ( 'NONE', #3824, #48365, #32709 ) ;
#16937=ORIENTED_EDGE ( 'NONE', *, *, #42994, .T. ) ;
#16950=ORIENTED_EDGE ( 'NONE', *, *, #19488, .T. ) ;
#16958=CARTESIAN_POINT ( 'NONE',  ( 10.00000000000000000, -36.13751322684404244, -21.40280677340410165 ) ) ;
#16966=DIRECTION ( 'NONE',  ( 1.000000000000000000, -0.000000000000000000, 0.000000000000000000 ) ) ;
#16970=DIRECTION ( 'NONE',  ( 0.000000000000000000, 0.000000000000000000, 1.000000000000000000 ) ) ;
#16995=CIRCLE ( 'NONE', #32622, 42.00000000000000000 ) ;
#17004=ORIENTED_EDGE ( 'NONE', *, *, #46085, .F. ) ;
#17012=CARTESIAN_POINT ( 'NONE',  ( 10.00000000000000000, 35.92658777277525672, -10.74501242461245809 ) ) ;
#17019=VERTEX_POINT ( 'NONE', #34318 ) ;
#17030=EDGE_CURVE ( 'NONE', #46829, #15966, #46566, .T. ) ;
#17052=ORIENTED_EDGE ( 'NONE', *, *, #18091, .T. ) ;
#17054=DIRECTION ( 'NONE',  ( -1.000000000000000000, 0.000000000000000000, -0.000000000000000000 ) ) ;
#17056=DIRECTION ( 'NONE',  ( -1.000000000000000000, -0.000000000000000000, -0.000000000000000000 ) ) ;
#17075=VERTEX_POINT ( 'NONE', #33841 ) ;
#17077=DIRECTION ( 'NONE',  ( -1.000000000000000000, 0.000000000000000000, 0.000000000000000000 ) ) ;
#17081=DIRECTION ( 'NONE',  ( 0.000000000000000000, 0.1564344650402244852, 0.9876883405951387696 ) ) ;
#17087=DIRECTION ( 'NONE',  ( 0.000000000000000000, 1.000000000000000000, 3.469446951953614189E-15 ) ) ;
#17100=AXIS2_PLACEMENT_3D ( 'NONE', #27646, #42583, #20286 ) ;
#17102=CYLINDRICAL_SURFACE ( 'NONE', #1494, 16.00000000000000000 ) ;
#17106=ADVANCED_FACE ( 'NONE', ( #22835 ), #37764, .T. ) ;
#17125=ORIENTED_EDGE ( 'NONE', *, *, #3010, .F. ) ;
#17141=CARTESIAN_POINT ( 'NONE',  ( 10.00000000000000000, -33.80338159004296017, 16.23288003029484727 ) ) ;
#17156=AXIS2_PLACEMENT_3D ( 'NONE', #10188, #10912, #20968 ) ;
#17157=LINE ( 'NONE', #13748, #39049 ) ;
#17158=VERTEX_POINT ( 'NONE', #21079 ) ;
#17176=DIRECTION ( 'NONE',  ( 0.000000000000000000, 0.000000000000000000, 1.000000000000000000 ) ) ;
#17203=DIRECTION ( 'NONE',  ( 0.000000000000000000, 0.000000000000000000, 1.000000000000000000 ) ) ;
#17208=EDGE_CURVE ( 'NONE', #26919, #1546, #2773, .T. ) ;
#17210=DIRECTION ( 'NONE',  ( 0.000000000000000000, 0.000000000000000000, 1.000000000000000000 ) ) ;
#17217=VECTOR ( 'NONE', #9831, 1000.000000000000000 ) ;
#17219=CARTESIAN_POINT ( 'NONE',  ( 0.000000000000000000, 37.01155633439059756, 6.555932627142549762 ) ) ;
#17232=DIRECTION ( 'NONE',  ( -1.000000000000000000, -0.000000000000000000, -0.000000000000000000 ) ) ;
#17242=CARTESIAN_POINT ( 'NONE',  ( 10.00000000000000000, 6.736453364083557105, 36.88895765772635826 ) ) ;
#17264=DIRECTION ( 'NONE',  ( -1.000000000000000000, 0.000000000000000000, 0.000000000000000000 ) ) ;
#17281=ORIENTED_EDGE ( 'NONE', *, *, #21784, .F. ) ;
#17284=CARTESIAN_POINT ( 'NONE',  ( 10.00000000000000000, -4.992566952384716927, -37.16516213103282951 ) ) ;
#17286=CIRCLE ( 'NONE', #6377, 37.49900000000000233 ) ;
#17300=VECTOR ( 'NONE', #14628, 1000.000000000000000 ) ;
#17314=FACE_OUTER_BOUND ( 'NONE', #1939, .T. ) ;
#17325=CIRCLE ( 'NONE', #24362, 37.49900000000000233 ) ;
#17329=DIRECTION ( 'NONE',  ( 0.000000000000000000, 0.000000000000000000, 1.000000000000000000 ) ) ;
#17346=CYLINDRICAL_SURFACE ( 'NONE', #29858, 16.00000000000000000 ) ;
#17352=ORIENTED_EDGE ( 'NONE', *, *, #13185, .F. ) ;
#17359=DIRECTION ( 'NONE',  ( 0.000000000000000000, -0.7071067811865389130, -0.7071067811865561215 ) ) ;
#17378=CARTESIAN_POINT ( 'NONE',  ( 0.000000000000000000, 0.000000000000000000, 0.000000000000000000 ) ) ;
#17384=VECTOR ( 'NONE', #14433, 1000.000000000000000 ) ;
#17385=EDGE_CURVE ( 'NONE', #3686, #37417, #34491, .T. ) ;
#17387=VERTEX_POINT ( 'NONE', #30864 ) ;
#17391=EDGE_CURVE ( 'NONE', #3376, #45432, #39204, .T. ) ;
#17394=CARTESIAN_POINT ( 'NONE',  ( 10.00000000000000000, 9.188173127307297960, 40.98264845739753071 ) ) ;
#17410=CARTESIAN_POINT ( 'NONE',  ( 10.00000000000000000, 0.000000000000000000, 0.000000000000000000 ) ) ;
#17413=EDGE_CURVE ( 'NONE', #25302, #17158, #38424, .T. ) ;
#17424=ORIENTED_EDGE ( 'NONE', *, *, #4208, .F. ) ;
#17447=VECTOR ( 'NONE', #15517, 1000.000000000000000 ) ;
#17448=VERTEX_POINT ( 'NONE', #41156 ) ;
#17449=EDGE_CURVE ( 'NONE', #21422, #42780, #15925, .T. ) ;
#17452=ADVANCED_FACE ( 'NONE', ( #22774 ), #512, .T. ) ;
#17455=ORIENTED_EDGE ( 'NONE', *, *, #45822, .F. ) ;
#17463=CARTESIAN_POINT ( 'NONE',  ( 10.00000000000000000, 30.00120703465205452, 22.64427369931179967 ) ) ;
#17471=ORIENTED_EDGE ( 'NONE', *, *, #1150, .T. ) ;
#17489=AXIS2_PLACEMENT_3D ( 'NONE', #34809, #24278, #1294 ) ;
#17490=CARTESIAN_POINT ( 'NONE',  ( 0.000000000000000000, 6.555932627142418312, 37.01155633439060466 ) ) ;
#17494=DIRECTION ( 'NONE',  ( -1.000000000000000000, -0.000000000000000000, 0.000000000000000000 ) ) ;
#17506=DIRECTION ( 'NONE',  ( 0.000000000000000000, 0.000000000000000000, -1.000000000000000000 ) ) ;
#17514=ADVANCED_FACE ( 'NONE', ( #34029, #41622 ), #8086, .F. ) ;
#17518=AXIS2_PLACEMENT_3D ( 'NONE', #7157, #40689, #14515 ) ;
#17544=AXIS2_PLACEMENT_3D ( 'NONE', #46353, #20395, #17203 ) ;
#17589=EDGE_LOOP ( 'NONE', ( #29382, #22040, #8559, #25460 ) ) ;
#17599=VERTEX_POINT ( 'NONE', #8801 ) ;
#17605=DIRECTION ( 'NONE',  ( 0.000000000000000000, 0.000000000000000000, 1.000000000000000000 ) ) ;
#17615=CYLINDRICAL_SURFACE ( 'NONE', #11805, 16.00000000000000000 ) ;
#17617=CARTESIAN_POINT ( 'NONE',  ( 10.00000000000000000, -10.74501242461308159, 35.92658777277507909 ) ) ;
#17628=CIRCLE ( 'NONE', #15310, 37.49900000000000944 ) ;
#17630=AXIS2_PLACEMENT_3D ( 'NONE', #5161, #20075, #20300 ) ;
#17638=AXIS2_PLACEMENT_3D ( 'NONE', #8772, #23712, #5127 ) ;
#17645=DIRECTION ( 'NONE',  ( -1.000000000000000000, 0.000000000000000000, 0.000000000000000000 ) ) ;
#17656=CIRCLE ( 'NONE', #41934, 37.49900000000000944 ) ;
#17660=AXIS2_PLACEMENT_3D ( 'NONE', #3462, #10819, #11056 ) ;
#17684=DIRECTION ( 'NONE',  ( 0.000000000000000000, 0.9510565162951544194, -0.3090169943749447867 ) ) ;
#17687=CARTESIAN_POINT ( 'NONE',  ( 10.00000000000000000, 0.8828120875900632436, 37.48860685352291000 ) ) ;
#17707=VECTOR ( 'NONE', #15636, 1000.000000000000000 ) ;
#17723=ADVANCED_FACE ( 'NONE', ( #47927 ), #17346, .T. ) ;
#17726=CARTESIAN_POINT ( 'NONE',  ( 10.00000000000000000, -40.98264845739755913, 9.188173127307164734 ) ) ;
#17728=VERTEX_POINT ( 'NONE', #18068 ) ;
#17740=CARTESIAN_POINT ( 'NONE',  ( 0.000000000000000000, -15.48615015657610527, 39.04073710021338428 ) ) ;
#17741=DIRECTION ( 'NONE',  ( -1.000000000000000000, 0.000000000000000000, -0.000000000000000000 ) ) ;
#17742=FACE_OUTER_BOUND ( 'NONE', #35494, .T. ) ;
#17744=ORIENTED_EDGE ( 'NONE', *, *, #34142, .T. ) ;
#17753=CARTESIAN_POINT ( 'NONE',  ( 0.000000000000000000, -33.00180498840035170, -17.80606268964575278 ) ) ;
#17754=ORIENTED_EDGE ( 'NONE', *, *, #20283, .T. ) ;
#17759=AXIS2_PLACEMENT_3D ( 'NONE', #40726, #14787, #26031 ) ;
#17771=VERTEX_POINT ( 'NONE', #36197 ) ;
#17774=CARTESIAN_POINT ( 'NONE',  ( 10.00000000000000000, 0.000000000000000000, 0.000000000000000000 ) ) ;
#17778=ORIENTED_EDGE ( 'NONE', *, *, #5539, .T. ) ;
#17779=VERTEX_POINT ( 'NONE', #44509 ) ;
#17787=ORIENTED_EDGE ( 'NONE', *, *, #31954, .T. ) ;
#17793=LINE ( 'NONE', #20501, #2456 ) ;
#17798=ORIENTED_EDGE ( 'NONE', *, *, #10609, .F. ) ;
#17799=VECTOR ( 'NONE', #9096, 1000.000000000000000 ) ;
#17826=VECTOR ( 'NONE', #4546, 1000.000000000000000 ) ;
#17834=PRODUCT_DEFINITION_FORMATION_WITH_SPECIFIED_SOURCE ( 'ANY', '', #42918, .NOT_KNOWN. ) ;
#17836=CARTESIAN_POINT ( 'NONE',  ( 10.00000000000000000, 30.00120703465236716, -22.64427369931138756 ) ) ;
#17859=CIRCLE ( 'NONE', #22586, 37.49900000000000233 ) ;
#17863=AXIS2_PLACEMENT_3D ( 'NONE', #46632, #27540, #28032 ) ;
#17864=FACE_OUTER_BOUND ( 'NONE', #35948, .T. ) ;
#17867=ORIENTED_EDGE ( 'NONE', *, *, #30664, .F. ) ;
#17875=CARTESIAN_POINT ( 'NONE',  ( 10.00000000000000000, -22.48208911017474065, -35.47612816024548721 ) ) ;
#17887=ORIENTED_EDGE ( 'NONE', *, *, #16160, .T. ) ;
#17894=EDGE_CURVE ( 'NONE', #37838, #5554, #24175, .T. ) ;
#17934=CIRCLE ( 'NONE', #31248, 16.00000000000000000 ) ;
#17936=EDGE_CURVE ( 'NONE', #20591, #19470, #13160, .T. ) ;
#17941=ADVANCED_FACE ( 'NONE', ( #46454 ), #9473, .T. ) ;
#17942=DIRECTION ( 'NONE',  ( 0.000000000000000000, 0.8910065241883688980, -0.4539904997395445840 ) ) ;
#17951=CIRCLE ( 'NONE', #43756, 16.00000000000000000 ) ;
#17967=DIRECTION ( 'NONE',  ( 0.000000000000000000, 0.000000000000000000, 1.000000000000000000 ) ) ;
#17970=DIRECTION ( 'NONE',  ( 0.000000000000000000, 0.000000000000000000, -1.000000000000000000 ) ) ;
#17975=CARTESIAN_POINT ( 'NONE',  ( 0.000000000000000000, 40.68715046381943523, -10.41901085202036370 ) ) ;
#18005=VERTEX_POINT ( 'NONE', #38879 ) ;
#18006=VERTEX_POINT ( 'NONE', #5339 ) ;
#18007=VERTEX_POINT ( 'NONE', #11109 ) ;
#18027=CIRCLE ( 'NONE', #28205, 15.99999999999999822 ) ;
#18034=CYLINDRICAL_SURFACE ( 'NONE', #8730, 37.49900000000000233 ) ;
#18036=DIRECTION ( 'NONE',  ( -1.000000000000000000, -0.000000000000000000, 0.000000000000000000 ) ) ;
#18055=EDGE_CURVE ( 'NONE', #45536, #41225, #18451, .T. ) ;
#18061=VERTEX_POINT ( 'NONE', #4010 ) ;
#18063=CIRCLE ( 'NONE', #29451, 42.00000000000000000 ) ;
#18065=ORIENTED_EDGE ( 'NONE', *, *, #43071, .F. ) ;
#18068=CARTESIAN_POINT ( 'NONE',  ( 0.000000000000000000, 33.80338159004283938, 16.23288003029508886 ) ) ;
#18079=ORIENTED_EDGE ( 'NONE', *, *, #6131, .F. ) ;
#18085=DIRECTION ( 'NONE',  ( 0.000000000000000000, 0.000000000000000000, 1.000000000000000000 ) ) ;
#18091=EDGE_CURVE ( 'NONE', #8075, #33159, #17934, .T. ) ;
#18096=DIRECTION ( 'NONE',  ( -1.000000000000000000, 0.000000000000000000, 0.000000000000000000 ) ) ;
#18103=EDGE_LOOP ( 'NONE', ( #11339, #44279, #3384, #38069 ) ) ;
#18118=CYLINDRICAL_SURFACE ( 'NONE', #16484, 16.00000000000000000 ) ;
#18128=CARTESIAN_POINT ( 'NONE',  ( 10.00000000000000000, -36.88895765772637247, 6.736453364083436313 ) ) ;
#18141=ORIENTED_EDGE ( 'NONE', *, *, #42267, .F. ) ;
#18146=ADVANCED_FACE ( 'NONE', ( #48069 ), #14554, .T. ) ;
#18154=DIRECTION ( 'NONE',  ( 0.000000000000000000, 0.000000000000000000, 1.000000000000000000 ) ) ;
#18164=AXIS2_PLACEMENT_3D ( 'NONE', #47641, #10451, #3094 ) ;
#18168=EDGE_LOOP ( 'NONE', ( #7707, #42716, #28256, #2899 ) ) ;
#18181=CARTESIAN_POINT ( 'NONE',  ( 10.00000000000000000, 29.81001611431041098, -22.74946021919100403 ) ) ;
#18183=ORIENTED_EDGE ( 'NONE', *, *, #18856, .F. ) ;
#18197=ORIENTED_EDGE ( 'NONE', *, *, #45109, .T. ) ;
#18209=CYLINDRICAL_SURFACE ( 'NONE', #44775, 16.00000000000000000 ) ;
#18249=ORIENTED_EDGE ( 'NONE', *, *, #12403, .T. ) ;
#18250=DIRECTION ( 'NONE',  ( -1.000000000000000000, -0.000000000000000000, -0.000000000000000000 ) ) ;
#18254=CARTESIAN_POINT ( 'NONE',  ( 50.00005079999999680, 0.000000000000000000, 0.000000000000000000 ) ) ;
#18263=CARTESIAN_POINT ( 'NONE',  ( 10.00000000000000000, 0.000000000000000000, 0.000000000000000000 ) ) ;
#18264=CYLINDRICAL_SURFACE ( 'NONE', #37038, 16.00000000000000000 ) ;
#18271=ORIENTED_EDGE ( 'NONE', *, *, #33912, .T. ) ;
#18275=CIRCLE ( 'NONE', #8959, 16.00000000000000000 ) ;
#18285=DIRECTION ( 'NONE',  ( -1.000000000000000000, -0.000000000000000000, -0.000000000000000000 ) ) ;
#18291=CIRCLE ( 'NONE', #37054, 16.00000000000000355 ) ;
#18312=EDGE_CURVE ( 'NONE', #40415, #26939, #25763, .T. ) ;
#18313=EDGE_CURVE ( 'NONE', #17075, #35109, #46093, .T. ) ;
#18325=CIRCLE ( 'NONE', #32398, 42.00000000000000000 ) ;
#18326=VERTEX_POINT ( 'NONE', #41946 ) ;
#18336=ORIENTED_EDGE ( 'NONE', *, *, #6196, .F. ) ;
#18346=LINE ( 'NONE', #3162, #30207 ) ;
#18347=FACE_OUTER_BOUND ( 'NONE', #10266, .T. ) ;
#18356=VERTEX_POINT ( 'NONE', #12801 ) ;
#18366=CYLINDRICAL_SURFACE ( 'NONE', #35862, 16.00000000000000000 ) ;
#18369=ORIENTED_EDGE ( 'NONE', *, *, #10625, .F. ) ;
#18391=AXIS2_PLACEMENT_3D ( 'NONE', #4248, #34089, #43133 ) ;
#18396=ORIENTED_EDGE ( 'NONE', *, *, #456, .F. ) ;
#18411=DIRECTION ( 'NONE',  ( -1.000000000000000000, 0.000000000000000000, 0.000000000000000000 ) ) ;
#18412=ORIENTED_EDGE ( 'NONE', *, *, #8425, .T. ) ;
#18424=ORIENTED_EDGE ( 'NONE', *, *, #4216, .F. ) ;
#18425=DIRECTION ( 'NONE',  ( 0.000000000000000000, -0.7071067811865389130, -0.7071067811865563435 ) ) ;
#18429=DIRECTION ( 'NONE',  ( 0.000000000000000000, 0.8910065241883688980, -0.4539904997395447506 ) ) ;
#18431=VECTOR ( 'NONE', #12015, 1000.000000000000000 ) ;
#18435=AXIS2_PLACEMENT_3D ( 'NONE', #22608, #15748, #16474 ) ;
#18444=VECTOR ( 'NONE', #43098, 1000.000000000000000 ) ;
#18451=LINE ( 'NONE', #43509, #11695 ) ;
#18455=ORIENTED_EDGE ( 'NONE', *, *, #2174, .T. ) ;
#18488=ORIENTED_EDGE ( 'NONE', *, *, #2903, .F. ) ;
#18516=FACE_OUTER_BOUND ( 'NONE', #21224, .T. ) ;
#18531=ORIENTED_EDGE ( 'NONE', *, *, #42270, .T. ) ;
#18532=LINE ( 'NONE', #25623, #29268 ) ;
#18552=ORIENTED_EDGE ( 'NONE', *, *, #18592, .T. ) ;
#18556=EDGE_CURVE ( 'NONE', #33236, #21422, #5483, .T. ) ;
#18566=EDGE_CURVE ( 'NONE', #13075, #32362, #29686, .T. ) ;
#18570=CYLINDRICAL_SURFACE ( 'NONE', #25411, 16.00000000000000000 ) ;
#18573=ORIENTED_EDGE ( 'NONE', *, *, #20619, .T. ) ;
#18582=CARTESIAN_POINT ( 'NONE',  ( 4.999999999999999112, 3.925862922256769583, -41.81611651403857621 ) ) ;
#18586=DIRECTION ( 'NONE',  ( -1.000000000000000000, -0.000000000000000000, -0.000000000000000000 ) ) ;
#18589=CARTESIAN_POINT ( 'NONE',  ( 10.00000000000000000, 6.555932627142418312, 37.01155633439060466 ) ) ;
#18591=CARTESIAN_POINT ( 'NONE',  ( 10.00000000000000000, -16.65560815589383381, -38.55633173627028754 ) ) ;
#18592=EDGE_CURVE ( 'NONE', #34102, #36999, #48441, .T. ) ;
#18631=ORIENTED_EDGE ( 'NONE', *, *, #41507, .T. ) ;
#18633=ORIENTED_EDGE ( 'NONE', *, *, #41076, .T. ) ;
#18638=CARTESIAN_POINT ( 'NONE',  ( -10.00000000000000000, 0.000000000000000000, 0.000000000000000000 ) ) ;
#18642=CARTESIAN_POINT ( 'NONE',  ( 10.00000000000000000, -2.663952781846440576, 41.91543099594817789 ) ) ;
#18645=ORIENTED_EDGE ( 'NONE', *, *, #47091, .F. ) ;
#18646=DIRECTION ( 'NONE',  ( -1.000000000000000000, 0.000000000000000000, 0.000000000000000000 ) ) ;
#18669=EDGE_CURVE ( 'NONE', #42455, #46829, #44563, .T. ) ;
#18676=EDGE_CURVE ( 'NONE', #43888, #39399, #41166, .T. ) ;
#18677=ORIENTED_EDGE ( 'NONE', *, *, #13042, .F. ) ;
#18692=DIRECTION ( 'NONE',  ( 0.000000000000000000, -6.938893903907228378E-15, 1.000000000000000000 ) ) ;
#18708=AXIS2_PLACEMENT_3D ( 'NONE', #45593, #34564, #11595 ) ;
#18709=DIRECTION ( 'NONE',  ( -1.000000000000000000, 0.000000000000000000, 0.000000000000000000 ) ) ;
#18716=ORIENTED_EDGE ( 'NONE', *, *, #1786, .F. ) ;
#18719=ORIENTED_EDGE ( 'NONE', *, *, #25674, .F. ) ;
#18720=EDGE_CURVE ( 'NONE', #40415, #42450, #15934, .T. ) ;
#18726=AXIS2_PLACEMENT_3D ( 'NONE', #15544, #30475, #11409 ) ;
#18734=DIRECTION ( 'NONE',  ( -0.000000000000000000, 0.000000000000000000, 1.000000000000000000 ) ) ;
#18736=VERTEX_POINT ( 'NONE', #7621 ) ;
#18743=LINE ( 'NONE', #23155, #40937 ) ;
#18760=EDGE_CURVE ( 'NONE', #8790, #23605, #27195, .T. ) ;
#18765=EDGE_CURVE ( 'NONE', #4312, #1546, #8341, .T. ) ;
#18767=EDGE_CURVE ( 'NONE', #13104, #41064, #15218, .T. ) ;
#18781=VERTEX_POINT ( 'NONE', #9785 ) ;
#18791=VERTEX_POINT ( 'NONE', #27933 ) ;
#18797=DIRECTION ( 'NONE',  ( 0.000000000000000000, 1.000000000000000000, -9.787530781167598712E-16 ) ) ;
#18815=DIRECTION ( 'NONE',  ( 0.000000000000000000, 0.000000000000000000, -1.000000000000000000 ) ) ;
#18818=DIRECTION ( 'NONE',  ( -1.000000000000000000, -0.000000000000000000, -0.000000000000000000 ) ) ;
#18834=EDGE_CURVE ( 'NONE', #38214, #22715, #819, .T. ) ;
#18843=DIRECTION ( 'NONE',  ( 0.000000000000000000, 0.1564344650402243742, 0.9876883405951387696 ) ) ;
#18845=CARTESIAN_POINT ( 'NONE',  ( 0.000000000000000000, 0.000000000000000000, 0.000000000000000000 ) ) ;
#18851=DIRECTION ( 'NONE',  ( 0.000000000000000000, 0.4539904997395414754, 0.8910065241883706744 ) ) ;
#18852=VERTEX_POINT ( 'NONE', #32076 ) ;
#18856=EDGE_CURVE ( 'NONE', #5626, #5369, #24272, .T. ) ;
#18876=LINE ( 'NONE', #22570, #15442 ) ;
#18878=EDGE_CURVE ( 'NONE', #11835, #27388, #46958, .T. ) ;
#18880=EDGE_CURVE ( 'NONE', #47714, #46188, #25825, .T. ) ;
#18882=CARTESIAN_POINT ( 'NONE',  ( 10.00000000000000000, 0.000000000000000000, 0.000000000000000000 ) ) ;
#18914=CARTESIAN_POINT ( 'NONE',  ( 10.00000000000000000, 0.000000000000000000, 0.000000000000000000 ) ) ;
#18924=FACE_OUTER_BOUND ( 'NONE', #37865, .T. ) ;
#18927=CIRCLE ( 'NONE', #4871, 42.00000000000000000 ) ;
#18940=EDGE_LOOP ( 'NONE', ( #20777, #30988, #14794, #26135 ) ) ;
#18956=ORIENTED_EDGE ( 'NONE', *, *, #46822, .T. ) ;
#18958=DIRECTION ( 'NONE',  ( 0.000000000000000000, 0.000000000000000000, 1.000000000000000000 ) ) ;
#18985=DIRECTION ( 'NONE',  ( -1.000000000000000000, -0.000000000000000000, -0.000000000000000000 ) ) ;
#18990=ORIENTED_EDGE ( 'NONE', *, *, #45367, .F. ) ;
#18999=CARTESIAN_POINT ( 'NONE',  ( 0.000000000000000000, 36.88895765772633695, 6.736453364083687667 ) ) ;
#19004=CARTESIAN_POINT ( 'NONE',  ( 0.000000000000000000, -0.8828120875903202602, 37.48860685352291000 ) ) ;
#19009=CIRCLE ( 'NONE', #25257, 37.49900000000000233 ) ;
#19011=DIRECTION ( 'NONE',  ( -1.000000000000000000, -0.000000000000000000, -0.000000000000000000 ) ) ;
#19014=AXIS2_PLACEMENT_3D ( 'NONE', #47598, #40033, #20451 ) ;
#19027=ORIENTED_EDGE ( 'NONE', *, *, #7837, .T. ) ;
#19036=CYLINDRICAL_SURFACE ( 'NONE', #14529, 37.49900000000000233 ) ;
#19040=CIRCLE ( 'NONE', #26070, 15.99999999999999645 ) ;
#19044=FACE_OUTER_BOUND ( 'NONE', #13916, .T. ) ;
#19049=DIRECTION ( 'NONE',  ( 1.000000000000000000, -0.000000000000000000, -0.000000000000000000 ) ) ;
#19061=LINE ( 'NONE', #37430, #37821 ) ;
#19083=ORIENTED_EDGE ( 'NONE', *, *, #20661, .F. ) ;
#19102=CARTESIAN_POINT ( 'NONE',  ( 10.00000000000000000, -30.00120703465222149, 22.64427369931158296 ) ) ;
#19106=DIRECTION ( 'NONE',  ( -1.000000000000000000, 0.000000000000000000, 0.000000000000000000 ) ) ;
#19107=ORIENTED_EDGE ( 'NONE', *, *, #9603, .F. ) ;
#19116=CIRCLE ( 'NONE', #26146, 16.00000000000000355 ) ;
#19146=DIRECTION ( 'NONE',  ( -1.000000000000000000, 0.000000000000000000, 0.000000000000000000 ) ) ;
#19165=EDGE_CURVE ( 'NONE', #21692, #35831, #32151, .T. ) ;
#19173=ADVANCED_FACE ( 'NONE', ( #34952 ), #24416, .T. ) ;
#19186=CARTESIAN_POINT ( 'NONE',  ( 10.00000000000000000, -37.16516213103273714, -4.992566952385376844 ) ) ;
#19191=EDGE_CURVE ( 'NONE', #13632, #4753, #28098, .T. ) ;
#19201=CARTESIAN_POINT ( 'NONE',  ( 0.000000000000000000, -33.80338159004296017, 16.23288003029484727 ) ) ;
#19208=EDGE_CURVE ( 'NONE', #15657, #31823, #35687, .T. ) ;
#19222=ADVANCED_FACE ( 'NONE', ( #13407 ), #28328, .T. ) ;
#19226=CARTESIAN_POINT ( 'NONE',  ( 10.00000000000000000, 4.992566952385523393, -37.16516213103272293 ) ) ;
#19228=AXIS2_PLACEMENT_3D ( 'NONE', #44744, #7558, #37650 ) ;
#19244=CARTESIAN_POINT ( 'NONE',  ( 0.000000000000000000, 37.22597642581150268, 5.202137450157037435 ) ) ;
#19247=FACE_OUTER_BOUND ( 'NONE', #34946, .T. ) ;
#19251=CARTESIAN_POINT ( 'NONE',  ( 10.00000000000000000, 6.736453364084091788, -36.88895765772625879 ) ) ;
#19252=FACE_OUTER_BOUND ( 'NONE', #42060, .T. ) ;
#19253=CARTESIAN_POINT ( 'NONE',  ( 0.000000000000000000, 15.48615015657637883, -39.04073710021327770 ) ) ;
#19254=VECTOR ( 'NONE', #44092, 1000.000000000000000 ) ;
#19257=CIRCLE ( 'NONE', #10673, 16.00000000000000000 ) ;
#19262=AXIS2_PLACEMENT_3D ( 'NONE', #4380, #41817, #19285 ) ;
#19266=DIRECTION ( 'NONE',  ( 0.000000000000000000, 0.000000000000000000, -1.000000000000000000 ) ) ;
#19268=ORIENTED_EDGE ( 'NONE', *, *, #11154, .F. ) ;
#19285=DIRECTION ( 'NONE',  ( 0.000000000000000000, 0.000000000000000000, 1.000000000000000000 ) ) ;
#19291=DIRECTION ( 'NONE',  ( -1.000000000000000000, -0.000000000000000000, 0.000000000000000000 ) ) ;
#19301=DIRECTION ( 'NONE',  ( -1.000000000000000000, -0.000000000000000000, 0.000000000000000000 ) ) ;
#19310=CYLINDRICAL_SURFACE ( 'NONE', #32467, 42.00000000000000000 ) ;
#19319=FACE_OUTER_BOUND ( 'NONE', #3799, .T. ) ;
#19329=VERTEX_POINT ( 'NONE', #24899 ) ;
#19345=DIRECTION ( 'NONE',  ( -1.000000000000000000, -0.000000000000000000, -0.000000000000000000 ) ) ;
#19357=VERTEX_POINT ( 'NONE', #25615 ) ;
#19358=DIRECTION ( 'NONE',  ( 0.000000000000000000, 0.000000000000000000, -1.000000000000000000 ) ) ;
#19361=LINE ( 'NONE', #19585, #3858 ) ;
#19362=CARTESIAN_POINT ( 'NONE',  ( 0.000000000000000000, 33.00180498840046539, 17.80606268964551120 ) ) ;
#19386=VERTEX_POINT ( 'NONE', #40797 ) ;
#19392=ORIENTED_EDGE ( 'NONE', *, *, #20722, .F. ) ;
#19397=DIRECTION ( 'NONE',  ( 0.000000000000000000, 0.7071067811865487940, -0.7071067811865462405 ) ) ;
#19405=CARTESIAN_POINT ( 'NONE',  ( 10.00000000000000000, 0.000000000000000000, 0.000000000000000000 ) ) ;
#19410=EDGE_LOOP ( 'NONE', ( #26089, #2579, #9104, #46023, #31500, #22211 ) ) ;
#19420=DIRECTION ( 'NONE',  ( 0.000000000000000000, 0.000000000000000000, 1.000000000000000000 ) ) ;
#19427=CIRCLE ( 'NONE', #2247, 16.00000000000000000 ) ;
#19429=AXIS2_PLACEMENT_3D ( 'NONE', #30537, #7553, #23431 ) ;
#19432=EDGE_LOOP ( 'NONE', ( #39026, #9522, #10746, #7222 ) ) ;
#19442=ADVANCED_FACE ( 'NONE', ( #44706 ), #7747, .T. ) ;
#19451=VERTEX_POINT ( 'NONE', #26830 ) ;
#19462=DIRECTION ( 'NONE',  ( -1.000000000000000000, -0.000000000000000000, 0.000000000000000000 ) ) ;
#19465=DIRECTION ( 'NONE',  ( 0.000000000000000000, 0.000000000000000000, 1.000000000000000000 ) ) ;
#19470=VERTEX_POINT ( 'NONE', #3590 ) ;
#19476=FACE_OUTER_BOUND ( 'NONE', #15578, .T. ) ;
#19479=CARTESIAN_POINT ( 'NONE',  ( 10.00000000000000000, -9.188173127307003085, -40.98264845739760176 ) ) ;
#19488=EDGE_CURVE ( 'NONE', #39693, #22548, #33597, .T. ) ;
#19519=DIRECTION ( 'NONE',  ( -1.000000000000000000, 0.000000000000000000, 0.000000000000000000 ) ) ;
#19520=VERTEX_POINT ( 'NONE', #23632 ) ;
#19525=CARTESIAN_POINT ( 'NONE',  ( 10.00000000000000000, 0.000000000000000000, 0.000000000000000000 ) ) ;
#19546=DIRECTION ( 'NONE',  ( 1.000000000000000000, -0.000000000000000000, -0.000000000000000000 ) ) ;
#19564=CARTESIAN_POINT ( 'NONE',  ( 10.00000000000000000, 0.000000000000000000, 0.000000000000000000 ) ) ;
#19571=CARTESIAN_POINT ( 'NONE',  ( 10.00000000000000000, -36.88895765772637247, 6.736453364083436313 ) ) ;
#19579=ORIENTED_EDGE ( 'NONE', *, *, #12557, .F. ) ;
#19580=EDGE_CURVE ( 'NONE', #18007, #28886, #15642, .T. ) ;
#19585=CARTESIAN_POINT ( 'NONE',  ( 50.00005079999999680, 0.000000000000000000, 12.50000000000000000 ) ) ;
#19589=AXIS2_PLACEMENT_3D ( 'NONE', #47406, #13880, #10440 ) ;
#19591=DIRECTION ( 'NONE',  ( 0.000000000000000000, 0.7071067811865439090, 0.7071067811865512365 ) ) ;
#19609=AXIS2_PLACEMENT_3D ( 'NONE', #22496, #37420, #11717 ) ;
#19611=DIRECTION ( 'NONE',  ( 0.000000000000000000, 0.000000000000000000, 1.000000000000000000 ) ) ;
#19635=EDGE_CURVE ( 'NONE', #25752, #18006, #35965, .T. ) ;
#19640=CIRCLE ( 'NONE', #38314, 37.49900000000000233 ) ;
#19660=VERTEX_POINT ( 'NONE', #17740 ) ;
#19665=AXIS2_PLACEMENT_3D ( 'NONE', #42905, #31418, #4721 ) ;
#19677=ORIENTED_EDGE ( 'NONE', *, *, #41564, .F. ) ;
#19685=ORIENTED_EDGE ( 'NONE', *, *, #26329, .F. ) ;
#19687=CARTESIAN_POINT ( 'NONE',  ( -10.00000000000000000, 0.000000000000000000, 0.000000000000000000 ) ) ;
#19715=EDGE_CURVE ( 'NONE', #26495, #15657, #785, .T. ) ;
#19717=CARTESIAN_POINT ( 'NONE',  ( 0.000000000000000000, 0.000000000000000000, 0.000000000000000000 ) ) ;
#19723=ORIENTED_EDGE ( 'NONE', *, *, #16317, .F. ) ;
#19739=DIRECTION ( 'NONE',  ( 0.000000000000000000, 0.000000000000000000, 1.000000000000000000 ) ) ;
#19740=ORIENTED_EDGE ( 'NONE', *, *, #41984, .T. ) ;
#19752=DIRECTION ( 'NONE',  ( -1.000000000000000000, -0.000000000000000000, 0.000000000000000000 ) ) ;
#19758=AXIS2_PLACEMENT_3D ( 'NONE', #4701, #45565, #19611 ) ;
#19762=ORIENTED_EDGE ( 'NONE', *, *, #18556, .F. ) ;
#19799=AXIS2_PLACEMENT_3D ( 'NONE', #26296, #3276, #11122 ) ;
#19809=EDGE_LOOP ( 'NONE', ( #18424, #30258, #8791, #30415 ) ) ;
#19811=ORIENTED_EDGE ( 'NONE', *, *, #3643, .F. ) ;
#19823=DIRECTION ( 'NONE',  ( 0.000000000000000000, -0.9876883405951393247, 0.1564344650402204329 ) ) ;
#19828=EDGE_LOOP ( 'NONE', ( #46435, #41758, #32289, #547, #13712, #3825, #30058, #36887, #6536, #30876, #35606, #19925, #2131, #37107, #30804, #43247, #3301, #42757, #20305, #45295, #43701, #12301, #6770, #15387, #4945, #7596, #4910, #7213, #40161, #44306, #20467, #40913, #18369, #31784, #42661, #4655, #26405, #44683, #45768, #3195, #42932, #8035, #31955, #45401, #1481, #29084, #27664, #45119, #5493, #2665, #20618, #13438, #47989, #34248, #34004, #25203, #2483, #17352, #9890, #21219, #15282, #34883, #21932, #29706, #19762, #45899, #16053, #47364, #30929, #24788, #45244, #12453, #2147, #33949, #38409, #24181, #33589, #18677, #13371, #22967, #5872, #23013, #15101, #11171, #27344, #23783, #43922, #40670, #43053, #9392, #32160, #39661, #17281, #25394, #13406, #5480, #29956, #24240, #14206, #31888, #32117, #21626, #41570, #25913, #18716, #42343, #12917, #34325, #16726, #38502, #20510, #6240, #83, #3955, #31530, #22012, #10157, #31907, #14350, #33015, #8978, #44147, #18065, #3705, #305, #3649, #15822, #17125, #28086, #9773, #24904, #35275, #29107, #15921, #379, #37082, #35811, #30544, #43432, #24340, #36672, #26695, #39967, #27149, #20598, #22299, #42790, #42513, #11014, #26446, #32055, #5400, #21716, #38336, #22532, #32059, #28532, #4297, #30732, #7538, #6443, #4594, #27605, #30234, #39422 ) ) ;
#19829=EDGE_CURVE ( 'NONE', #35109, #22493, #43003, .T. ) ;
#19839=LINE ( 'NONE', #45548, #39633 ) ;
#19843=CARTESIAN_POINT ( 'NONE',  ( 0.000000000000000000, 32.34446384430010113, -26.79245525562679831 ) ) ;
#19866=AXIS2_PLACEMENT_3D ( 'NONE', #4400, #19301, #26904 ) ;
#19872=CIRCLE ( 'NONE', #40239, 42.00000000000000000 ) ;
#19873=ORIENTED_EDGE ( 'NONE', *, *, #45946, .T. ) ;
#19875=ADVANCED_FACE ( 'NONE', ( #14471 ), #18118, .T. ) ;
#19885=CIRCLE ( 'NONE', #2700, 37.49900000000000944 ) ;
#19887=CYLINDRICAL_SURFACE ( 'NONE', #32616, 16.00000000000000000 ) ;
#19894=ORIENTED_EDGE ( 'NONE', *, *, #20381, .F. ) ;
#19899=CARTESIAN_POINT ( 'NONE',  ( 10.00000000000000000, 35.47612816024523141, 22.48208911017513145 ) ) ;
#19916=DIRECTION ( 'NONE',  ( 0.000000000000000000, 0.000000000000000000, 1.000000000000000000 ) ) ;
#19925=ORIENTED_EDGE ( 'NONE', *, *, #31945, .F. ) ;
#19930=ORIENTED_EDGE ( 'NONE', *, *, #24818, .T. ) ;
#19934=DIRECTION ( 'NONE',  ( -1.000000000000000000, 0.000000000000000000, -0.000000000000000000 ) ) ;
#19937=VERTEX_POINT ( 'NONE', #3951 ) ;
#19941=ORIENTED_EDGE ( 'NONE', *, *, #42154, .T. ) ;
#19943=EDGE_CURVE ( 'NONE', #28297, #8075, #7622, .T. ) ;
#19946=CARTESIAN_POINT ( 'NONE',  ( 0.000000000000000000, 35.95386929396241271, 10.96151621346552751 ) ) ;
#19949=ORIENTED_EDGE ( 'NONE', *, *, #7837, .F. ) ;
#19953=DIRECTION ( 'NONE',  ( 0.000000000000000000, 0.000000000000000000, 1.000000000000000000 ) ) ;
#19970=( LENGTH_UNIT ( ) NAMED_UNIT ( * ) SI_UNIT ( .MILLI., .METRE. ) );
#19973=CYLINDRICAL_SURFACE ( 'NONE', #40051, 42.00000000000000000 ) ;
#19974=CARTESIAN_POINT ( 'NONE',  ( 0.000000000000000000, -2.663952781846440576, 41.91543099594817789 ) ) ;
#19975=AXIS2_PLACEMENT_3D ( 'NONE', #33390, #3765, #26291 ) ;
#19981=DIRECTION ( 'NONE',  ( -1.000000000000000000, -0.000000000000000000, -0.000000000000000000 ) ) ;
#19991=FACE_OUTER_BOUND ( 'NONE', #11909, .T. ) ;
#19994=ORIENTED_EDGE ( 'NONE', *, *, #17030, .T. ) ;
#19997=LINE ( 'NONE', #42527, #12848 ) ;
#20011=ADVANCED_FACE ( 'NONE', ( #34039 ), #522, .T. ) ;
#20020=AXIS2_PLACEMENT_3D ( 'NONE', #17410, #35788, #47744 ) ;
#20028=CARTESIAN_POINT ( 'NONE',  ( 10.00000000000000000, 37.58145647212453611, 0.6853352020791767529 ) ) ;
#20032=DIRECTION ( 'NONE',  ( -1.000000000000000000, 0.000000000000000000, 0.000000000000000000 ) ) ;
#20038=DIRECTION ( 'NONE',  ( -1.000000000000000000, -0.000000000000000000, 0.000000000000000000 ) ) ;
#20045=CYLINDRICAL_SURFACE ( 'NONE', #12104, 42.00000000000000000 ) ;
#20046=EDGE_CURVE ( 'NONE', #25493, #22407, #44606, .T. ) ;
#20050=CARTESIAN_POINT ( 'NONE',  ( 10.00000000000000000, -21.53537804866103045, 30.80686688397002371 ) ) ;
#20053=EDGE_CURVE ( 'NONE', #5351, #929, #30616, .T. ) ;
#20055=EDGE_CURVE ( 'NONE', #8930, #48358, #32882, .T. ) ;
#20059=ORIENTED_EDGE ( 'NONE', *, *, #33154, .F. ) ;
#20060=VERTEX_POINT ( 'NONE', #31603 ) ;
#20066=DIRECTION ( 'NONE',  ( -1.000000000000000000, 0.000000000000000000, 0.000000000000000000 ) ) ;
#20068=ORIENTED_EDGE ( 'NONE', *, *, #549, .T. ) ;
#20075=DIRECTION ( 'NONE',  ( 1.000000000000000000, 0.000000000000000000, 0.000000000000000000 ) ) ;
#20083=EDGE_LOOP ( 'NONE', ( #43212, #16659, #1709, #35284 ) ) ;
#20112=DIRECTION ( 'NONE',  ( 0.000000000000000000, 0.000000000000000000, 1.000000000000000000 ) ) ;
#20116=CARTESIAN_POINT ( 'NONE',  ( 10.00000000000000000, 31.52238457039599595, 27.75498641678753842 ) ) ;
#20120=ADVANCED_FACE ( 'NONE', ( #8571 ), #42357, .T. ) ;
#20131=ORIENTED_EDGE ( 'NONE', *, *, #36065, .T. ) ;
#20135=DIRECTION ( 'NONE',  ( -1.000000000000000000, -0.000000000000000000, -0.000000000000000000 ) ) ;
#20137=AXIS2_PLACEMENT_3D ( 'NONE', #15937, #14970, #44823 ) ;
#20144=ORIENTED_EDGE ( 'NONE', *, *, #48112, .T. ) ;
#20152=DIRECTION ( 'NONE',  ( 0.000000000000000000, 0.3090169943749480619, -0.9510565162951533091 ) ) ;
#20162=ORIENTED_EDGE ( 'NONE', *, *, #14705, .F. ) ;
#20166=EDGE_CURVE ( 'NONE', #24152, #33539, #45800, .T. ) ;
#20170=CARTESIAN_POINT ( 'NONE',  ( 10.00000000000000000, 12.42422080174688404, -35.38097989696498047 ) ) ;
#20192=DIRECTION ( 'NONE',  ( -1.000000000000000000, -0.000000000000000000, 0.000000000000000000 ) ) ;
#20203=DIRECTION ( 'NONE',  ( 1.000000000000000000, -0.000000000000000000, -0.000000000000000000 ) ) ;
#20220=DIRECTION ( 'NONE',  ( 0.000000000000000000, 0.9510565162951523099, 0.3090169943749517811 ) ) ;
#20221=DIRECTION ( 'NONE',  ( -1.000000000000000000, -0.000000000000000000, -0.000000000000000000 ) ) ;
#20229=EDGE_CURVE ( 'NONE', #36905, #26495, #4773, .T. ) ;
#20243=VERTEX_POINT ( 'NONE', #39670 ) ;
#20252=EDGE_LOOP ( 'NONE', ( #447, #8747, #33584, #2501 ) ) ;
#20277=DIRECTION ( 'NONE',  ( -1.000000000000000000, 0.000000000000000000, -0.000000000000000000 ) ) ;
#20279=FACE_OUTER_BOUND ( 'NONE', #24647, .T. ) ;
#20283=EDGE_CURVE ( 'NONE', #30855, #38126, #11024, .T. ) ;
#20286=DIRECTION ( 'NONE',  ( 0.000000000000000000, 0.7071067811865437980, 0.7071067811865512365 ) ) ;
#20288=EDGE_LOOP ( 'NONE', ( #22587, #25831, #7181, #22314 ) ) ;
#20290=DIRECTION ( 'NONE',  ( -1.000000000000000000, -0.000000000000000000, -0.000000000000000000 ) ) ;
#20292=ORIENTED_EDGE ( 'NONE', *, *, #15963, .T. ) ;
#20300=DIRECTION ( 'NONE',  ( 0.000000000000000000, 0.000000000000000000, -1.000000000000000000 ) ) ;
#20301=CARTESIAN_POINT ( 'NONE',  ( 5.000000000000000000, 26.79245525562714292, 32.34446384429980981 ) ) ;
#20303=AXIS2_PLACEMENT_3D ( 'NONE', #19244, #4081, #34169 ) ;
#20305=ORIENTED_EDGE ( 'NONE', *, *, #38591, .F. ) ;
#20324=EDGE_CURVE ( 'NONE', #36936, #35718, #14942, .T. ) ;
#20334=ORIENTED_EDGE ( 'NONE', *, *, #43498, .T. ) ;
#20335=AXIS2_PLACEMENT_3D ( 'NONE', #35839, #46141, #27538 ) ;
#20337=CIRCLE ( 'NONE', #43781, 37.49900000000001654 ) ;
#20346=ADVANCED_FACE ( 'NONE', ( #464 ), #44759, .T. ) ;
#20349=ORIENTED_EDGE ( 'NONE', *, *, #43165, .T. ) ;
#20362=CARTESIAN_POINT ( 'NONE',  ( 10.00000000000000000, 0.000000000000000000, 0.000000000000000000 ) ) ;
#20381=EDGE_CURVE ( 'NONE', #36999, #18005, #26414, .T. ) ;
#20385=DIRECTION ( 'NONE',  ( 0.000000000000000000, -1.000000000000000000, -1.040834085586084257E-14 ) ) ;
#20389=EDGE_CURVE ( 'NONE', #15559, #10554, #12602, .T. ) ;
#20392=CARTESIAN_POINT ( 'NONE',  ( 10.00000000000000000, 21.40280677340421533, -36.13751322684397138 ) ) ;
#20395=DIRECTION ( 'NONE',  ( -1.000000000000000000, 0.000000000000000000, -0.000000000000000000 ) ) ;
#20399=VERTEX_POINT ( 'NONE', #15402 ) ;
#20423=ORIENTED_EDGE ( 'NONE', *, *, #40565, .T. ) ;
#20434=EDGE_CURVE ( 'NONE', #38924, #7360, #38152, .T. ) ;
#20449=EDGE_CURVE ( 'NONE', #26893, #34798, #30590, .T. ) ;
#20451=DIRECTION ( 'NONE',  ( 0.000000000000000000, 0.000000000000000000, 1.000000000000000000 ) ) ;
#20453=VECTOR ( 'NONE', #28587, 1000.000000000000000 ) ;
#20456=CARTESIAN_POINT ( 'NONE',  ( 0.000000000000000000, 0.000000000000000000, 0.000000000000000000 ) ) ;
#20467=ORIENTED_EDGE ( 'NONE', *, *, #13515, .F. ) ;
#20475=CARTESIAN_POINT ( 'NONE',  ( 10.00000000000000000, 30.80686688397041451, -21.53537804866048688 ) ) ;
#20493=CARTESIAN_POINT ( 'NONE',  ( 10.00000000000000000, 0.000000000000000000, 0.000000000000000000 ) ) ;
#20497=EDGE_CURVE ( 'NONE', #43945, #27073, #31304, .T. ) ;
#20498=ADVANCED_FACE ( 'NONE', ( #46221 ), #35190, .T. ) ;
#20501=CARTESIAN_POINT ( 'NONE',  ( 5.000000000000000000, -31.52238457039579345, -27.75498641678775158 ) ) ;
#20510=ORIENTED_EDGE ( 'NONE', *, *, #4114, .F. ) ;
#20511=DIRECTION ( 'NONE',  ( -1.000000000000000000, 0.000000000000000000, 0.000000000000000000 ) ) ;
#20513=DIRECTION ( 'NONE',  ( -1.000000000000000000, -0.000000000000000000, -0.000000000000000000 ) ) ;
#20540=ORIENTED_EDGE ( 'NONE', *, *, #4322, .T. ) ;
#20549=CARTESIAN_POINT ( 'NONE',  ( 0.000000000000000000, 0.000000000000000000, 0.000000000000000000 ) ) ;
#20552=DIRECTION ( 'NONE',  ( -1.000000000000000000, 0.000000000000000000, 0.000000000000000000 ) ) ;
#20591=VERTEX_POINT ( 'NONE', #35913 ) ;
#20592=CIRCLE ( 'NONE', #47942, 42.00000000000000000 ) ;
#20595=VERTEX_POINT ( 'NONE', #39114 ) ;
#20597=EDGE_CURVE ( 'NONE', #1742, #40355, #17793, .T. ) ;
#20598=ORIENTED_EDGE ( 'NONE', *, *, #3917, .F. ) ;
#20618=ORIENTED_EDGE ( 'NONE', *, *, #3989, .F. ) ;
#20619=EDGE_CURVE ( 'NONE', #41225, #39728, #11869, .T. ) ;
#20620=CIRCLE ( 'NONE', #45598, 16.00000000000000000 ) ;
#20628=CARTESIAN_POINT ( 'NONE',  ( 10.00000000000000000, -25.88420570971381807, -27.13269053701123212 ) ) ;
#20641=AXIS2_PLACEMENT_3D ( 'NONE', #41235, #4023, #25557 ) ;
#20654=EDGE_CURVE ( 'NONE', #8389, #36993, #1925, .T. ) ;
#20655=VERTEX_POINT ( 'NONE', #39842 ) ;
#20661=EDGE_CURVE ( 'NONE', #11933, #15480, #24370, .T. ) ;
#20689=DIRECTION ( 'NONE',  ( 1.000000000000000000, 0.000000000000000000, 0.000000000000000000 ) ) ;
#20693=ADVANCED_FACE ( 'NONE', ( #47422 ), #43746, .T. ) ;
#20699=CIRCLE ( 'NONE', #33204, 16.00000000000000000 ) ;
#20713=VECTOR ( 'NONE', #7628, 1000.000000000000000 ) ;
#20722=EDGE_CURVE ( 'NONE', #21510, #29992, #39222, .T. ) ;
#20734=ORIENTED_EDGE ( 'NONE', *, *, #38354, .T. ) ;
#20743=CIRCLE ( 'NONE', #48096, 16.00000000000000000 ) ;
#20744=ORIENTED_EDGE ( 'NONE', *, *, #20823, .T. ) ;
#20751=CARTESIAN_POINT ( 'NONE',  ( 10.00000000000000000, 36.13751322684419165, 21.40280677340384230 ) ) ;
#20763=DIRECTION ( 'NONE',  ( 0.000000000000000000, 0.000000000000000000, 1.000000000000000000 ) ) ;
#20764=CARTESIAN_POINT ( 'NONE',  ( 10.00000000000000000, 4.992566952385523393, -37.16516213103272293 ) ) ;
#20772=CARTESIAN_POINT ( 'NONE',  ( 10.00000000000000000, 0.000000000000000000, 0.000000000000000000 ) ) ;
#20777=ORIENTED_EDGE ( 'NONE', *, *, #45483, .T. ) ;
#20778=ORIENTED_EDGE ( 'NONE', *, *, #27561, .T. ) ;
#20788=ORIENTED_EDGE ( 'NONE', *, *, #29556, .F. ) ;
#20804=AXIS2_PLACEMENT_3D ( 'NONE', #39562, #46168, #45933 ) ;
#20812=VERTEX_POINT ( 'NONE', #25376 ) ;
#20815=CARTESIAN_POINT ( 'NONE',  ( 10.00000000000000000, 0.8828120875905820508, -37.48860685352290290 ) ) ;
#20823=EDGE_CURVE ( 'NONE', #31993, #6127, #48142, .T. ) ;
#20827=EDGE_CURVE ( 'NONE', #23361, #22815, #40337, .T. ) ;
#20839=LINE ( 'NONE', #24261, #42509 ) ;
#20862=ORIENTED_EDGE ( 'NONE', *, *, #18856, .T. ) ;
#20886=DIRECTION ( 'NONE',  ( 1.000000000000000000, 0.000000000000000000, 0.000000000000000000 ) ) ;
#20904=DIRECTION ( 'NONE',  ( -1.000000000000000000, 0.000000000000000000, -0.000000000000000000 ) ) ;
#20907=ADVANCED_FACE ( 'NONE', ( #19247 ), #31009, .T. ) ;
#20909=CYLINDRICAL_SURFACE ( 'NONE', #40251, 16.00000000000000000 ) ;
#20968=DIRECTION ( 'NONE',  ( 0.000000000000000000, 0.000000000000000000, -1.000000000000000000 ) ) ;
#20971=ORIENTED_EDGE ( 'NONE', *, *, #29735, .F. ) ;
#20975=CARTESIAN_POINT ( 'NONE',  ( 0.000000000000000000, 30.00120703465236716, -22.64427369931138756 ) ) ;
#20984=DIRECTION ( 'NONE',  ( -1.000000000000000000, 0.000000000000000000, 0.000000000000000000 ) ) ;
#20985=DIRECTION ( 'NONE',  ( 0.000000000000000000, 0.5877852522924741363, -0.8090169943749465631 ) ) ;
#21001=DIRECTION ( 'NONE',  ( -1.000000000000000000, -0.000000000000000000, -0.000000000000000000 ) ) ;
#21010=VECTOR ( 'NONE', #17645, 1000.000000000000000 ) ;
#21012=FACE_OUTER_BOUND ( 'NONE', #20252, .T. ) ;
#21022=ORIENTED_EDGE ( 'NONE', *, *, #18055, .F. ) ;
#21029=CARTESIAN_POINT ( 'NONE',  ( 10.00000000000000000, -26.08949754953044220, 27.05870788708222818 ) ) ;
#21036=CIRCLE ( 'NONE', #46072, 16.00000000000000000 ) ;
#21043=DIRECTION ( 'NONE',  ( -1.000000000000000000, 0.000000000000000000, 0.000000000000000000 ) ) ;
#21046=DIRECTION ( 'NONE',  ( 0.000000000000000000, 0.000000000000000000, 1.000000000000000000 ) ) ;
#21059=FACE_OUTER_BOUND ( 'NONE', #39791, .T. ) ;
#21070=ORIENTED_EDGE ( 'NONE', *, *, #20055, .T. ) ;
#21073=VERTEX_POINT ( 'NONE', #24358 ) ;
#21079=CARTESIAN_POINT ( 'NONE',  ( 10.00000000000000000, -40.68715046381937128, 10.41901085202062660 ) ) ;
#21089=EDGE_LOOP ( 'NONE', ( #8020, #30785, #20744, #37558 ) ) ;
#21096=CARTESIAN_POINT ( 'NONE',  ( 0.000000000000000000, 0.000000000000000000, 0.000000000000000000 ) ) ;
#21102=EDGE_CURVE ( 'NONE', #14954, #20060, #46655, .T. ) ;
#21111=CIRCLE ( 'NONE', #10863, 42.00000000000000000 ) ;
#21119=ORIENTED_EDGE ( 'NONE', *, *, #38753, .T. ) ;
#21123=DIRECTION ( 'NONE',  ( -1.000000000000000000, 0.000000000000000000, 0.000000000000000000 ) ) ;
#21134=AXIS2_PLACEMENT_3D ( 'NONE', #27004, #35051, #12548 ) ;
#21148=AXIS2_PLACEMENT_3D ( 'NONE', #13524, #43398, #41409 ) ;
#21149=DIRECTION ( 'NONE',  ( 0.000000000000000000, 0.000000000000000000, 1.000000000000000000 ) ) ;
#21158=LINE ( 'NONE', #44407, #31316 ) ;
#21161=DIRECTION ( 'NONE',  ( -1.000000000000000000, 0.000000000000000000, 0.000000000000000000 ) ) ;
#21162=EDGE_CURVE ( 'NONE', #8930, #451, #30658, .T. ) ;
#21168=EDGE_LOOP ( 'NONE', ( #6161, #30780, #10414, #41573 ) ) ;
#21175=LINE ( 'NONE', #10662, #45897 ) ;
#21187=AXIS2_PLACEMENT_3D ( 'NONE', #37366, #30025, #23161 ) ;
#21192=DIRECTION ( 'NONE',  ( -1.000000000000000000, -0.000000000000000000, -0.000000000000000000 ) ) ;
#21193=ADVANCED_FACE ( 'NONE', ( #17742 ), #32667, .T. ) ;
#21198=DIRECTION ( 'NONE',  ( -1.000000000000000000, 0.000000000000000000, 0.000000000000000000 ) ) ;
#21203=ORIENTED_EDGE ( 'NONE', *, *, #19165, .T. ) ;
#21208=AXIS2_PLACEMENT_3D ( 'NONE', #23026, #30869, #45797 ) ;
#21210=DIRECTION ( 'NONE',  ( -1.000000000000000000, 0.000000000000000000, 0.000000000000000000 ) ) ;
#21219=ORIENTED_EDGE ( 'NONE', *, *, #26537, .F. ) ;
#21221=VECTOR ( 'NONE', #28758, 1000.000000000000000 ) ;
#21224=EDGE_LOOP ( 'NONE', ( #20734, #18956, #23876, #37586 ) ) ;
#21252=ORIENTED_EDGE ( 'NONE', *, *, #43071, .T. ) ;
#21254=ORIENTED_EDGE ( 'NONE', *, *, #14302, .F. ) ;
#21258=ORIENTED_EDGE ( 'NONE', *, *, #45319, .T. ) ;
#21278=ORIENTED_EDGE ( 'NONE', *, *, #48286, .T. ) ;
#21280=DIRECTION ( 'NONE',  ( 0.000000000000000000, 0.000000000000000000, 1.000000000000000000 ) ) ;
#21306=ORIENTED_EDGE ( 'NONE', *, *, #39812, .T. ) ;
#21310=VECTOR ( 'NONE', #38386, 1000.000000000000000 ) ;
#21311=ORIENTED_EDGE ( 'NONE', *, *, #45248, .T. ) ;
#21317=ORIENTED_EDGE ( 'NONE', *, *, #19635, .T. ) ;
#21325=ORIENTED_EDGE ( 'NONE', *, *, #12922, .F. ) ;
#21336=EDGE_LOOP ( 'NONE', ( #44274, #12470, #30652, #40638 ) ) ;
#21342=CARTESIAN_POINT ( 'NONE',  ( 10.00000000000000000, -17.80606268964516659, -33.00180498840066434 ) ) ;
#21356=AXIS2_PLACEMENT_3D ( 'NONE', #42792, #39612, #20985 ) ;
#21363=CIRCLE ( 'NONE', #12013, 42.00000000000000000 ) ;
#21368=AXIS2_PLACEMENT_3D ( 'NONE', #23472, #45505, #26927 ) ;
#21384=AXIS2_PLACEMENT_3D ( 'NONE', #12771, #27467, #35038 ) ;
#21386=DIRECTION ( 'NONE',  ( -1.000000000000000000, -0.000000000000000000, -0.000000000000000000 ) ) ;
#21388=ORIENTED_EDGE ( 'NONE', *, *, #47620, .T. ) ;
#21389=DIRECTION ( 'NONE',  ( 0.000000000000000000, -0.4539904997395351471, -0.8910065241883737830 ) ) ;
#21404=DIRECTION ( 'NONE',  ( 0.000000000000000000, -0.9510565162951565288, 0.3090169943749384029 ) ) ;
#21422=VERTEX_POINT ( 'NONE', #4509 ) ;
#21430=CARTESIAN_POINT ( 'NONE',  ( 10.00000000000000000, 35.38097989696512968, 12.42422080174651100 ) ) ;
#21447=VERTEX_POINT ( 'NONE', #24796 ) ;
#21466=DIRECTION ( 'NONE',  ( 0.000000000000000000, -0.3090169943749349057, -0.9510565162951576390 ) ) ;
#21481=FACE_OUTER_BOUND ( 'NONE', #13452, .T. ) ;
#21490=CARTESIAN_POINT ( 'NONE',  ( 10.00000000000000000, -10.41901085202050403, -40.68715046381940681 ) ) ;
#21492=EDGE_CURVE ( 'NONE', #22246, #30938, #28221, .T. ) ;
#21499=VECTOR ( 'NONE', #31553, 1000.000000000000000 ) ;
#21510=VERTEX_POINT ( 'NONE', #39738 ) ;
#21511=EDGE_LOOP ( 'NONE', ( #21119, #19392, #14353, #23478 ) ) ;
#21515=CIRCLE ( 'NONE', #3554, 16.00000000000000000 ) ;
#21519=EDGE_LOOP ( 'NONE', ( #39768, #24972, #32474, #21258 ) ) ;
#21532=ORIENTED_EDGE ( 'NONE', *, *, #661, .T. ) ;
#21558=EDGE_CURVE ( 'NONE', #28265, #13104, #28352, .T. ) ;
#21565=VECTOR ( 'NONE', #18646, 1000.000000000000000 ) ;
#21566=ORIENTED_EDGE ( 'NONE', *, *, #12331, .T. ) ;
#21583=ORIENTED_EDGE ( 'NONE', *, *, #2078, .T. ) ;
#21586=EDGE_CURVE ( 'NONE', #14862, #45459, #14919, .T. ) ;
#21592=CARTESIAN_POINT ( 'NONE',  ( 5.000000000000000000, -36.13751322684404244, -21.40280677340410165 ) ) ;
#21596=CARTESIAN_POINT ( 'NONE',  ( 0.000000000000000000, -39.04073710021332744, -15.48615015657624028 ) ) ;
#21604=CARTESIAN_POINT ( 'NONE',  ( 0.000000000000000000, 2.663952781846728790, -41.91543099594814947 ) ) ;
#21607=ORIENTED_EDGE ( 'NONE', *, *, #22115, .F. ) ;
#21626=ORIENTED_EDGE ( 'NONE', *, *, #9842, .F. ) ;
#21633=AXIS2_PLACEMENT_3D ( 'NONE', #10949, #25866, #40808 ) ;
#21647=EDGE_LOOP ( 'NONE', ( #31406, #34882, #21566, #9060 ) ) ;
#21651=DIRECTION ( 'NONE',  ( 1.000000000000000000, 0.000000000000000000, -0.000000000000000000 ) ) ;
#21662=VERTEX_POINT ( 'NONE', #45260 ) ;
#21667=EDGE_CURVE ( 'NONE', #43612, #26338, #10357, .T. ) ;
#21669=AXIS2_PLACEMENT_3D ( 'NONE', #23408, #20221, #28060 ) ;
#21671=LINE ( 'NONE', #44426, #40970 ) ;
#21677=VERTEX_POINT ( 'NONE', #7325 ) ;
#21682=ORIENTED_EDGE ( 'NONE', *, *, #18676, .T. ) ;
#21686=DIRECTION ( 'NONE',  ( -1.000000000000000000, 0.000000000000000000, 0.000000000000000000 ) ) ;
#21692=VERTEX_POINT ( 'NONE', #29599 ) ;
#21698=EDGE_CURVE ( 'NONE', #36999, #45459, #44530, .T. ) ;
#21701=DIRECTION ( 'NONE',  ( 0.000000000000000000, 0.000000000000000000, -1.000000000000000000 ) ) ;
#21703=DIRECTION ( 'NONE',  ( 0.000000000000000000, 0.000000000000000000, 1.000000000000000000 ) ) ;
#21712=CARTESIAN_POINT ( 'NONE',  ( 5.000000000000000000, 21.40280677340421889, -36.13751322684397138 ) ) ;
#21714=VERTEX_POINT ( 'NONE', #7579 ) ;
#21716=ORIENTED_EDGE ( 'NONE', *, *, #28295, .F. ) ;
#21729=EDGE_LOOP ( 'NONE', ( #36347, #23486, #2726, #48341 ) ) ;
#21738=ORIENTED_EDGE ( 'NONE', *, *, #32443, .F. ) ;
#21750=DIRECTION ( 'NONE',  ( 0.000000000000000000, 0.000000000000000000, 1.000000000000000000 ) ) ;
#21776=CARTESIAN_POINT ( 'NONE',  ( -10.00000000000000000, 0.000000000000000000, 0.000000000000000000 ) ) ;
#21784=EDGE_CURVE ( 'NONE', #23562, #44578, #41671, .T. ) ;
#21791=FACE_OUTER_BOUND ( 'NONE', #36959, .T. ) ;
#21799=CARTESIAN_POINT ( 'NONE',  ( 0.000000000000000000, 10.74501242461333028, -35.92658777277499382 ) ) ;
#21800=ORIENTED_EDGE ( 'NONE', *, *, #33361, .F. ) ;
#21813=ORIENTED_EDGE ( 'NONE', *, *, #36015, .T. ) ;
#21828=EDGE_CURVE ( 'NONE', #26808, #10918, #39325, .T. ) ;
#21832=CARTESIAN_POINT ( 'NONE',  ( 5.000000000000000000, 38.55633173627010279, 16.65560815589424593 ) ) ;
#21833=EDGE_CURVE ( 'NONE', #10918, #715, #15886, .T. ) ;
#21846=ORIENTED_EDGE ( 'NONE', *, *, #43552, .F. ) ;
#21865=DIRECTION ( 'NONE',  ( -1.000000000000000000, 0.000000000000000000, 0.000000000000000000 ) ) ;
#21870=DIRECTION ( 'NONE',  ( 0.000000000000000000, -1.000000000000000000, -1.040834085586084257E-14 ) ) ;
#21889=ORIENTED_EDGE ( 'NONE', *, *, #2472, .F. ) ;
#21903=ORIENTED_EDGE ( 'NONE', *, *, #3643, .T. ) ;
#21917=DIRECTION ( 'NONE',  ( -1.000000000000000000, -0.000000000000000000, 0.000000000000000000 ) ) ;
#21932=ORIENTED_EDGE ( 'NONE', *, *, #32175, .F. ) ;
#21935=EDGE_CURVE ( 'NONE', #46202, #26395, #32034, .T. ) ;
#21938=ADVANCED_FACE ( 'NONE', ( #6553 ), #16859, .T. ) ;
#21942=DIRECTION ( 'NONE',  ( -1.000000000000000000, -0.000000000000000000, -0.000000000000000000 ) ) ;
#21946=ORIENTED_EDGE ( 'NONE', *, *, #45424, .T. ) ;
#21954=AXIS2_PLACEMENT_3D ( 'NONE', #35008, #46273, #27934 ) ;
#21961=CARTESIAN_POINT ( 'NONE',  ( 10.00000000000000000, 0.000000000000000000, 0.000000000000000000 ) ) ;
#21966=FACE_OUTER_BOUND ( 'NONE', #6642, .T. ) ;
#21974=AXIS2_PLACEMENT_3D ( 'NONE', #2362, #35672, #32012 ) ;
#21987=EDGE_CURVE ( 'NONE', #1423, #13574, #44967, .T. ) ;
#22012=ORIENTED_EDGE ( 'NONE', *, *, #24530, .F. ) ;
#22023=VECTOR ( 'NONE', #27134, 1000.000000000000000 ) ;
#22032=ORIENTED_EDGE ( 'NONE', *, *, #38605, .F. ) ;
#22040=ORIENTED_EDGE ( 'NONE', *, *, #2174, .F. ) ;
#22051=DIRECTION ( 'NONE',  ( 0.000000000000000000, 0.8910065241883657894, 0.4539904997395509678 ) ) ;
#22052=CARTESIAN_POINT ( 'NONE',  ( 10.00000000000000000, -30.00120703465189465, -22.64427369931201639 ) ) ;
#22056=VERTEX_POINT ( 'NONE', #18999 ) ;
#22079=EDGE_LOOP ( 'NONE', ( #35743, #17052, #31155, #1432 ) ) ;
#22087=AXIS2_PLACEMENT_3D ( 'NONE', #15152, #41824, #29584 ) ;
#22094=VECTOR ( 'NONE', #475, 1000.000000000000000 ) ;
#22096=VECTOR ( 'NONE', #11665, 1000.000000000000000 ) ;
#22097=AXIS2_PLACEMENT_3D ( 'NONE', #33359, #10850, #18429 ) ;
#22104=EDGE_CURVE ( 'NONE', #13054, #33911, #10421, .T. ) ;
#22109=CIRCLE ( 'NONE', #195, 37.49900000000000233 ) ;
#22111=CARTESIAN_POINT ( 'NONE',  ( 0.000000000000000000, -37.48860685352290290, -0.8828120875904512665 ) ) ;
#22112=CARTESIAN_POINT ( 'NONE',  ( 0.000000000000000000, -17.80606268964563554, 33.00180498840040855 ) ) ;
#22113=CARTESIAN_POINT ( 'NONE',  ( 5.000000000000000000, 15.48615015657581750, 39.04073710021349797 ) ) ;
#22115=EDGE_CURVE ( 'NONE', #43390, #19329, #29958, .T. ) ;
#22116=CARTESIAN_POINT ( 'NONE',  ( 10.00000000000000000, 16.45098606841173705, -33.79645857604496229 ) ) ;
#22157=AXIS2_PLACEMENT_3D ( 'NONE', #5833, #34948, #16355 ) ;
#22165=DIRECTION ( 'NONE',  ( 0.000000000000000000, 0.5877852522924742473, -0.8090169943749465631 ) ) ;
#22171=ORIENTED_EDGE ( 'NONE', *, *, #32053, .T. ) ;
#22182=ORIENTED_EDGE ( 'NONE', *, *, #5203, .T. ) ;
#22188=DIRECTION ( 'NONE',  ( 0.000000000000000000, 0.8090169943749445647, 0.5877852522924770229 ) ) ;
#22208=CARTESIAN_POINT ( 'NONE',  ( 0.000000000000000000, -27.13269053701114331, 25.88420570971391754 ) ) ;
#22209=CARTESIAN_POINT ( 'NONE',  ( 0.000000000000000000, 0.000000000000000000, 0.000000000000000000 ) ) ;
#22211=ORIENTED_EDGE ( 'NONE', *, *, #34056, .F. ) ;
#22213=AXIS2_PLACEMENT_3D ( 'NONE', #18882, #41916, #8369 ) ;
#22226=VERTEX_POINT ( 'NONE', #19974 ) ;
#22228=DIRECTION ( 'NONE',  ( 1.000000000000000000, 0.000000000000000000, 0.000000000000000000 ) ) ;
#22230=VERTEX_POINT ( 'NONE', #31018 ) ;
#22234=CARTESIAN_POINT ( 'NONE',  ( 10.00000000000000000, 37.16516213103277977, 4.992566952385115719 ) ) ;
#22246=VERTEX_POINT ( 'NONE', #19253 ) ;
#22266=DIRECTION ( 'NONE',  ( 0.000000000000000000, 0.000000000000000000, 1.000000000000000000 ) ) ;
#22271=CARTESIAN_POINT ( 'NONE',  ( -10.00000000000000000, 0.000000000000000000, 0.000000000000000000 ) ) ;
#22274=CARTESIAN_POINT ( 'NONE',  ( 0.000000000000000000, 5.202137450156907761, -37.22597642581151689 ) ) ;
#22283=ADVANCED_FACE ( 'NONE', ( #31981 ), #46895, .T. ) ;
#22284=AXIS2_PLACEMENT_3D ( 'NONE', #12749, #32313, #24239 ) ;
#22299=ORIENTED_EDGE ( 'NONE', *, *, #48228, .F. ) ;
#22302=DIRECTION ( 'NONE',  ( 1.000000000000000000, -0.000000000000000000, -0.000000000000000000 ) ) ;
#22308=DIRECTION ( 'NONE',  ( -1.000000000000000000, 0.000000000000000000, -0.000000000000000000 ) ) ;
#22313=CARTESIAN_POINT ( 'NONE',  ( 10.00000000000000000, 0.000000000000000000, 0.000000000000000000 ) ) ;
#22314=ORIENTED_EDGE ( 'NONE', *, *, #18313, .F. ) ;
#22323=CARTESIAN_POINT ( 'NONE',  ( 10.00000000000000000, 37.48860685352291000, -0.8828120875901940279 ) ) ;
#22332=CARTESIAN_POINT ( 'NONE',  ( 0.000000000000000000, -37.16516213103280108, 4.992566952384862589 ) ) ;
#22336=LINE ( 'NONE', #21832, #13710 ) ;
#22338=DIRECTION ( 'NONE',  ( -1.000000000000000000, 0.000000000000000000, -0.000000000000000000 ) ) ;
#22345=EDGE_CURVE ( 'NONE', #34798, #46920, #28426, .T. ) ;
#22357=VECTOR ( 'NONE', #18411, 1000.000000000000000 ) ;
#22359=DIRECTION ( 'NONE',  ( 0.000000000000000000, 0.000000000000000000, -1.000000000000000000 ) ) ;
#22377=ORIENTED_EDGE ( 'NONE', *, *, #1150, .F. ) ;
#22387=DIRECTION ( 'NONE',  ( -1.000000000000000000, 0.000000000000000000, 0.000000000000000000 ) ) ;
#22391=CARTESIAN_POINT ( 'NONE',  ( 10.00000000000000000, 29.81001611431009479, 22.74946021919143391 ) ) ;
#22407=VERTEX_POINT ( 'NONE', #16799 ) ;
#22416=AXIS2_PLACEMENT_3D ( 'NONE', #25839, #10928, #21701 ) ;
#22421=EDGE_LOOP ( 'NONE', ( #43110, #46915, #137, #33779 ) ) ;
#22422=AXIS2_PLACEMENT_3D ( 'NONE', #12956, #20513, #28601 ) ;
#22424=EDGE_LOOP ( 'NONE', ( #28906, #7506, #34385, #7223 ) ) ;
#22433=DIRECTION ( 'NONE',  ( -1.000000000000000000, 0.000000000000000000, 0.000000000000000000 ) ) ;
#22460=DIRECTION ( 'NONE',  ( -1.000000000000000000, -0.000000000000000000, 0.000000000000000000 ) ) ;
#22462=AXIS2_PLACEMENT_3D ( 'NONE', #7190, #32653, #48308 ) ;
#22468=FILL_AREA_STYLE ('',( #41793 ) ) ;
#22472=CIRCLE ( 'NONE', #47471, 15.99999999999999822 ) ;
#22479=CYLINDRICAL_SURFACE ( 'NONE', #31999, 37.49900000000000233 ) ;
#22483=CARTESIAN_POINT ( 'NONE',  ( 10.00000000000000000, -37.58145647212455032, 0.6853352020789044152 ) ) ;
#22493=VERTEX_POINT ( 'NONE', #14809 ) ;
#22496=CARTESIAN_POINT ( 'NONE',  ( 0.000000000000000000, 30.00120703465205452, 22.64427369931179967 ) ) ;
#22505=DIRECTION ( 'NONE',  ( 0.000000000000000000, 0.000000000000000000, 1.000000000000000000 ) ) ;
#22507=DIRECTION ( 'NONE',  ( 1.000000000000000000, 0.000000000000000000, 0.000000000000000000 ) ) ;
#22532=ORIENTED_EDGE ( 'NONE', *, *, #14104, .F. ) ;
#22533=CARTESIAN_POINT ( 'NONE',  ( 10.00000000000000000, -5.202137450156655518, 37.22597642581156663 ) ) ;
#22548=VERTEX_POINT ( 'NONE', #17975 ) ;
#22549=DIRECTION ( 'NONE',  ( 1.000000000000000000, 0.000000000000000000, -0.000000000000000000 ) ) ;
#22553=ORIENTED_EDGE ( 'NONE', *, *, #38666, .F. ) ;
#22560=FACE_OUTER_BOUND ( 'NONE', #9908, .T. ) ;
#22561=ADVANCED_FACE ( 'NONE', ( #41973 ), #597, .T. ) ;
#22569=DIRECTION ( 'NONE',  ( 0.000000000000000000, -0.8910065241883626808, -0.4539904997395570740 ) ) ;
#22570=CARTESIAN_POINT ( 'NONE',  ( 10.00000000000000000, 37.16516213103285082, -4.992566952384588141 ) ) ;
#22577=DIRECTION ( 'NONE',  ( -1.000000000000000000, 0.000000000000000000, 0.000000000000000000 ) ) ;
#22583=AXIS2_PLACEMENT_3D ( 'NONE', #14887, #11214, #180 ) ;
#22586=AXIS2_PLACEMENT_3D ( 'NONE', #48166, #29330, #40359 ) ;
#22587=ORIENTED_EDGE ( 'NONE', *, *, #31126, .T. ) ;
#22596=EDGE_CURVE ( 'NONE', #29992, #409, #21363, .T. ) ;
#22602=MECHANICAL_DESIGN_GEOMETRIC_PRESENTATION_REPRESENTATION('',(#16359),#26452);
#22603=DIRECTION ( 'NONE',  ( -1.000000000000000000, 0.000000000000000000, -0.000000000000000000 ) ) ;
#22608=CARTESIAN_POINT ( 'NONE',  ( -10.00000000000000000, 0.000000000000000000, 0.000000000000000000 ) ) ;
#22612=CARTESIAN_POINT ( 'NONE',  ( -10.00000000000000000, 0.000000000000000000, 0.000000000000000000 ) ) ;
#22643=VECTOR ( 'NONE', #33840, 1000.000000000000000 ) ;
#22657=DIRECTION ( 'NONE',  ( -1.000000000000000000, -0.000000000000000000, 0.000000000000000000 ) ) ;
#22715=VERTEX_POINT ( 'NONE', #39506 ) ;
#22718=CIRCLE ( 'NONE', #45389, 16.00000000000000000 ) ;
#22721=CARTESIAN_POINT ( 'NONE',  ( 0.000000000000000000, 22.48208911017500355, 35.47612816024530957 ) ) ;
#22732=FACE_OUTER_BOUND ( 'NONE', #37373, .T. ) ;
#22736=CYLINDRICAL_SURFACE ( 'NONE', #11832, 42.00000000000000000 ) ;
#22739=DIRECTION ( 'NONE',  ( -1.000000000000000000, 0.000000000000000000, 0.000000000000000000 ) ) ;
#22741=DIRECTION ( 'NONE',  ( -1.000000000000000000, -0.000000000000000000, -0.000000000000000000 ) ) ;
#22752=AXIS2_PLACEMENT_3D ( 'NONE', #9468, #40066, #36389 ) ;
#22773=ORIENTED_EDGE ( 'NONE', *, *, #22596, .F. ) ;
#22774=FACE_OUTER_BOUND ( 'NONE', #7331, .T. ) ;
#22777=DIRECTION ( 'NONE',  ( -1.000000000000000000, 0.000000000000000000, 0.000000000000000000 ) ) ;
#22792=CARTESIAN_POINT ( 'NONE',  ( 0.000000000000000000, -36.88895765772637247, 6.736453364083436313 ) ) ;
#22815=VERTEX_POINT ( 'NONE', #20392 ) ;
#22817=VERTEX_POINT ( 'NONE', #46607 ) ;
#22818=DIRECTION ( 'NONE',  ( 0.000000000000000000, 0.8910065241883656784, 0.4539904997395511899 ) ) ;
#22835=FACE_OUTER_BOUND ( 'NONE', #27850, .T. ) ;
#22841=DIRECTION ( 'NONE',  ( -1.000000000000000000, 0.000000000000000000, -0.000000000000000000 ) ) ;
#22869=AXIS2_PLACEMENT_3D ( 'NONE', #14371, #29302, #25848 ) ;
#22870=CARTESIAN_POINT ( 'NONE',  ( 4.999999999999999112, -3.925862922255855647, -41.81611651403866858 ) ) ;
#22873=EDGE_CURVE ( 'NONE', #12321, #1420, #28470, .T. ) ;
#22881=CYLINDRICAL_SURFACE ( 'NONE', #18726, 16.00000000000000000 ) ;
#22884=AXIS2_PLACEMENT_3D ( 'NONE', #34516, #41894, #38448 ) ;
#22900=ORIENTED_EDGE ( 'NONE', *, *, #14034, .F. ) ;
#22918=ADVANCED_FACE ( 'NONE', ( #33581 ), #3728, .T. ) ;
#22931=AXIS2_PLACEMENT_3D ( 'NONE', #21961, #36885, #48161 ) ;
#22945=ORIENTED_EDGE ( 'NONE', *, *, #43826, .T. ) ;
#22957=CARTESIAN_POINT ( 'NONE',  ( 10.00000000000000000, 0.000000000000000000, 0.000000000000000000 ) ) ;
#22963=AXIS2_PLACEMENT_3D ( 'NONE', #33412, #37326, #33638 ) ;
#22964=DIRECTION ( 'NONE',  ( 0.000000000000000000, 0.000000000000000000, 1.000000000000000000 ) ) ;
#22967=ORIENTED_EDGE ( 'NONE', *, *, #18669, .F. ) ;
#22981=CARTESIAN_POINT ( 'NONE',  ( 10.00000000000000000, -10.96151621346461447, -35.95386929396268272 ) ) ;
#22995=EDGE_CURVE ( 'NONE', #36805, #21677, #43317, .T. ) ;
#23007=EDGE_LOOP ( 'NONE', ( #10174, #30224, #1782, #125 ) ) ;
#23013=ORIENTED_EDGE ( 'NONE', *, *, #27422, .F. ) ;
#23018=EDGE_LOOP ( 'NONE', ( #35098, #4079, #30244, #1229 ) ) ;
#23021=CARTESIAN_POINT ( 'NONE',  ( 0.000000000000000000, 0.000000000000000000, 0.000000000000000000 ) ) ;
#23022=ORIENTED_EDGE ( 'NONE', *, *, #24868, .T. ) ;
#23026=CARTESIAN_POINT ( 'NONE',  ( 10.00000000000000000, -35.53030884539077050, -12.26510123303296851 ) ) ;
#23028=DIRECTION ( 'NONE',  ( -1.000000000000000000, 0.000000000000000000, 0.000000000000000000 ) ) ;
#23033=EDGE_LOOP ( 'NONE', ( #18531, #41483, #46018, #36961 ) ) ;
#23035=DIRECTION ( 'NONE',  ( -1.000000000000000000, 0.000000000000000000, 0.000000000000000000 ) ) ;
#23049=CYLINDRICAL_SURFACE ( 'NONE', #24683, 37.49900000000000233 ) ;
#23054=CIRCLE ( 'NONE', #4303, 42.00000000000000000 ) ;
#23068=EDGE_CURVE ( 'NONE', #46997, #908, #37991, .T. ) ;
#23073=ORIENTED_EDGE ( 'NONE', *, *, #20827, .F. ) ;
#23076=CIRCLE ( 'NONE', #12925, 42.00000000000000000 ) ;
#23085=CYLINDRICAL_SURFACE ( 'NONE', #23128, 42.00000000000000000 ) ;
#23092=DIRECTION ( 'NONE',  ( -1.000000000000000000, 0.000000000000000000, -0.000000000000000000 ) ) ;
#23113=DIRECTION ( 'NONE',  ( 0.000000000000000000, 0.000000000000000000, 1.000000000000000000 ) ) ;
#23115=DIRECTION ( 'NONE',  ( -1.000000000000000000, -0.000000000000000000, -0.000000000000000000 ) ) ;
#23120=FACE_OUTER_BOUND ( 'NONE', #11428, .T. ) ;
#23128=AXIS2_PLACEMENT_3D ( 'NONE', #37526, #15503, #11830 ) ;
#23134=CARTESIAN_POINT ( 'NONE',  ( 0.000000000000000000, 33.17418723428333749, -17.67226234102790272 ) ) ;
#23146=ORIENTED_EDGE ( 'NONE', *, *, #26399, .T. ) ;
#23152=AXIS2_PLACEMENT_3D ( 'NONE', #28930, #40214, #39976 ) ;
#23155=CARTESIAN_POINT ( 'NONE',  ( 4.999999999999999112, 40.98264845739763018, -9.188173127306860977 ) ) ;
#23161=DIRECTION ( 'NONE',  ( 0.000000000000000000, 0.000000000000000000, 1.000000000000000000 ) ) ;
#23165=DIRECTION ( 'NONE',  ( 0.000000000000000000, 0.000000000000000000, 1.000000000000000000 ) ) ;
#23173=CARTESIAN_POINT ( 'NONE',  ( 10.00000000000000000, 0.000000000000000000, 0.000000000000000000 ) ) ;
#23193=EDGE_CURVE ( 'NONE', #46188, #47238, #38962, .T. ) ;
#23196=CIRCLE ( 'NONE', #36473, 42.00000000000000000 ) ;
#23197=EDGE_CURVE ( 'NONE', #25587, #1295, #19885, .T. ) ;
#23200=EDGE_LOOP ( 'NONE', ( #21583, #30542, #11893, #43718, #21306, #1199, #6825, #21903, #44371, #24806, #32483, #986, #21203, #60, #27418, #1578, #34861, #31707, #19268, #10121, #35373, #46253, #2715, #33037, #760, #28118, #24174, #16706, #41277, #21813, #10861, #13877, #5022, #41165, #9457, #17754, #37534, #40537, #1771, #25569, #6111, #13745, #34432, #27440, #48379, #6184, #11708, #11152, #44694, #29674, #7998, #41258, #32642, #15256, #40666, #44155, #42674, #12938, #12612, #17778, #34265, #7044, #9992, #67, #11486, #18573, #35164, #42205, #19677, #14454, #24933, #47265, #25645, #11551, #11765, #36176, #13345, #20862, #18197, #34304, #37749, #16626, #18271, #40531, #28795, #15577, #6296, #2431, #5815, #36811, #8520, #35296, #4193, #8548, #4658, #11653, #48038, #6039, #12832, #40378, #45482, #27930, #42770, #17471, #34030, #22182, #23690, #15933, #36728, #1228, #13024, #46993, #25693, #1814, #35833, #24205, #33242, #23565, #15841, #36922, #35066, #21070, #10213, #41036, #10796, #33769, #1555, #31382, #1475, #26662, #10244, #40384, #10085, #41982, #42362, #45932, #29868, #25349, #27620, #46696, #12201, #14282, #45485, #5101, #21278, #11815, #34600, #43913, #6353, #19027, #28231, #35502, #41818, #24046, #33055, #3361, #48307, #12294, #47577, #383, #15838, #18633, #42766, #40450, #28067 ) ) ;
#23214=EDGE_CURVE ( 'NONE', #43260, #5351, #364, .T. ) ;
#23228=EDGE_CURVE ( 'NONE', #13266, #13632, #5064, .T. ) ;
#23247=FACE_OUTER_BOUND ( 'NONE', #10140, .T. ) ;
#23248=DIRECTION ( 'NONE',  ( -1.000000000000000000, -0.000000000000000000, 0.000000000000000000 ) ) ;
#23266=DIRECTION ( 'NONE',  ( 0.000000000000000000, 0.7071067811865437980, 0.7071067811865512365 ) ) ;
#23286=CARTESIAN_POINT ( 'NONE',  ( 10.00000000000000000, 0.000000000000000000, 0.000000000000000000 ) ) ;
#23289=DIRECTION ( 'NONE',  ( 0.000000000000000000, 0.000000000000000000, 1.000000000000000000 ) ) ;
#23294=DIRECTION ( 'NONE',  ( 0.000000000000000000, 0.000000000000000000, 1.000000000000000000 ) ) ;
#23303=VERTEX_POINT ( 'NONE', #40625 ) ;
#23319=EDGE_LOOP ( 'NONE', ( #31876, #34812, #12207, #4643 ) ) ;
#23323=CARTESIAN_POINT ( 'NONE',  ( 0.000000000000000000, -27.75498641678720446, -31.52238457039628727 ) ) ;
#23333=DIRECTION ( 'NONE',  ( -1.000000000000000000, 0.000000000000000000, 0.000000000000000000 ) ) ;
#23335=CYLINDRICAL_SURFACE ( 'NONE', #36789, 42.00000000000000000 ) ;
#23344=CARTESIAN_POINT ( 'NONE',  ( 0.000000000000000000, -30.84782396557233142, 21.32104025579104345 ) ) ;
#23361=VERTEX_POINT ( 'NONE', #11012 ) ;
#23372=ORIENTED_EDGE ( 'NONE', *, *, #34056, .T. ) ;
#23386=DIRECTION ( 'NONE',  ( 1.000000000000000000, 0.000000000000000000, 0.000000000000000000 ) ) ;
#23392=DIRECTION ( 'NONE',  ( -1.000000000000000000, -0.000000000000000000, -0.000000000000000000 ) ) ;
#23393=DIRECTION ( 'NONE',  ( 0.000000000000000000, 0.000000000000000000, 1.000000000000000000 ) ) ;
#23404=CARTESIAN_POINT ( 'NONE',  ( 10.00000000000000000, 0.000000000000000000, 0.000000000000000000 ) ) ;
#23408=CARTESIAN_POINT ( 'NONE',  ( 0.000000000000000000, 0.000000000000000000, 0.000000000000000000 ) ) ;
#23409=CARTESIAN_POINT ( 'NONE',  ( 10.00000000000000000, -26.08949754953005495, -27.05870788708258701 ) ) ;
#23431=DIRECTION ( 'NONE',  ( 0.000000000000000000, 0.8090169943749447867, 0.5877852522924769119 ) ) ;
#23436=DIRECTION ( 'NONE',  ( 0.000000000000000000, 0.000000000000000000, 1.000000000000000000 ) ) ;
#23459=CARTESIAN_POINT ( 'NONE',  ( 10.00000000000000000, 0.000000000000000000, 0.000000000000000000 ) ) ;
#23461=VECTOR ( 'NONE', #23028, 1000.000000000000000 ) ;
#23465=CARTESIAN_POINT ( 'NONE',  ( 5.000000000000000000, 27.75498641678786527, -31.52238457039571173 ) ) ;
#23472=CARTESIAN_POINT ( 'NONE',  ( 10.00000000000000000, -27.05870788708250885, 26.08949754953014022 ) ) ;
#23478=ORIENTED_EDGE ( 'NONE', *, *, #35259, .T. ) ;
#23486=ORIENTED_EDGE ( 'NONE', *, *, #13185, .T. ) ;
#23505=CARTESIAN_POINT ( 'NONE',  ( 10.00000000000000000, -21.53537804866058991, -30.80686688397033635 ) ) ;
#23508=DIRECTION ( 'NONE',  ( 1.000000000000000000, -0.000000000000000000, 0.000000000000000000 ) ) ;
#23513=CYLINDRICAL_SURFACE ( 'NONE', #29790, 37.49900000000000233 ) ;
#23514=CARTESIAN_POINT ( 'NONE',  ( 10.00000000000000000, 0.000000000000000000, 0.000000000000000000 ) ) ;
#23515=CYLINDRICAL_SURFACE ( 'NONE', #4653, 16.00000000000000000 ) ;
#23518=VECTOR ( 'NONE', #30220, 1000.000000000000000 ) ;
#23521=DIRECTION ( 'NONE',  ( 0.000000000000000000, 0.000000000000000000, 1.000000000000000000 ) ) ;
#23529=CARTESIAN_POINT ( 'NONE',  ( 10.00000000000000000, 35.53030884539084866, 12.26510123303271982 ) ) ;
#23532=AXIS2_PLACEMENT_3D ( 'NONE', #10269, #47004, #35746 ) ;
#23539=DIRECTION ( 'NONE',  ( 0.000000000000000000, -0.9510565162951500895, -0.3090169943749583314 ) ) ;
#23541=EDGE_CURVE ( 'NONE', #32362, #34492, #27741, .T. ) ;
#23550=DIRECTION ( 'NONE',  ( 1.000000000000000000, 0.000000000000000000, -0.000000000000000000 ) ) ;
#23557=AXIS2_PLACEMENT_3D ( 'NONE', #42798, #9253, #9727 ) ;
#23562=VERTEX_POINT ( 'NONE', #32460 ) ;
#23565=ORIENTED_EDGE ( 'NONE', *, *, #8449, .T. ) ;
#23567=DIRECTION ( 'NONE',  ( 0.000000000000000000, -0.4539904997395352027, -0.8910065241883737830 ) ) ;
#23568=AXIS2_PLACEMENT_3D ( 'NONE', #19564, #973, #4188 ) ;
#23569=DIRECTION ( 'NONE',  ( 1.000000000000000000, 0.000000000000000000, 0.000000000000000000 ) ) ;
#23570=DIRECTION ( 'NONE',  ( 1.000000000000000000, 0.000000000000000000, -0.000000000000000000 ) ) ;
#23579=LINE ( 'NONE', #4281, #30914 ) ;
#23596=DIRECTION ( 'NONE',  ( 0.000000000000000000, 0.000000000000000000, 1.000000000000000000 ) ) ;
#23603=AXIS2_PLACEMENT_3D ( 'NONE', #31055, #16350, #12930 ) ;
#23605=VERTEX_POINT ( 'NONE', #40041 ) ;
#23616=DIRECTION ( 'NONE',  ( -1.000000000000000000, 0.000000000000000000, -0.000000000000000000 ) ) ;
#23621=FACE_OUTER_BOUND ( 'NONE', #29167, .T. ) ;
#23632=CARTESIAN_POINT ( 'NONE',  ( 0.000000000000000000, -17.80606268964516659, -33.00180498840066434 ) ) ;
#23638=SURFACE_STYLE_FILL_AREA ( #13123 ) ;
#23646=CARTESIAN_POINT ( 'NONE',  ( 10.00000000000000000, -41.91543099594819921, 2.663952781846001816 ) ) ;
#23649=FACE_OUTER_BOUND ( 'NONE', #24173, .T. ) ;
#23650=DIRECTION ( 'NONE',  ( 0.000000000000000000, 0.000000000000000000, 1.000000000000000000 ) ) ;
#23681=EDGE_LOOP ( 'NONE', ( #20162, #19949, #22553, #13971 ) ) ;
#23685=ORIENTED_EDGE ( 'NONE', *, *, #45820, .T. ) ;
#23686=CARTESIAN_POINT ( 'NONE',  ( 10.00000000000000000, -22.74946021919153694, 29.81001611431000597 ) ) ;
#23690=ORIENTED_EDGE ( 'NONE', *, *, #45847, .T. ) ;
#23696=CYLINDRICAL_SURFACE ( 'NONE', #11628, 16.00000000000000000 ) ;
#23703=DIRECTION ( 'NONE',  ( -1.000000000000000000, 0.000000000000000000, -0.000000000000000000 ) ) ;
#23712=DIRECTION ( 'NONE',  ( -1.000000000000000000, -0.000000000000000000, -0.000000000000000000 ) ) ;
#23721=DIRECTION ( 'NONE',  ( 1.000000000000000000, 0.000000000000000000, 0.000000000000000000 ) ) ;
#23727=CIRCLE ( 'NONE', #22931, 42.00000000000000000 ) ;
#23743=DIRECTION ( 'NONE',  ( 1.000000000000000000, -0.000000000000000000, -0.000000000000000000 ) ) ;
#23746=DIRECTION ( 'NONE',  ( -1.000000000000000000, -0.000000000000000000, -0.000000000000000000 ) ) ;
#23775=CARTESIAN_POINT ( 'NONE',  ( 10.00000000000000000, 27.05870788708231700, 26.08949754953034272 ) ) ;
#23783=ORIENTED_EDGE ( 'NONE', *, *, #18091, .F. ) ;
#23794=CIRCLE ( 'NONE', #8947, 16.00000000000000000 ) ;
#23808=ADVANCED_FACE ( 'NONE', ( #2255 ), #36507, .T. ) ;
#23813=ORIENTED_EDGE ( 'NONE', *, *, #9541, .T. ) ;
#23824=CIRCLE ( 'NONE', #30079, 16.00000000000000000 ) ;
#23838=CARTESIAN_POINT ( 'NONE',  ( 10.00000000000000000, 21.32104025579158701, -30.84782396557194772 ) ) ;
#23844=AXIS2_PLACEMENT_3D ( 'NONE', #42310, #38894, #46720 ) ;
#23849=ORIENTED_EDGE ( 'NONE', *, *, #11233, .F. ) ;
#23872=ORIENTED_EDGE ( 'NONE', *, *, #31330, .F. ) ;
#23876=ORIENTED_EDGE ( 'NONE', *, *, #39431, .T. ) ;
#23890=DIRECTION ( 'NONE',  ( 0.000000000000000000, 0.9510565162951521989, 0.3090169943749515591 ) ) ;
#23900=FACE_OUTER_BOUND ( 'NONE', #33959, .T. ) ;
#23918=VERTEX_POINT ( 'NONE', #6660 ) ;
#23923=ORIENTED_EDGE ( 'NONE', *, *, #22873, .T. ) ;
#23925=ORIENTED_EDGE ( 'NONE', *, *, #17385, .T. ) ;
#23931=LINE ( 'NONE', #27598, #32134 ) ;
#23934=ORIENTED_EDGE ( 'NONE', *, *, #21935, .F. ) ;
#23972=ORIENTED_EDGE ( 'NONE', *, *, #4440, .F. ) ;
#23974=EDGE_CURVE ( 'NONE', #46639, #42124, #23076, .T. ) ;
#23982=VERTEX_POINT ( 'NONE', #37042 ) ;
#24004=CARTESIAN_POINT ( 'NONE',  ( 0.000000000000000000, 0.000000000000000000, 0.000000000000000000 ) ) ;
#24016=CIRCLE ( 'NONE', #5256, 37.49900000000000944 ) ;
#24018=DIRECTION ( 'NONE',  ( 0.000000000000000000, 0.000000000000000000, 1.000000000000000000 ) ) ;
#24021=EDGE_CURVE ( 'NONE', #19470, #45584, #435, .T. ) ;
#24031=DIRECTION ( 'NONE',  ( 0.000000000000000000, 0.000000000000000000, 1.000000000000000000 ) ) ;
#24032=ORIENTED_EDGE ( 'NONE', *, *, #30515, .F. ) ;
#24035=AXIS2_PLACEMENT_3D ( 'NONE', #33141, #14057, #29704 ) ;
#24046=ORIENTED_EDGE ( 'NONE', *, *, #46924, .T. ) ;
#24074=ORIENTED_EDGE ( 'NONE', *, *, #27496, .F. ) ;
#24075=CARTESIAN_POINT ( 'NONE',  ( 0.000000000000000000, -6.736453364083290651, -36.88895765772640090 ) ) ;
#24076=CARTESIAN_POINT ( 'NONE',  ( 10.00000000000000000, -35.92658777277517856, 10.74501242461269257 ) ) ;
#24079=CARTESIAN_POINT ( 'NONE',  ( 0.000000000000000000, -16.65560815589439159, 38.55633173627004595 ) ) ;
#24082=CARTESIAN_POINT ( 'NONE',  ( 10.00000000000000000, 25.88420570971400991, 27.13269053701105449 ) ) ;
#24107=EDGE_LOOP ( 'NONE', ( #41432, #29450, #28949, #25217 ) ) ;
#24109=EDGE_CURVE ( 'NONE', #46672, #6962, #20743, .T. ) ;
#24126=DIRECTION ( 'NONE',  ( 0.000000000000000000, -6.938893903907228378E-15, 1.000000000000000000 ) ) ;
#24140=EDGE_CURVE ( 'NONE', #25302, #7292, #26947, .T. ) ;
#24141=CARTESIAN_POINT ( 'NONE',  ( -10.00000000000000000, 0.000000000000000000, 0.000000000000000000 ) ) ;
#24145=EDGE_CURVE ( 'NONE', #20591, #25493, #34849, .T. ) ;
#24152=VERTEX_POINT ( 'NONE', #5157 ) ;
#24173=EDGE_LOOP ( 'NONE', ( #34701, #27401, #8686, #19994 ) ) ;
#24174=ORIENTED_EDGE ( 'NONE', *, *, #42573, .F. ) ;
#24175=LINE ( 'NONE', #16838, #22023 ) ;
#24178=CARTESIAN_POINT ( 'NONE',  ( 10.00000000000000000, 37.58145647212455032, -0.6853352020786441789 ) ) ;
#24181=ORIENTED_EDGE ( 'NONE', *, *, #12178, .F. ) ;
#24192=CARTESIAN_POINT ( 'NONE',  ( 0.000000000000000000, 41.91543099594818500, 2.663952781846294915 ) ) ;
#24199=DIRECTION ( 'NONE',  ( 0.000000000000000000, 0.000000000000000000, 1.000000000000000000 ) ) ;
#24205=ORIENTED_EDGE ( 'NONE', *, *, #31805, .T. ) ;
#24213=DIRECTION ( 'NONE',  ( 0.000000000000000000, 0.000000000000000000, 1.000000000000000000 ) ) ;
#24217=EDGE_CURVE ( 'NONE', #38437, #30519, #4657, .T. ) ;
#24237=EDGE_LOOP ( 'NONE', ( #34254, #10607, #28152, #20334 ) ) ;
#24239=DIRECTION ( 'NONE',  ( 0.000000000000000000, 0.000000000000000000, 1.000000000000000000 ) ) ;
#24240=ORIENTED_EDGE ( 'NONE', *, *, #46493, .F. ) ;
#24242=FACE_OUTER_BOUND ( 'NONE', #3057, .T. ) ;
#24259=EDGE_CURVE ( 'NONE', #26816, #32422, #25442, .T. ) ;
#24261=CARTESIAN_POINT ( 'NONE',  ( -1.200000000000000030E-05, 16.95692799528845995, 2.500000000000000000 ) ) ;
#24262=EDGE_CURVE ( 'NONE', #45536, #2845, #12194, .T. ) ;
#24265=DIRECTION ( 'NONE',  ( 0.000000000000000000, 1.000000000000000000, 3.491481338843133750E-15 ) ) ;
#24266=VECTOR ( 'NONE', #43204, 1000.000000000000000 ) ;
#24272=CIRCLE ( 'NONE', #3150, 37.49900000000000944 ) ;
#24278=DIRECTION ( 'NONE',  ( -1.000000000000000000, -0.000000000000000000, 0.000000000000000000 ) ) ;
#24282=ORIENTED_EDGE ( 'NONE', *, *, #13158, .T. ) ;
#24285=CARTESIAN_POINT ( 'NONE',  ( 10.00000000000000000, -26.79245525562691199, -32.34446384430000876 ) ) ;
#24298=CIRCLE ( 'NONE', #37614, 37.49900000000000944 ) ;
#24300=CARTESIAN_POINT ( 'NONE',  ( -10.00000000000000000, 0.000000000000000000, 0.000000000000000000 ) ) ;
#24307=AXIS2_PLACEMENT_3D ( 'NONE', #43575, #6373, #44292 ) ;
#24310=CARTESIAN_POINT ( 'NONE',  ( 10.00000000000000178, 0.000000000000000000, 0.000000000000000000 ) ) ;
#24315=EDGE_CURVE ( 'NONE', #1295, #12027, #28611, .T. ) ;
#24316=CARTESIAN_POINT ( 'NONE',  ( 10.00000000000000000, 0.000000000000000000, 0.000000000000000000 ) ) ;
#24324=FACE_OUTER_BOUND ( 'NONE', #5320, .T. ) ;
#24325=CARTESIAN_POINT ( 'NONE',  ( 10.00000000000000178, 12.24744871391589385, -2.499999999999995559 ) ) ;
#24340=ORIENTED_EDGE ( 'NONE', *, *, #24386, .F. ) ;
#24353=CARTESIAN_POINT ( 'NONE',  ( 10.00000000000000000, 0.000000000000000000, 0.000000000000000000 ) ) ;
#24358=CARTESIAN_POINT ( 'NONE',  ( 10.00000000000000000, -32.34446384429989507, 26.79245525562703278 ) ) ;
#24361=ORIENTED_EDGE ( 'NONE', *, *, #47591, .F. ) ;
#24362=AXIS2_PLACEMENT_3D ( 'NONE', #45591, #22841, #11366 ) ;
#24365=CIRCLE ( 'NONE', #30625, 42.00000000000000000 ) ;
#24370=CIRCLE ( 'NONE', #7942, 37.49900000000000233 ) ;
#24371=DIRECTION ( 'NONE',  ( 0.000000000000000000, 0.7071067811865486830, -0.7071067811865463515 ) ) ;
#24374=CARTESIAN_POINT ( 'NONE',  ( 0.000000000000000000, 36.13751322684419165, 21.40280677340384585 ) ) ;
#24385=VERTEX_POINT ( 'NONE', #29816 ) ;
#24386=EDGE_CURVE ( 'NONE', #908, #36805, #15337, .T. ) ;
#24388=AXIS2_PLACEMENT_3D ( 'NONE', #34121, #596, #10891 ) ;
#24399=ORIENTED_EDGE ( 'NONE', *, *, #27544, .T. ) ;
#24409=ADVANCED_FACE ( 'NONE', ( #4124 ), #19036, .T. ) ;
#24412=CARTESIAN_POINT ( 'NONE',  ( 0.000000000000000000, -2.446882695291883605E-15, -2.499999999999983569 ) ) ;
#24416=CYLINDRICAL_SURFACE ( 'NONE', #11026, 16.00000000000000000 ) ;
#24425=EDGE_LOOP ( 'NONE', ( #16776, #47234, #42408, #22773 ) ) ;
#24426=DIRECTION ( 'NONE',  ( 0.000000000000000000, 0.000000000000000000, 1.000000000000000000 ) ) ;
#24432=AXIS2_PLACEMENT_3D ( 'NONE', #14751, #14514, #45320 ) ;
#24450=FACE_OUTER_BOUND ( 'NONE', #25351, .T. ) ;
#24454=VECTOR ( 'NONE', #19146, 1000.000000000000000 ) ;
#24472=ORIENTED_EDGE ( 'NONE', *, *, #1740, .T. ) ;
#24485=LINE ( 'NONE', #1989, #32408 ) ;
#24486=DIRECTION ( 'NONE',  ( -1.000000000000000000, 0.000000000000000000, 0.000000000000000000 ) ) ;
#24493=DIRECTION ( 'NONE',  ( -1.000000000000000000, 0.000000000000000000, 0.000000000000000000 ) ) ;
#24498=CYLINDRICAL_SURFACE ( 'NONE', #12450, 16.00000000000000000 ) ;
#24513=AXIS2_PLACEMENT_3D ( 'NONE', #13358, #43696, #25085 ) ;
#24519=EDGE_LOOP ( 'NONE', ( #47120, #15418, #24361, #43587, #771, #31343 ) ) ;
#24530=EDGE_CURVE ( 'NONE', #47530, #16794, #14570, .T. ) ;
#24541=ADVANCED_FACE ( 'NONE', ( #26883 ), #8278, .T. ) ;
#24544=CIRCLE ( 'NONE', #36237, 37.49900000000000233 ) ;
#24580=CARTESIAN_POINT ( 'NONE',  ( 10.00000000000000000, 6.736453364083557105, 36.88895765772635826 ) ) ;
#24588=EDGE_CURVE ( 'NONE', #32422, #8858, #8746, .T. ) ;
#24612=CARTESIAN_POINT ( 'NONE',  ( 10.00000000000000000, 6.555932627142418312, 37.01155633439060466 ) ) ;
#24621=DIRECTION ( 'NONE',  ( -1.000000000000000000, 0.000000000000000000, -0.000000000000000000 ) ) ;
#24634=ORIENTED_EDGE ( 'NONE', *, *, #30913, .T. ) ;
#24638=EDGE_LOOP ( 'NONE', ( #42040, #9298, #10510, #14703 ) ) ;
#24640=AXIS2_PLACEMENT_3D ( 'NONE', #13302, #47318, #9374 ) ;
#24641=ADVANCED_FACE ( 'NONE', ( #26636 ), #27131, .T. ) ;
#24647=EDGE_LOOP ( 'NONE', ( #43183, #13974, #15684, #18079 ) ) ;
#24662=FACE_OUTER_BOUND ( 'NONE', #44151, .T. ) ;
#24676=DIRECTION ( 'NONE',  ( -1.000000000000000000, -0.000000000000000000, -0.000000000000000000 ) ) ;
#24682=CARTESIAN_POINT ( 'NONE',  ( 10.00000000000000000, -16.45098606841149902, 33.79645857604508308 ) ) ;
#24683=AXIS2_PLACEMENT_3D ( 'NONE', #30167, #46056, #12046 ) ;
#24718=DIRECTION ( 'NONE',  ( 0.000000000000000000, 0.3090169943749411230, 0.9510565162951555296 ) ) ;
#24728=VERTEX_POINT ( 'NONE', #31533 ) ;
#24752=AXIS2_PLACEMENT_3D ( 'NONE', #886, #37383, #11457 ) ;
#24754=FACE_OUTER_BOUND ( 'NONE', #1192, .T. ) ;
#24760=VECTOR ( 'NONE', #27074, 1000.000000000000000 ) ;
#24775=CIRCLE ( 'NONE', #37279, 37.49900000000001654 ) ;
#24784=FACE_OUTER_BOUND ( 'NONE', #46003, .T. ) ;
#24788=ORIENTED_EDGE ( 'NONE', *, *, #47620, .F. ) ;
#24796=CARTESIAN_POINT ( 'NONE',  ( 0.000000000000000000, -10.41901085202050581, -40.68715046381939970 ) ) ;
#24798=CIRCLE ( 'NONE', #11560, 37.49900000000000233 ) ;
#24799=CARTESIAN_POINT ( 'NONE',  ( 10.00000000000000000, -38.55633173627023069, 16.65560815589396526 ) ) ;
#24800=CARTESIAN_POINT ( 'NONE',  ( 10.00000000000000000, 35.95386929396256903, -10.96151621346501237 ) ) ;
#24806=ORIENTED_EDGE ( 'NONE', *, *, #32980, .T. ) ;
#24813=EDGE_CURVE ( 'NONE', #10410, #9130, #8304, .T. ) ;
#24818=EDGE_CURVE ( 'NONE', #11933, #409, #39588, .T. ) ;
#24820=CIRCLE ( 'NONE', #44358, 16.00000000000000000 ) ;
#24821=FACE_OUTER_BOUND ( 'NONE', #3633, .T. ) ;
#24827=AXIS2_PLACEMENT_3D ( 'NONE', #10468, #47897, #10717 ) ;
#24833=EDGE_CURVE ( 'NONE', #30139, #8790, #32576, .T. ) ;
#24840=DIRECTION ( 'NONE',  ( -1.000000000000000000, 0.000000000000000000, 0.000000000000000000 ) ) ;
#24843=CYLINDRICAL_SURFACE ( 'NONE', #33147, 37.49900000000000233 ) ;
#24868=EDGE_CURVE ( 'NONE', #35718, #37838, #41199, .T. ) ;
#24894=CARTESIAN_POINT ( 'NONE',  ( 0.000000000000000000, -27.05870788708250885, 26.08949754953014022 ) ) ;
#24899=CARTESIAN_POINT ( 'NONE',  ( 0.000000000000000000, -9.188173127307001309, -40.98264845739759465 ) ) ;
#24904=ORIENTED_EDGE ( 'NONE', *, *, #22345, .F. ) ;
#24933=ORIENTED_EDGE ( 'NONE', *, *, #27813, .T. ) ;
#24943=DIRECTION ( 'NONE',  ( 0.000000000000000000, 0.000000000000000000, 1.000000000000000000 ) ) ;
#24951=ORIENTED_EDGE ( 'NONE', *, *, #43851, .T. ) ;
#24952=ORIENTED_EDGE ( 'NONE', *, *, #18669, .T. ) ;
#24954=LINE ( 'NONE', #31608, #44925 ) ;
#24968=CARTESIAN_POINT ( 'NONE',  ( 10.00000000000000000, 36.88895765772642932, -6.736453364083163642 ) ) ;
#24969=ADVANCED_FACE ( 'NONE', ( #23621 ), #12383, .F. ) ;
#24972=ORIENTED_EDGE ( 'NONE', *, *, #20654, .F. ) ;
#24973=EDGE_CURVE ( 'NONE', #3577, #6962, #41757, .T. ) ;
#24985=ORIENTED_EDGE ( 'NONE', *, *, #36454, .F. ) ;
#25003=EDGE_CURVE ( 'NONE', #17728, #42769, #36486, .T. ) ;
#25044=FACE_OUTER_BOUND ( 'NONE', #25326, .T. ) ;
#25061=DIRECTION ( 'NONE',  ( -1.000000000000000000, 0.000000000000000000, 0.000000000000000000 ) ) ;
#25063=ORIENTED_EDGE ( 'NONE', *, *, #27496, .T. ) ;
#25072=DIRECTION ( 'NONE',  ( -1.000000000000000000, -0.000000000000000000, 0.000000000000000000 ) ) ;
#25080=CARTESIAN_POINT ( 'NONE',  ( 10.00000000000000000, -37.01155633439053361, -6.555932627142825986 ) ) ;
#25084=CARTESIAN_POINT ( 'NONE',  ( 10.00000000000000000, 16.23288003029497162, 33.80338159004289622 ) ) ;
#25085=DIRECTION ( 'NONE',  ( 0.000000000000000000, 0.000000000000000000, 1.000000000000000000 ) ) ;
#25095=CIRCLE ( 'NONE', #1659, 42.00000000000000000 ) ;
#25113=DIRECTION ( 'NONE',  ( -1.000000000000000000, 0.000000000000000000, 0.000000000000000000 ) ) ;
#25121=EDGE_LOOP ( 'NONE', ( #48199, #20144, #46008, #43271 ) ) ;
#25144=CYLINDRICAL_SURFACE ( 'NONE', #11475, 37.49900000000000233 ) ;
#25154=VECTOR ( 'NONE', #40032, 1000.000000000000000 ) ;
#25193=AXIS2_PLACEMENT_3D ( 'NONE', #33509, #7081, #11733 ) ;
#25203=ORIENTED_EDGE ( 'NONE', *, *, #20389, .F. ) ;
#25206=LINE ( 'NONE', #43827, #44855 ) ;
#25207=ORIENTED_EDGE ( 'NONE', *, *, #27163, .F. ) ;
#25217=ORIENTED_EDGE ( 'NONE', *, *, #9125, .F. ) ;
#25219=AXIS2_PLACEMENT_3D ( 'NONE', #815, #15757, #45610 ) ;
#25234=DIRECTION ( 'NONE',  ( 0.000000000000000000, 0.000000000000000000, 1.000000000000000000 ) ) ;
#25246=ORIENTED_EDGE ( 'NONE', *, *, #11785, .T. ) ;
#25254=LINE ( 'NONE', #14511, #42001 ) ;
#25257=AXIS2_PLACEMENT_3D ( 'NONE', #2153, #39839, #43742 ) ;
#25259=DIRECTION ( 'NONE',  ( 0.000000000000000000, 0.000000000000000000, 1.000000000000000000 ) ) ;
#25262=DIRECTION ( 'NONE',  ( 0.000000000000000000, -0.4539904997395352027, -0.8910065241883737830 ) ) ;
#25266=DIRECTION ( 'NONE',  ( -1.000000000000000000, -0.000000000000000000, 0.000000000000000000 ) ) ;
#25273=CIRCLE ( 'NONE', #21368, 15.99999999999999822 ) ;
#25276=ADVANCED_FACE ( 'NONE', ( #29472 ), #25547, .T. ) ;
#25281=CIRCLE ( 'NONE', #1040, 42.00000000000000000 ) ;
#25284=DIRECTION ( 'NONE',  ( -1.000000000000000000, 0.000000000000000000, -0.000000000000000000 ) ) ;
#25293=EDGE_CURVE ( 'NONE', #6451, #46491, #5266, .T. ) ;
#25302=VERTEX_POINT ( 'NONE', #17726 ) ;
#25316=CARTESIAN_POINT ( 'NONE',  ( 0.000000000000000000, -21.32104025579135964, 30.84782396557210760 ) ) ;
#25326=EDGE_LOOP ( 'NONE', ( #30620, #33352, #10665, #31162 ) ) ;
#25334=EDGE_CURVE ( 'NONE', #25666, #3261, #33384, .T. ) ;
#25335=CIRCLE ( 'NONE', #47221, 37.49900000000000944 ) ;
#25336=AXIS2_PLACEMENT_3D ( 'NONE', #23775, #27953, #42871 ) ;
#25338=CIRCLE ( 'NONE', #6589, 16.00000000000000000 ) ;
#25339=VECTOR ( 'NONE', #34733, 1000.000000000000000 ) ;
#25341=DIRECTION ( 'NONE',  ( 0.000000000000000000, -0.8090169943749403458, -0.5877852522924830181 ) ) ;
#25349=ORIENTED_EDGE ( 'NONE', *, *, #23974, .T. ) ;
#25351=EDGE_LOOP ( 'NONE', ( #21254, #46851, #36333, #16377 ) ) ;
#25371=DIRECTION ( 'NONE',  ( -1.000000000000000000, 0.000000000000000000, 0.000000000000000000 ) ) ;
#25373=CARTESIAN_POINT ( 'NONE',  ( 10.00000000000000000, -37.48860685352291711, 0.8828120875899322373 ) ) ;
#25376=CARTESIAN_POINT ( 'NONE',  ( 10.00000000000000000, -41.81611651403864727, 3.925862922256025289 ) ) ;
#25382=VECTOR ( 'NONE', #39260, 1000.000000000000000 ) ;
#25385=DIRECTION ( 'NONE',  ( -1.000000000000000000, -0.000000000000000000, -0.000000000000000000 ) ) ;
#25388=FACE_OUTER_BOUND ( 'NONE', #12373, .T. ) ;
#25394=ORIENTED_EDGE ( 'NONE', *, *, #661, .F. ) ;
#25402=ADVANCED_FACE ( 'NONE', ( #8401 ), #19887, .T. ) ;
#25411=AXIS2_PLACEMENT_3D ( 'NONE', #28854, #7306, #21750 ) ;
#25430=DIRECTION ( 'NONE',  ( -1.000000000000000000, -0.000000000000000000, -0.000000000000000000 ) ) ;
#25434=DIRECTION ( 'NONE',  ( 0.000000000000000000, 0.000000000000000000, 1.000000000000000000 ) ) ;
#25442=CIRCLE ( 'NONE', #34077, 16.00000000000000000 ) ;
#25443=CARTESIAN_POINT ( 'NONE',  ( -10.00000000000000000, 0.000000000000000000, 0.000000000000000000 ) ) ;
#25449=CARTESIAN_POINT ( 'NONE',  ( -10.00000000000000000, 0.000000000000000000, 0.000000000000000000 ) ) ;
#25452=VERTEX_POINT ( 'NONE', #37533 ) ;
#25456=ORIENTED_EDGE ( 'NONE', *, *, #33085, .F. ) ;
#25460=ORIENTED_EDGE ( 'NONE', *, *, #28049, .T. ) ;
#25475=CARTESIAN_POINT ( 'NONE',  ( 0.000000000000000000, 0.000000000000000000, 0.000000000000000000 ) ) ;
#25479=AXIS2_PLACEMENT_3D ( 'NONE', #24310, #20886, #39243 ) ;
#25480=DIRECTION ( 'NONE',  ( -1.000000000000000000, 0.000000000000000000, 0.000000000000000000 ) ) ;
#25486=ORIENTED_EDGE ( 'NONE', *, *, #3815, .T. ) ;
#25489=ORIENTED_EDGE ( 'NONE', *, *, #7714, .F. ) ;
#25493=VERTEX_POINT ( 'NONE', #41453 ) ;
#25510=DIRECTION ( 'NONE',  ( -1.000000000000000000, 0.000000000000000000, 0.000000000000000000 ) ) ;
#25520=DIRECTION ( 'NONE',  ( 1.000000000000000000, 0.000000000000000000, 0.000000000000000000 ) ) ;
#25522=EDGE_CURVE ( 'NONE', #36119, #11835, #24798, .T. ) ;
#25543=CARTESIAN_POINT ( 'NONE',  ( 10.00000000000000000, -10.96151621346514382, 35.95386929396252640 ) ) ;
#25547=CYLINDRICAL_SURFACE ( 'NONE', #24035, 16.00000000000000000 ) ;
#25548=VERTEX_POINT ( 'NONE', #5454 ) ;
#25557=DIRECTION ( 'NONE',  ( 0.000000000000000000, -0.5877852522924802425, 0.8090169943749422332 ) ) ;
#25564=EDGE_CURVE ( 'NONE', #35109, #22226, #24820, .T. ) ;
#25567=DIRECTION ( 'NONE',  ( -1.000000000000000000, -0.000000000000000000, -0.000000000000000000 ) ) ;
#25569=ORIENTED_EDGE ( 'NONE', *, *, #6196, .T. ) ;
#25587=VERTEX_POINT ( 'NONE', #35307 ) ;
#25595=CARTESIAN_POINT ( 'NONE',  ( 0.000000000000000000, 0.000000000000000000, 0.000000000000000000 ) ) ;
#25599=FACE_OUTER_BOUND ( 'NONE', #5481, .T. ) ;
#25615=CARTESIAN_POINT ( 'NONE',  ( 0.000000000000000000, -32.34446384429989507, 26.79245525562703278 ) ) ;
#25618=ADVANCED_FACE ( 'NONE', ( #24784 ), #16716, .T. ) ;
#25623=CARTESIAN_POINT ( 'NONE',  ( 10.00000000000000000, -37.58145647212455032, 16.68533520207890319 ) ) ;
#25628=CARTESIAN_POINT ( 'NONE',  ( 0.000000000000000000, -26.79245525562738095, 32.34446384429961796 ) ) ;
#25632=DIRECTION ( 'NONE',  ( 0.000000000000000000, -0.7071067811865389130, -0.7071067811865561215 ) ) ;
#25645=ORIENTED_EDGE ( 'NONE', *, *, #44315, .F. ) ;
#25658=CIRCLE ( 'NONE', #6159, 15.99999999999999822 ) ;
#25666=VERTEX_POINT ( 'NONE', #47525 ) ;
#25674=EDGE_CURVE ( 'NONE', #38938, #44456, #3458, .T. ) ;
#25690=UNCERTAINTY_MEASURE_WITH_UNIT (LENGTH_MEASURE( 1.000000000000000082E-05 ), #19970, 'distance_accuracy_value', 'NONE');
#25693=ORIENTED_EDGE ( 'NONE', *, *, #44712, .F. ) ;
#25697=LINE ( 'NONE', #40174, #33513 ) ;
#25710=AXIS2_PLACEMENT_3D ( 'NONE', #30784, #37881, #670 ) ;
#25742=DIRECTION ( 'NONE',  ( -1.000000000000000000, -0.000000000000000000, 0.000000000000000000 ) ) ;
#25752=VERTEX_POINT ( 'NONE', #39956 ) ;
#25763=CIRCLE ( 'NONE', #18708, 42.00000000000000000 ) ;
#25772=DIRECTION ( 'NONE',  ( 0.000000000000000000, 0.000000000000000000, -1.000000000000000000 ) ) ;
#25773=CARTESIAN_POINT ( 'NONE',  ( 0.000000000000000000, 27.13269053701132094, -25.88420570971372570 ) ) ;
#25798=AXIS2_PLACEMENT_3D ( 'NONE', #28914, #47746, #22051 ) ;
#25802=FACE_OUTER_BOUND ( 'NONE', #3570, .T. ) ;
#25806=DIRECTION ( 'NONE',  ( 0.000000000000000000, -0.9876883405951361050, -0.1564344650402419989 ) ) ;
#25808=CARTESIAN_POINT ( 'NONE',  ( 10.00000000000000000, 0.000000000000000000, 0.000000000000000000 ) ) ;
#25810=DIRECTION ( 'NONE',  ( 0.000000000000000000, 0.000000000000000000, 1.000000000000000000 ) ) ;
#25812=ORIENTED_EDGE ( 'NONE', *, *, #5035, .T. ) ;
#25825=CIRCLE ( 'NONE', #45372, 16.00000000000000000 ) ;
#25827=CARTESIAN_POINT ( 'NONE',  ( 0.000000000000000000, 0.000000000000000000, 0.000000000000000000 ) ) ;
#25830=ORIENTED_EDGE ( 'NONE', *, *, #26470, .F. ) ;
#25831=ORIENTED_EDGE ( 'NONE', *, *, #30969, .T. ) ;
#25839=CARTESIAN_POINT ( 'NONE',  ( 0.000000000000000000, -30.80686688396994910, -21.53537804866113703 ) ) ;
#25840=ORIENTED_EDGE ( 'NONE', *, *, #4943, .T. ) ;
#25844=DIRECTION ( 'NONE',  ( 0.000000000000000000, 0.3090169943749412340, 0.9510565162951556406 ) ) ;
#25845=CYLINDRICAL_SURFACE ( 'NONE', #27653, 16.00000000000000000 ) ;
#25848=DIRECTION ( 'NONE',  ( 0.000000000000000000, 0.4539904997395477482, -0.8910065241883673437 ) ) ;
#25862=FACE_OUTER_BOUND ( 'NONE', #24237, .T. ) ;
#25865=VERTEX_POINT ( 'NONE', #45803 ) ;
#25866=DIRECTION ( 'NONE',  ( -1.000000000000000000, -0.000000000000000000, 0.000000000000000000 ) ) ;
#25879=EDGE_LOOP ( 'NONE', ( #27842, #36323, #10341, #45719 ) ) ;
#25886=AXIS2_PLACEMENT_3D ( 'NONE', #25543, #3028, #21149 ) ;
#25893=EDGE_CURVE ( 'NONE', #7880, #20655, #41256, .T. ) ;
#25904=EDGE_CURVE ( 'NONE', #11527, #26816, #8573, .T. ) ;
#25913=ORIENTED_EDGE ( 'NONE', *, *, #42441, .F. ) ;
#25921=CARTESIAN_POINT ( 'NONE',  ( 0.000000000000000000, 2.446882695291915554E-15, 2.500000000000016431 ) ) ;
#25969=DIRECTION ( 'NONE',  ( 1.000000000000000000, -0.000000000000000000, 0.000000000000000000 ) ) ;
#25975=CARTESIAN_POINT ( 'NONE',  ( 0.000000000000000000, -22.74946021919153694, 29.81001611431000597 ) ) ;
#25985=CARTESIAN_POINT ( 'NONE',  ( 10.00000000000000000, 33.00180498840072829, -17.80606268964504935 ) ) ;
#25987=DIRECTION ( 'NONE',  ( 0.000000000000000000, 0.000000000000000000, 1.000000000000000000 ) ) ;
#26003=AXIS2_PLACEMENT_3D ( 'NONE', #15620, #921, #22964 ) ;
#26007=CIRCLE ( 'NONE', #43213, 37.49900000000000944 ) ;
#26008=AXIS2_PLACEMENT_3D ( 'NONE', #8656, #359, #23596 ) ;
#26009=ORIENTED_EDGE ( 'NONE', *, *, #41526, .F. ) ;
#26014=LINE ( 'NONE', #40963, #38616 ) ;
#26016=EDGE_CURVE ( 'NONE', #4066, #1962, #46524, .T. ) ;
#26031=DIRECTION ( 'NONE',  ( 0.000000000000000000, -0.1564344650402170744, -0.9876883405951398798 ) ) ;
#26032=ORIENTED_EDGE ( 'NONE', *, *, #32403, .F. ) ;
#26048=EDGE_CURVE ( 'NONE', #15657, #31375, #45201, .T. ) ;
#26050=CIRCLE ( 'NONE', #41674, 15.99999999999999822 ) ;
#26052=ORIENTED_EDGE ( 'NONE', *, *, #5534, .T. ) ;
#26065=CARTESIAN_POINT ( 'NONE',  ( 0.000000000000000000, -2.663952781845850826, -41.91543099594819921 ) ) ;
#26067=AXIS2_PLACEMENT_3D ( 'NONE', #30105, #18096, #41364 ) ;
#26070=AXIS2_PLACEMENT_3D ( 'NONE', #11660, #15092, #8462 ) ;
#26078=DIRECTION ( 'NONE',  ( -1.000000000000000000, 0.000000000000000000, -0.000000000000000000 ) ) ;
#26086=DIRECTION ( 'NONE',  ( -1.000000000000000000, 0.000000000000000000, 0.000000000000000000 ) ) ;
#26089=ORIENTED_EDGE ( 'NONE', *, *, #2144, .T. ) ;
#26103=LINE ( 'NONE', #27556, #10417 ) ;
#26105=AXIS2_PLACEMENT_3D ( 'NONE', #42933, #19011, #33943 ) ;
#26118=DIRECTION ( 'NONE',  ( -1.000000000000000000, 0.000000000000000000, 0.000000000000000000 ) ) ;
#26123=ADVANCED_FACE ( 'NONE', ( #32960 ), #30023, .T. ) ;
#26135=ORIENTED_EDGE ( 'NONE', *, *, #42022, .T. ) ;
#26146=AXIS2_PLACEMENT_3D ( 'NONE', #44441, #26078, #22165 ) ;
#26154=AXIS2_PLACEMENT_3D ( 'NONE', #16432, #9323, #43583 ) ;
#26163=CARTESIAN_POINT ( 'NONE',  ( 0.000000000000000000, 15.48615015657581750, 39.04073710021349797 ) ) ;
#26166=VERTEX_POINT ( 'NONE', #48376 ) ;
#26170=VERTEX_POINT ( 'NONE', #25373 ) ;
#26207=ORIENTED_EDGE ( 'NONE', *, *, #3128, .F. ) ;
#26210=EDGE_CURVE ( 'NONE', #28599, #17728, #15848, .T. ) ;
#26223=CARTESIAN_POINT ( 'NONE',  ( 10.00000000000000000, 41.81611651403861885, 3.925862922256313503 ) ) ;
#26230=ORIENTED_EDGE ( 'NONE', *, *, #42708, .F. ) ;
#26242=AXIS2_PLACEMENT_3D ( 'NONE', #6356, #3640, #13933 ) ;
#26247=DIRECTION ( 'NONE',  ( -1.000000000000000000, 0.000000000000000000, 0.000000000000000000 ) ) ;
#26266=DIRECTION ( 'NONE',  ( 0.000000000000000000, 6.938893903907228378E-16, 1.000000000000000000 ) ) ;
#26291=DIRECTION ( 'NONE',  ( 0.000000000000000000, -0.8090169943749403458, -0.5877852522924830181 ) ) ;
#26294=DIRECTION ( 'NONE',  ( -1.000000000000000000, -0.000000000000000000, -0.000000000000000000 ) ) ;
#26296=CARTESIAN_POINT ( 'NONE',  ( 10.00000000000000000, -35.53030884539094103, 12.26510123303246935 ) ) ;
#26304=DIRECTION ( 'NONE',  ( 0.000000000000000000, 0.000000000000000000, 1.000000000000000000 ) ) ;
#26308=CYLINDRICAL_SURFACE ( 'NONE', #24388, 42.00000000000000000 ) ;
#26320=EDGE_CURVE ( 'NONE', #12477, #41267, #26007, .T. ) ;
#26329=EDGE_CURVE ( 'NONE', #34476, #36248, #34893, .T. ) ;
#26331=CARTESIAN_POINT ( 'NONE',  ( 10.00000000000000000, 0.000000000000000000, 0.000000000000000000 ) ) ;
#26338=VERTEX_POINT ( 'NONE', #7973 ) ;
#26349=DIRECTION ( 'NONE',  ( 0.000000000000000000, 0.000000000000000000, 1.000000000000000000 ) ) ;
#26369=ADVANCED_FACE ( 'NONE', ( #2099 ), #24843, .T. ) ;
#26371=DIRECTION ( 'NONE',  ( 0.000000000000000000, 0.000000000000000000, 1.000000000000000000 ) ) ;
#26380=SURFACE_SIDE_STYLE ('',( #45699 ) ) ;
#26395=VERTEX_POINT ( 'NONE', #36097 ) ;
#26399=EDGE_CURVE ( 'NONE', #29561, #42467, #12068, .T. ) ;
#26405=ORIENTED_EDGE ( 'NONE', *, *, #38248, .F. ) ;
#26414=LINE ( 'NONE', #33733, #39196 ) ;
#26417=EDGE_CURVE ( 'NONE', #27310, #21510, #46886, .T. ) ;
#26418=DIRECTION ( 'NONE',  ( -1.000000000000000000, -0.000000000000000000, 0.000000000000000000 ) ) ;
#26421=DIRECTION ( 'NONE',  ( -1.000000000000000000, 0.000000000000000000, 0.000000000000000000 ) ) ;
#26446=ORIENTED_EDGE ( 'NONE', *, *, #6239, .F. ) ;
#26452=( GEOMETRIC_REPRESENTATION_CONTEXT ( 3 ) GLOBAL_UNCERTAINTY_ASSIGNED_CONTEXT ( ( #47719 ) ) GLOBAL_UNIT_ASSIGNED_CONTEXT ( ( #4820, #34663, #37628 ) ) REPRESENTATION_CONTEXT ( 'NONE', 'WORKASPACE' ) );
#26455=ORIENTED_EDGE ( 'NONE', *, *, #9596, .F. ) ;
#26459=CARTESIAN_POINT ( 'NONE',  ( 0.000000000000000000, -41.91543099594816368, -2.663952781846588014 ) ) ;
#26460=DIRECTION ( 'NONE',  ( -1.000000000000000000, -0.000000000000000000, -0.000000000000000000 ) ) ;
#26462=CARTESIAN_POINT ( 'NONE',  ( 10.00000000000000000, -4.992566952385247170, 37.16516213103275845 ) ) ;
#26463=CARTESIAN_POINT ( 'NONE',  ( 10.00000000000000000, -30.84782396557233142, 21.32104025579104345 ) ) ;
#26470=EDGE_CURVE ( 'NONE', #36854, #17158, #39055, .T. ) ;
#26481=CARTESIAN_POINT ( 'NONE',  ( 10.00000000000000000, -30.80686688396994910, -21.53537804866113703 ) ) ;
#26495=VERTEX_POINT ( 'NONE', #17242 ) ;
#26504=CIRCLE ( 'NONE', #22583, 42.00000000000000000 ) ;
#26517=ADVANCED_FACE ( 'NONE', ( #44894 ), #18209, .T. ) ;
#26528=CARTESIAN_POINT ( 'NONE',  ( 10.00000000000000000, 27.13269053701132094, -25.88420570971372570 ) ) ;
#26537=EDGE_CURVE ( 'NONE', #48195, #17387, #41746, .T. ) ;
#26543=DIRECTION ( 'NONE',  ( -1.000000000000000000, 0.000000000000000000, -0.000000000000000000 ) ) ;
#26546=AXIS2_PLACEMENT_3D ( 'NONE', #28302, #10419, #25341 ) ;
#26568=EDGE_CURVE ( 'NONE', #1420, #27090, #26050, .T. ) ;
#26569=ORIENTED_EDGE ( 'NONE', *, *, #3709, .T. ) ;
#26590=DIRECTION ( 'NONE',  ( 0.000000000000000000, 1.000000000000000000, 3.491481338843133750E-15 ) ) ;
#26611=CARTESIAN_POINT ( 'NONE',  ( 0.000000000000000000, 0.000000000000000000, 0.000000000000000000 ) ) ;
#26618=AXIS2_PLACEMENT_3D ( 'NONE', #27436, #20552, #5166 ) ;
#26632=AXIS2_PLACEMENT_3D ( 'NONE', #16009, #45873, #42182 ) ;
#26636=FACE_OUTER_BOUND ( 'NONE', #46225, .T. ) ;
#26639=VERTEX_POINT ( 'NONE', #42181 ) ;
#26647=ORIENTED_EDGE ( 'NONE', *, *, #8016, .T. ) ;
#26654=ORIENTED_EDGE ( 'NONE', *, *, #44273, .T. ) ;
#26658=DIRECTION ( 'NONE',  ( 0.000000000000000000, 0.000000000000000000, 1.000000000000000000 ) ) ;
#26660=FACE_OUTER_BOUND ( 'NONE', #7076, .T. ) ;
#26662=ORIENTED_EDGE ( 'NONE', *, *, #34309, .F. ) ;
#26663=CARTESIAN_POINT ( 'NONE',  ( 0.000000000000000000, -10.96151621346514382, 35.95386929396252640 ) ) ;
#26683=AXIS2_PLACEMENT_3D ( 'NONE', #33985, #4135, #7568 ) ;
#26687=EDGE_CURVE ( 'NONE', #15060, #34442, #8412, .T. ) ;
#26692=AXIS2_PLACEMENT_3D ( 'NONE', #11326, #38662, #41188 ) ;
#26693=DIRECTION ( 'NONE',  ( 0.000000000000000000, -1.776356839400250465E-15, -1.000000000000000000 ) ) ;
#26695=ORIENTED_EDGE ( 'NONE', *, *, #23214, .F. ) ;
#26703=DIRECTION ( 'NONE',  ( 0.000000000000000000, 0.000000000000000000, 1.000000000000000000 ) ) ;
#26704=ORIENTED_EDGE ( 'NONE', *, *, #46092, .F. ) ;
#26706=CARTESIAN_POINT ( 'NONE',  ( 4.999999999999999112, 36.13751322684449008, -21.40280677340332716 ) ) ;
#26711=ORIENTED_EDGE ( 'NONE', *, *, #44315, .T. ) ;
#26712=ORIENTED_EDGE ( 'NONE', *, *, #42968, .F. ) ;
#26725=DIRECTION ( 'NONE',  ( -1.000000000000000000, -0.000000000000000000, 0.000000000000000000 ) ) ;
#26744=CYLINDRICAL_SURFACE ( 'NONE', #14343, 16.00000000000000000 ) ;
#26754=ADVANCED_FACE ( 'NONE', ( #26770 ), #34336, .T. ) ;
#26756=CYLINDRICAL_SURFACE ( 'NONE', #14410, 37.49900000000000233 ) ;
#26770=FACE_OUTER_BOUND ( 'NONE', #2876, .T. ) ;
#26777=CYLINDRICAL_SURFACE ( 'NONE', #33380, 42.00000000000000000 ) ;
#26778=DIRECTION ( 'NONE',  ( -1.000000000000000000, 0.000000000000000000, 0.000000000000000000 ) ) ;
#26784=DIRECTION ( 'NONE',  ( -1.000000000000000000, -0.000000000000000000, 0.000000000000000000 ) ) ;
#26799=VERTEX_POINT ( 'NONE', #31679 ) ;
#26808=VERTEX_POINT ( 'NONE', #24076 ) ;
#26816=VERTEX_POINT ( 'NONE', #2268 ) ;
#26827=DIRECTION ( 'NONE',  ( -1.000000000000000000, -0.000000000000000000, 0.000000000000000000 ) ) ;
#26830=CARTESIAN_POINT ( 'NONE',  ( 10.00000000000000000, -36.88895765772628010, -6.736453364083947015 ) ) ;
#26832=ORIENTED_EDGE ( 'NONE', *, *, #23197, .F. ) ;
#26835=ORIENTED_EDGE ( 'NONE', *, *, #35476, .F. ) ;
#26838=DIRECTION ( 'NONE',  ( 0.000000000000000000, 0.4539904997395479702, -0.8910065241883673437 ) ) ;
#26882=VERTEX_POINT ( 'NONE', #27759 ) ;
#26883=FACE_OUTER_BOUND ( 'NONE', #10962, .T. ) ;
#26893=VERTEX_POINT ( 'NONE', #32837 ) ;
#26895=CARTESIAN_POINT ( 'NONE',  ( 5.000000000000000000, 2.663952781846149254, 41.91543099594818500 ) ) ;
#26899=AXIS2_PLACEMENT_3D ( 'NONE', #13237, #28871, #32779 ) ;
#26904=DIRECTION ( 'NONE',  ( 0.000000000000000000, -0.9876883405951361050, -0.1564344650402419989 ) ) ;
#26919=VERTEX_POINT ( 'NONE', #22332 ) ;
#26927=DIRECTION ( 'NONE',  ( 0.000000000000000000, 0.3090169943749412340, 0.9510565162951556406 ) ) ;
#26929=ORIENTED_EDGE ( 'NONE', *, *, #3310, .T. ) ;
#26939=VERTEX_POINT ( 'NONE', #18642 ) ;
#26947=LINE ( 'NONE', #42346, #18431 ) ;
#26973=ORIENTED_EDGE ( 'NONE', *, *, #34688, .T. ) ;
#26998=CARTESIAN_POINT ( 'NONE',  ( 10.00000000000000000, -33.80338159004273280, -16.23288003029533044 ) ) ;
#27003=CARTESIAN_POINT ( 'NONE',  ( 0.000000000000000000, 39.04073710021344112, 15.48615015657596672 ) ) ;
#27004=CARTESIAN_POINT ( 'NONE',  ( 10.00000000000000000, 0.000000000000000000, 0.000000000000000000 ) ) ;
#27011=LINE ( 'NONE', #42165, #13647 ) ;
#27020=ORIENTED_EDGE ( 'NONE', *, *, #5539, .F. ) ;
#27048=ADVANCED_FACE ( 'NONE', ( #4920 ), #27207, .T. ) ;
#27056=CYLINDRICAL_SURFACE ( 'NONE', #16402, 42.00000000000000000 ) ;
#27061=CARTESIAN_POINT ( 'NONE',  ( 0.000000000000000000, 40.98264845739749518, 9.188173127307448951 ) ) ;
#27064=CARTESIAN_POINT ( 'NONE',  ( 0.000000000000000000, 0.6853352020795618893, -37.58145647212453611 ) ) ;
#27071=AXIS2_PLACEMENT_3D ( 'NONE', #22957, #38876, #23436 ) ;
#27073=VERTEX_POINT ( 'NONE', #33802 ) ;
#27074=DIRECTION ( 'NONE',  ( -1.000000000000000000, 0.000000000000000000, -0.000000000000000000 ) ) ;
#27076=CARTESIAN_POINT ( 'NONE',  ( 10.00000000000000000, 0.000000000000000000, 0.000000000000000000 ) ) ;
#27078=VECTOR ( 'NONE', #28467, 1000.000000000000000 ) ;
#27090=VERTEX_POINT ( 'NONE', #34286 ) ;
#27091=AXIS2_PLACEMENT_3D ( 'NONE', #29490, #33405, #35443 ) ;
#27099=EDGE_CURVE ( 'NONE', #23605, #19451, #21036, .T. ) ;
#27104=CARTESIAN_POINT ( 'NONE',  ( 10.00000000000000000, 40.98264845739749518, 9.188173127307441845 ) ) ;
#27109=( NAMED_UNIT ( * ) SI_UNIT ( $, .STERADIAN. ) SOLID_ANGLE_UNIT ( ) );
#27127=CIRCLE ( 'NONE', #9159, 16.00000000000000000 ) ;
#27131=CYLINDRICAL_SURFACE ( 'NONE', #19262, 42.00000000000000000 ) ;
#27134=DIRECTION ( 'NONE',  ( -1.000000000000000000, -0.000000000000000000, 0.000000000000000000 ) ) ;
#27139=DIRECTION ( 'NONE',  ( 0.000000000000000000, 0.000000000000000000, -1.000000000000000000 ) ) ;
#27148=CYLINDRICAL_SURFACE ( 'NONE', #30679, 16.00000000000000000 ) ;
#27149=ORIENTED_EDGE ( 'NONE', *, *, #43713, .F. ) ;
#27150=CARTESIAN_POINT ( 'NONE',  ( 4.999999999999999112, -41.91543099594819921, 2.663952781846001816 ) ) ;
#27151=LINE ( 'NONE', #37918, #17707 ) ;
#27155=ADVANCED_FACE ( 'NONE', ( #34054 ), #23515, .T. ) ;
#27163=EDGE_CURVE ( 'NONE', #35465, #34102, #19361, .T. ) ;
#27185=CARTESIAN_POINT ( 'NONE',  ( 10.00000000000000000, -17.67226234102801286, -33.17418723428327354 ) ) ;
#27195=LINE ( 'NONE', #30871, #44611 ) ;
#27207=CYLINDRICAL_SURFACE ( 'NONE', #12464, 37.49900000000000233 ) ;
#27211=DIRECTION ( 'NONE',  ( 0.000000000000000000, 0.000000000000000000, -1.000000000000000000 ) ) ;
#27212=VECTOR ( 'NONE', #5641, 1000.000000000000000 ) ;
#27226=ORIENTED_EDGE ( 'NONE', *, *, #12601, .F. ) ;
#27237=LINE ( 'NONE', #42159, #46177 ) ;
#27271=CYLINDRICAL_SURFACE ( 'NONE', #428, 16.00000000000000000 ) ;
#27277=ORIENTED_EDGE ( 'NONE', *, *, #2764, .T. ) ;
#27310=VERTEX_POINT ( 'NONE', #17617 ) ;
#27318=DIRECTION ( 'NONE',  ( 0.000000000000000000, 0.000000000000000000, -1.000000000000000000 ) ) ;
#27338=ORIENTED_EDGE ( 'NONE', *, *, #36184, .T. ) ;
#27344=ORIENTED_EDGE ( 'NONE', *, *, #36184, .F. ) ;
#27351=ADVANCED_FACE ( 'NONE', ( #2680 ), #44051, .T. ) ;
#27361=ORIENTED_EDGE ( 'NONE', *, *, #20055, .F. ) ;
#27373=LINE ( 'NONE', #24412, #21310 ) ;
#27378=CARTESIAN_POINT ( 'NONE',  ( 5.000000000000000000, 41.91543099594818500, -2.663952781846291362 ) ) ;
#27381=CARTESIAN_POINT ( 'NONE',  ( 10.00000000000000000, 0.000000000000000000, 0.000000000000000000 ) ) ;
#27386=CARTESIAN_POINT ( 'NONE',  ( 0.000000000000000000, 12.26510123303259725, 35.53030884539089840 ) ) ;
#27388=VERTEX_POINT ( 'NONE', #40864 ) ;
#27389=CARTESIAN_POINT ( 'NONE',  ( 10.00000000000000000, 0.000000000000000000, 0.000000000000000000 ) ) ;
#27395=CARTESIAN_POINT ( 'NONE',  ( 0.000000000000000000, 27.05870788708267582, -26.08949754952995903 ) ) ;
#27401=ORIENTED_EDGE ( 'NONE', *, *, #6410, .F. ) ;
#27406=ORIENTED_EDGE ( 'NONE', *, *, #40729, .T. ) ;
#27407=CARTESIAN_POINT ( 'NONE',  ( 0.000000000000000000, 37.58145647212453611, 0.6853352020791767529 ) ) ;
#27415=CIRCLE ( 'NONE', #5500, 16.00000000000000000 ) ;
#27418=ORIENTED_EDGE ( 'NONE', *, *, #26399, .F. ) ;
#27419=ORIENTED_EDGE ( 'NONE', *, *, #4442, .T. ) ;
#27422=EDGE_CURVE ( 'NONE', #3261, #8389, #40635, .T. ) ;
#27424=DIRECTION ( 'NONE',  ( 0.000000000000000000, -0.5877852522924802425, 0.8090169943749422332 ) ) ;
#27428=DIRECTION ( 'NONE',  ( 0.000000000000000000, -0.5877852522924624790, -0.8090169943749553338 ) ) ;
#27436=CARTESIAN_POINT ( 'NONE',  ( 0.000000000000000000, -33.17418723428294669, -17.67226234102862747 ) ) ;
#27439=DIRECTION ( 'NONE',  ( 0.000000000000000000, 0.000000000000000000, 1.000000000000000000 ) ) ;
#27440=ORIENTED_EDGE ( 'NONE', *, *, #3488, .T. ) ;
#27441=ORIENTED_EDGE ( 'NONE', *, *, #46245, .F. ) ;
#27461=AXIS2_PLACEMENT_3D ( 'NONE', #33009, #47937, #40604 ) ;
#27467=DIRECTION ( 'NONE',  ( -1.000000000000000000, 0.000000000000000000, 0.000000000000000000 ) ) ;
#27472=PRODUCT_CONTEXT ( 'NONE', #47580, 'mechanical' ) ;
#27476=CARTESIAN_POINT ( 'NONE',  ( 10.00000000000000000, 0.6853352020790449695, 37.58145647212454321 ) ) ;
#27483=AXIS2_PLACEMENT_3D ( 'NONE', #19946, #34880, #46149 ) ;
#27489=ORIENTED_EDGE ( 'NONE', *, *, #15325, .F. ) ;
#27492=AXIS2_PLACEMENT_3D ( 'NONE', #32724, #6544, #43031 ) ;
#27496=EDGE_CURVE ( 'NONE', #26808, #8338, #213, .T. ) ;
#27504=CARTESIAN_POINT ( 'NONE',  ( 10.00000000000000000, 0.000000000000000000, 0.000000000000000000 ) ) ;
#27509=DIRECTION ( 'NONE',  ( -1.000000000000000000, 0.000000000000000000, -0.000000000000000000 ) ) ;
#27514=DIRECTION ( 'NONE',  ( -1.000000000000000000, -0.000000000000000000, 0.000000000000000000 ) ) ;
#27517=AXIS2_PLACEMENT_3D ( 'NONE', #5653, #29314, #9315 ) ;
#27520=CARTESIAN_POINT ( 'NONE',  ( 10.00000000000000000, 17.67226234102874116, -33.17418723428288274 ) ) ;
#27538=DIRECTION ( 'NONE',  ( 0.000000000000000000, 0.000000000000000000, 1.000000000000000000 ) ) ;
#27540=DIRECTION ( 'NONE',  ( -1.000000000000000000, 0.000000000000000000, -0.000000000000000000 ) ) ;
#27544=EDGE_CURVE ( 'NONE', #22817, #46629, #30098, .T. ) ;
#27556=CARTESIAN_POINT ( 'NONE',  ( 4.999999999999999112, 40.98264845739749518, 9.188173127307448951 ) ) ;
#27561=EDGE_CURVE ( 'NONE', #21422, #1742, #17951, .T. ) ;
#27588=CARTESIAN_POINT ( 'NONE',  ( 10.00000000000000000, -10.74501242461258244, -35.92658777277521409 ) ) ;
#27598=CARTESIAN_POINT ( 'NONE',  ( 10.00000000000000000, 16.23288003029543347, -33.80338159004267595 ) ) ;
#27605=ORIENTED_EDGE ( 'NONE', *, *, #20229, .F. ) ;
#27609=DIRECTION ( 'NONE',  ( 0.000000000000000000, -0.4539904997395351471, -0.8910065241883737830 ) ) ;
#27620=ORIENTED_EDGE ( 'NONE', *, *, #28693, .F. ) ;
#27625=DIRECTION ( 'NONE',  ( 1.000000000000000000, 0.000000000000000000, 0.000000000000000000 ) ) ;
#27626=DIRECTION ( 'NONE',  ( 0.000000000000000000, 0.3090169943749482839, -0.9510565162951533091 ) ) ;
#27627=DIRECTION ( 'NONE',  ( 0.000000000000000000, -0.9510565162951500895, -0.3090169943749581649 ) ) ;
#27629=ORIENTED_EDGE ( 'NONE', *, *, #7345, .F. ) ;
#27632=AXIS2_PLACEMENT_3D ( 'NONE', #32411, #47337, #17210 ) ;
#27635=CARTESIAN_POINT ( 'NONE',  ( 10.00000000000000000, 37.22597642581158084, -5.202137450156524068 ) ) ;
#27643=DIRECTION ( 'NONE',  ( -1.000000000000000000, -0.000000000000000000, -0.000000000000000000 ) ) ;
#27645=ADVANCED_FACE ( 'NONE', ( #29520 ), #29754, .F. ) ;
#27646=CARTESIAN_POINT ( 'NONE',  ( 10.00000000000000000, 0.000000000000000000, 0.000000000000000000 ) ) ;
#27653=AXIS2_PLACEMENT_3D ( 'NONE', #43980, #14621, #40075 ) ;
#27664=ORIENTED_EDGE ( 'NONE', *, *, #44818, .F. ) ;
#27668=DIRECTION ( 'NONE',  ( 0.000000000000000000, 0.000000000000000000, 1.000000000000000000 ) ) ;
#27692=EDGE_LOOP ( 'NONE', ( #20059, #21846, #14719, #7849 ) ) ;
#27693=CIRCLE ( 'NONE', #13600, 16.00000000000000355 ) ;
#27694=DIRECTION ( 'NONE',  ( 0.000000000000000000, -0.4539904997395351471, -0.8910065241883737830 ) ) ;
#27696=DIRECTION ( 'NONE',  ( 1.000000000000000000, 0.000000000000000000, 0.000000000000000000 ) ) ;
#27703=EDGE_CURVE ( 'NONE', #12027, #12600, #40679, .T. ) ;
#27704=DIRECTION ( 'NONE',  ( -1.000000000000000000, -0.000000000000000000, -0.000000000000000000 ) ) ;
#27725=CARTESIAN_POINT ( 'NONE',  ( 0.000000000000000000, -37.58145647212455032, 0.6853352020789044152 ) ) ;
#27726=DIRECTION ( 'NONE',  ( -1.000000000000000000, 0.000000000000000000, -0.000000000000000000 ) ) ;
#27727=EDGE_LOOP ( 'NONE', ( #19811, #46391, #16362, #43021 ) ) ;
#27731=VERTEX_POINT ( 'NONE', #29282 ) ;
#27736=EDGE_CURVE ( 'NONE', #9130, #14954, #2375, .T. ) ;
#27740=CIRCLE ( 'NONE', #29307, 37.49900000000000944 ) ;
#27741=CIRCLE ( 'NONE', #5870, 42.00000000000000000 ) ;
#27743=DIRECTION ( 'NONE',  ( 1.000000000000000000, 0.000000000000000000, 0.000000000000000000 ) ) ;
#27745=VERTEX_POINT ( 'NONE', #15073 ) ;
#27752=AXIS2_PLACEMENT_3D ( 'NONE', #46823, #5958, #2260 ) ;
#27759=CARTESIAN_POINT ( 'NONE',  ( 0.000000000000000000, 30.84782396557217865, 21.32104025579125306 ) ) ;
#27761=CARTESIAN_POINT ( 'NONE',  ( 5.000000000000000000, 15.48615015657637706, -39.04073710021327770 ) ) ;
#27763=DIRECTION ( 'NONE',  ( 1.000000000000000000, 0.000000000000000000, 0.000000000000000000 ) ) ;
#27773=ORIENTED_EDGE ( 'NONE', *, *, #5709, .T. ) ;
#27783=ORIENTED_EDGE ( 'NONE', *, *, #9893, .F. ) ;
#27786=AXIS2_PLACEMENT_3D ( 'NONE', #24800, #32390, #40457 ) ;
#27791=ORIENTED_EDGE ( 'NONE', *, *, #23541, .T. ) ;
#27795=ORIENTED_EDGE ( 'NONE', *, *, #13114, .T. ) ;
#27812=CARTESIAN_POINT ( 'NONE',  ( 10.00000000000000000, -33.79645857604525361, 16.45098606841114730 ) ) ;
#27813=EDGE_CURVE ( 'NONE', #13396, #6444, #28822, .T. ) ;
#27814=CARTESIAN_POINT ( 'NONE',  ( 10.00000000000000000, 0.000000000000000000, 0.000000000000000000 ) ) ;
#27840=AXIS2_PLACEMENT_3D ( 'NONE', #8184, #4033, #33635 ) ;
#27842=ORIENTED_EDGE ( 'NONE', *, *, #20053, .T. ) ;
#27849=( GEOMETRIC_REPRESENTATION_CONTEXT ( 3 ) GLOBAL_UNCERTAINTY_ASSIGNED_CONTEXT ( ( #25690 ) ) GLOBAL_UNIT_ASSIGNED_CONTEXT ( ( #19970, #35135, #8703 ) ) REPRESENTATION_CONTEXT ( 'NONE', 'WORKASPACE' ) );
#27850=EDGE_LOOP ( 'NONE', ( #37333, #45411, #32524, #40943 ) ) ;
#27890=ORIENTED_EDGE ( 'NONE', *, *, #17936, .T. ) ;
#27924=ADVANCED_FACE ( 'NONE', ( #12610 ), #39535, .T. ) ;
#27930=ORIENTED_EDGE ( 'NONE', *, *, #33154, .T. ) ;
#27933=CARTESIAN_POINT ( 'NONE',  ( 10.00000000000000000, -36.13751322684434797, 21.40280677340358295 ) ) ;
#27934=DIRECTION ( 'NONE',  ( 0.000000000000000000, -6.982962677686267499E-15, 1.000000000000000000 ) ) ;
#27938=EDGE_CURVE ( 'NONE', #25666, #13717, #13332, .T. ) ;
#27953=DIRECTION ( 'NONE',  ( -1.000000000000000000, 0.000000000000000000, -0.000000000000000000 ) ) ;
#27955=DIRECTION ( 'NONE',  ( -1.000000000000000000, 0.000000000000000000, 0.000000000000000000 ) ) ;
#27968=CARTESIAN_POINT ( 'NONE',  ( 10.00000000000000000, 21.53537804866081373, 30.80686688397018358 ) ) ;
#27974=DIRECTION ( 'NONE',  ( 0.000000000000000000, 0.1564344650402243742, 0.9876883405951387696 ) ) ;
#28001=LINE ( 'NONE', #2057, #13436 ) ;
#28008=LINE ( 'NONE', #39510, #9718 ) ;
#28021=ADVANCED_FACE ( 'NONE', ( #9173 ), #16767, .T. ) ;
#28032=DIRECTION ( 'NONE',  ( 0.000000000000000000, 0.9876883405951381034, -0.1564344650402276216 ) ) ;
#28039=ORIENTED_EDGE ( 'NONE', *, *, #17894, .F. ) ;
#28042=CARTESIAN_POINT ( 'NONE',  ( 10.00000000000000000, 0.000000000000000000, 0.000000000000000000 ) ) ;
#28048=CARTESIAN_POINT ( 'NONE',  ( 10.00000000000000000, 0.000000000000000000, 0.000000000000000000 ) ) ;
#28049=EDGE_CURVE ( 'NONE', #13273, #8092, #4024, .T. ) ;
#28060=DIRECTION ( 'NONE',  ( 0.000000000000000000, 0.000000000000000000, 1.000000000000000000 ) ) ;
#28067=ORIENTED_EDGE ( 'NONE', *, *, #42753, .T. ) ;
#28072=CARTESIAN_POINT ( 'NONE',  ( 10.00000000000000000, -33.80338159004273280, -16.23288003029533044 ) ) ;
#28077=ORIENTED_EDGE ( 'NONE', *, *, #39812, .F. ) ;
#28086=ORIENTED_EDGE ( 'NONE', *, *, #17385, .F. ) ;
#28089=VERTEX_POINT ( 'NONE', #11124 ) ;
#28091=ORIENTED_EDGE ( 'NONE', *, *, #9893, .T. ) ;
#28098=LINE ( 'NONE', #42304, #47729 ) ;
#28118=ORIENTED_EDGE ( 'NONE', *, *, #42623, .T. ) ;
#28144=LINE ( 'NONE', #1242, #44729 ) ;
#28152=ORIENTED_EDGE ( 'NONE', *, *, #20324, .T. ) ;
#28165=CARTESIAN_POINT ( 'NONE',  ( 10.00000000000000000, 37.58145647212453611, 0.6853352020791767529 ) ) ;
#28167=DIRECTION ( 'NONE',  ( -1.000000000000000000, 0.000000000000000000, 0.000000000000000000 ) ) ;
#28176=DIRECTION ( 'NONE',  ( -1.000000000000000000, 0.000000000000000000, -0.000000000000000000 ) ) ;
#28185=EDGE_CURVE ( 'NONE', #13632, #9450, #12559, .T. ) ;
#28186=DIRECTION ( 'NONE',  ( -1.000000000000000000, -0.000000000000000000, -0.000000000000000000 ) ) ;
#28190=DIRECTION ( 'NONE',  ( 0.000000000000000000, 0.9876883405951382144, -0.1564344650402276493 ) ) ;
#28197=ORIENTED_EDGE ( 'NONE', *, *, #38354, .F. ) ;
#28205=AXIS2_PLACEMENT_3D ( 'NONE', #47867, #39828, #36615 ) ;
#28208=ORIENTED_EDGE ( 'NONE', *, *, #45424, .F. ) ;
#28212=DIRECTION ( 'NONE',  ( 0.000000000000000000, 0.000000000000000000, 1.000000000000000000 ) ) ;
#28221=LINE ( 'NONE', #27761, #16616 ) ;
#28231=ORIENTED_EDGE ( 'NONE', *, *, #25893, .F. ) ;
#28256=ORIENTED_EDGE ( 'NONE', *, *, #40977, .T. ) ;
#28260=DIRECTION ( 'NONE',  ( 0.000000000000000000, 0.1564344650402311743, -0.9876883405951377704 ) ) ;
#28262=EDGE_LOOP ( 'NONE', ( #33735, #23813, #615, #32586 ) ) ;
#28265=VERTEX_POINT ( 'NONE', #45611 ) ;
#28268=LINE ( 'NONE', #9420, #24266 ) ;
#28279=FILL_AREA_STYLE_COLOUR ( '', #6729 ) ;
#28290=DIRECTION ( 'NONE',  ( 0.000000000000000000, 0.000000000000000000, 1.000000000000000000 ) ) ;
#28295=EDGE_CURVE ( 'NONE', #38611, #25752, #47717, .T. ) ;
#28297=VERTEX_POINT ( 'NONE', #21604 ) ;
#28300=ORIENTED_EDGE ( 'NONE', *, *, #45691, .T. ) ;
#28302=CARTESIAN_POINT ( 'NONE',  ( 10.00000000000000000, 6.555932627142952995, -37.01155633439051940 ) ) ;
#28328=CYLINDRICAL_SURFACE ( 'NONE', #38394, 16.00000000000000355 ) ;
#28329=DIRECTION ( 'NONE',  ( -1.000000000000000000, -0.000000000000000000, 0.000000000000000000 ) ) ;
#28346=DIRECTION ( 'NONE',  ( 0.000000000000000000, 0.3090169943749482839, -0.9510565162951533091 ) ) ;
#28349=VECTOR ( 'NONE', #20984, 1000.000000000000000 ) ;
#28352=CIRCLE ( 'NONE', #43964, 16.00000000000000000 ) ;
#28363=EDGE_CURVE ( 'NONE', #27745, #42340, #13392, .T. ) ;
#28365=DIRECTION ( 'NONE',  ( 0.000000000000000000, 0.000000000000000000, 1.000000000000000000 ) ) ;
#28369=AXIS2_PLACEMENT_3D ( 'NONE', #46543, #42380, #8589 ) ;
#28378=AXIS2_PLACEMENT_3D ( 'NONE', #4326, #637, #26349 ) ;
#28388=EDGE_LOOP ( 'NONE', ( #47526, #7903, #47217, #46820 ) ) ;
#28392=VECTOR ( 'NONE', #26266, 1000.000000000000000 ) ;
#28395=DIRECTION ( 'NONE',  ( -1.000000000000000000, 0.000000000000000000, 0.000000000000000000 ) ) ;
#28401=CARTESIAN_POINT ( 'NONE',  ( 4.999999999999999112, 9.188173127307898369, -40.98264845739739570 ) ) ;
#28412=CIRCLE ( 'NONE', #7295, 37.49900000000000233 ) ;
#28418=CIRCLE ( 'NONE', #15907, 42.00000000000000000 ) ;
#28426=CIRCLE ( 'NONE', #24513, 42.00000000000000000 ) ;
#28428=DIRECTION ( 'NONE',  ( -1.000000000000000000, 0.000000000000000000, 0.000000000000000000 ) ) ;
#28429=DIRECTION ( 'NONE',  ( 0.000000000000000000, 0.000000000000000000, 1.000000000000000000 ) ) ;
#28432=AXIS2_PLACEMENT_3D ( 'NONE', #27725, #42157, #9111 ) ;
#28445=AXIS2_PLACEMENT_3D ( 'NONE', #46099, #42421, #8885 ) ;
#28467=DIRECTION ( 'NONE',  ( -1.000000000000000000, 0.000000000000000000, 0.000000000000000000 ) ) ;
#28470=CIRCLE ( 'NONE', #17518, 42.00000000000000000 ) ;
#28476=DIRECTION ( 'NONE',  ( -1.000000000000000000, 0.000000000000000000, 0.000000000000000000 ) ) ;
#28477=CIRCLE ( 'NONE', #4265, 42.00000000000000000 ) ;
#28490=AXIS2_PLACEMENT_3D ( 'NONE', #18638, #11784, #33568 ) ;
#28514=CARTESIAN_POINT ( 'NONE',  ( 10.00000000000000000, -12.26510123303284594, 35.53030884539080603 ) ) ;
#28521=CARTESIAN_POINT ( 'NONE',  ( 10.00000000000000000, 41.91543099594818500, -2.663952781846293139 ) ) ;
#28532=ORIENTED_EDGE ( 'NONE', *, *, #11115, .F. ) ;
#28536=CARTESIAN_POINT ( 'NONE',  ( 10.00000000000000000, 0.000000000000000000, 0.000000000000000000 ) ) ;
#28544=CARTESIAN_POINT ( 'NONE',  ( 10.00000000000000000, 0.000000000000000000, 0.000000000000000000 ) ) ;
#28570=AXIS2_PLACEMENT_3D ( 'NONE', #43852, #13997, #25234 ) ;
#28571=ORIENTED_EDGE ( 'NONE', *, *, #28295, .T. ) ;
#28587=DIRECTION ( 'NONE',  ( -1.000000000000000000, -0.000000000000000000, 0.000000000000000000 ) ) ;
#28590=EDGE_CURVE ( 'NONE', #18006, #6864, #17286, .T. ) ;
#28592=CARTESIAN_POINT ( 'NONE',  ( 0.000000000000000000, -25.88420570971419821, 27.13269053701087330 ) ) ;
#28598=VECTOR ( 'NONE', #41247, 1000.000000000000000 ) ;
#28599=VERTEX_POINT ( 'NONE', #19362 ) ;
#28601=DIRECTION ( 'NONE',  ( 0.000000000000000000, 0.000000000000000000, 1.000000000000000000 ) ) ;
#28605=LINE ( 'NONE', #31816, #33938 ) ;
#28611=CIRCLE ( 'NONE', #2810, 16.00000000000000355 ) ;
#28616=EDGE_CURVE ( 'NONE', #8291, #451, #3996, .T. ) ;
#28625=AXIS2_PLACEMENT_3D ( 'NONE', #3903, #37674, #18815 ) ;
#28632=DIRECTION ( 'NONE',  ( -1.000000000000000000, 0.000000000000000000, -0.000000000000000000 ) ) ;
#28635=CARTESIAN_POINT ( 'NONE',  ( 10.00000000000000000, -6.736453364083817341, 36.88895765772630142 ) ) ;
#28648=CYLINDRICAL_SURFACE ( 'NONE', #24307, 16.00000000000000000 ) ;
#28677=CYLINDRICAL_SURFACE ( 'NONE', #30778, 16.00000000000000000 ) ;
#28681=DIRECTION ( 'NONE',  ( -1.000000000000000000, 0.000000000000000000, -0.000000000000000000 ) ) ;
#28686=DIRECTION ( 'NONE',  ( -1.000000000000000000, 0.000000000000000000, 0.000000000000000000 ) ) ;
#28690=VERTEX_POINT ( 'NONE', #12287 ) ;
#28693=EDGE_CURVE ( 'NONE', #45549, #42124, #5564, .T. ) ;
#28708=DIRECTION ( 'NONE',  ( 0.000000000000000000, -0.1564344650402172410, -0.9876883405951399908 ) ) ;
#28716=CARTESIAN_POINT ( 'NONE',  ( 10.00000000000000000, 33.79645857604513992, 16.45098606841138178 ) ) ;
#28727=CARTESIAN_POINT ( 'NONE',  ( 0.000000000000000000, 40.68715046381927891, 10.41901085202092858 ) ) ;
#28730=CIRCLE ( 'NONE', #7620, 12.50000000000000000 ) ;
#28737=ADVANCED_FACE ( 'NONE', ( #25862 ), #18034, .T. ) ;
#28740=ADVANCED_FACE ( 'NONE', ( #21481 ), #47893, .T. ) ;
#28741=DIRECTION ( 'NONE',  ( -1.000000000000000000, 0.000000000000000000, -0.000000000000000000 ) ) ;
#28758=DIRECTION ( 'NONE',  ( -1.000000000000000000, -0.000000000000000000, 0.000000000000000000 ) ) ;
#28765=ADVANCED_FACE ( 'NONE', ( #10944 ), #40805, .T. ) ;
#28766=FACE_OUTER_BOUND ( 'NONE', #452, .T. ) ;
#28776=ORIENTED_EDGE ( 'NONE', *, *, #28616, .F. ) ;
#28779=AXIS2_PLACEMENT_3D ( 'NONE', #33437, #37831, #30486 ) ;
#28793=DIRECTION ( 'NONE',  ( 0.000000000000000000, 0.000000000000000000, 1.000000000000000000 ) ) ;
#28795=ORIENTED_EDGE ( 'NONE', *, *, #45820, .F. ) ;
#28796=EDGE_LOOP ( 'NONE', ( #23372, #36026, #18552, #41513 ) ) ;
#28797=DIRECTION ( 'NONE',  ( -1.000000000000000000, -0.000000000000000000, -0.000000000000000000 ) ) ;
#28799=ORIENTED_EDGE ( 'NONE', *, *, #44864, .T. ) ;
#28802=EDGE_LOOP ( 'NONE', ( #23073, #26009, #8101, #38993 ) ) ;
#28803=DIRECTION ( 'NONE',  ( 0.000000000000000000, 0.000000000000000000, -1.000000000000000000 ) ) ;
#28819=DIRECTION ( 'NONE',  ( -1.000000000000000000, 0.000000000000000000, 0.000000000000000000 ) ) ;
#28822=CIRCLE ( 'NONE', #8623, 16.00000000000000000 ) ;
#28842=ADVANCED_FACE ( 'NONE', ( #19252 ), #11190, .T. ) ;
#28847=ORIENTED_EDGE ( 'NONE', *, *, #11908, .T. ) ;
#28849=CYLINDRICAL_SURFACE ( 'NONE', #43862, 16.00000000000000000 ) ;
#28854=CARTESIAN_POINT ( 'NONE',  ( 10.00000000000000000, 30.80686688397010542, 21.53537804866092387 ) ) ;
#28871=DIRECTION ( 'NONE',  ( -1.000000000000000000, 0.000000000000000000, 0.000000000000000000 ) ) ;
#28875=CARTESIAN_POINT ( 'NONE',  ( 0.000000000000000000, -31.52238457039619490, 27.75498641678731104 ) ) ;
#28886=VERTEX_POINT ( 'NONE', #414 ) ;
#28888=EDGE_CURVE ( 'NONE', #45584, #34499, #7525, .T. ) ;
#28906=ORIENTED_EDGE ( 'NONE', *, *, #11233, .T. ) ;
#28914=CARTESIAN_POINT ( 'NONE',  ( 10.00000000000000000, -0.6853352020793173072, 37.58145647212453611 ) ) ;
#28921=DIRECTION ( 'NONE',  ( 0.000000000000000000, 0.000000000000000000, 1.000000000000000000 ) ) ;
#28930=CARTESIAN_POINT ( 'NONE',  ( 10.00000000000000000, -12.26510123303234501, -35.53030884539098366 ) ) ;
#28935=CARTESIAN_POINT ( 'NONE',  ( 0.000000000000000000, -22.74946021919110706, -29.81001611431033282 ) ) ;
#28941=EDGE_LOOP ( 'NONE', ( #429, #24951, #11822, #38086 ) ) ;
#28949=ORIENTED_EDGE ( 'NONE', *, *, #25003, .F. ) ;
#28963=AXIS2_PLACEMENT_3D ( 'NONE', #31718, #22387, #33156 ) ;
#28969=AXIS2_PLACEMENT_3D ( 'NONE', #31837, #20066, #27424 ) ;
#28972=ORIENTED_EDGE ( 'NONE', *, *, #19715, .T. ) ;
#28997=DIRECTION ( 'NONE',  ( 0.000000000000000000, -0.8910065241883627918, -0.4539904997395568520 ) ) ;
#29004=CIRCLE ( 'NONE', #41531, 16.00000000000000000 ) ;
#29007=DIRECTION ( 'NONE',  ( -1.000000000000000000, -0.000000000000000000, -0.000000000000000000 ) ) ;
#29011=AXIS2_PLACEMENT_3D ( 'NONE', #1981, #39893, #17605 ) ;
#29018=EDGE_CURVE ( 'NONE', #13986, #5941, #42982, .T. ) ;
#29054=ADVANCED_FACE ( 'NONE', ( #5057 ), #19973, .T. ) ;
#29057=AXIS2_PLACEMENT_3D ( 'NONE', #30138, #33777, #23266 ) ;
#29084=ORIENTED_EDGE ( 'NONE', *, *, #45666, .F. ) ;
#29088=CARTESIAN_POINT ( 'NONE',  ( 0.000000000000000000, -26.08949754953044220, 27.05870788708222818 ) ) ;
#29102=EDGE_CURVE ( 'NONE', #27731, #20060, #18927, .T. ) ;
#29104=CARTESIAN_POINT ( 'NONE',  ( 0.000000000000000000, 0.000000000000000000, 0.000000000000000000 ) ) ;
#29107=ORIENTED_EDGE ( 'NONE', *, *, #35159, .F. ) ;
#29117=CIRCLE ( 'NONE', #37725, 37.49900000000000944 ) ;
#29121=CARTESIAN_POINT ( 'NONE',  ( 10.00000000000000000, 35.38097989696528600, -12.42422080174602605 ) ) ;
#29139=EDGE_LOOP ( 'NONE', ( #25812, #26032, #40802, #11864 ) ) ;
#29150=VERTEX_POINT ( 'NONE', #9928 ) ;
#29155=DIRECTION ( 'NONE',  ( -1.000000000000000000, 0.000000000000000000, 0.000000000000000000 ) ) ;
#29167=EDGE_LOOP ( 'NONE', ( #43711, #34157, #30279, #25207 ) ) ;
#29172=EDGE_CURVE ( 'NONE', #31993, #2457, #7959, .T. ) ;
#29181=CIRCLE ( 'NONE', #36955, 37.49900000000000233 ) ;
#29188=DIRECTION ( 'NONE',  ( 0.000000000000000000, -0.3090169943749349057, -0.9510565162951577500 ) ) ;
#29197=CIRCLE ( 'NONE', #46392, 42.00000000000000000 ) ;
#29209=VECTOR ( 'NONE', #21123, 1000.000000000000000 ) ;
#29213=CARTESIAN_POINT ( 'NONE',  ( 10.00000000000000000, 0.000000000000000000, 0.000000000000000000 ) ) ;
#29215=AXIS2_PLACEMENT_3D ( 'NONE', #44462, #25371, #33447 ) ;
#29221=EDGE_CURVE ( 'NONE', #19386, #15851, #9675, .T. ) ;
#29268=VECTOR ( 'NONE', #26118, 1000.000000000000000 ) ;
#29280=ADVANCED_FACE ( 'NONE', ( #11388 ), #26308, .T. ) ;
#29282=CARTESIAN_POINT ( 'NONE',  ( 10.00000000000000000, 26.79245525562714647, 32.34446384429980981 ) ) ;
#29286=DIRECTION ( 'NONE',  ( 0.000000000000000000, 0.000000000000000000, 1.000000000000000000 ) ) ;
#29297=CARTESIAN_POINT ( 'NONE',  ( 10.00000000000000000, 16.45098606841173705, -33.79645857604496229 ) ) ;
#29301=CARTESIAN_POINT ( 'NONE',  ( 0.000000000000000000, 0.000000000000000000, 0.000000000000000000 ) ) ;
#29302=DIRECTION ( 'NONE',  ( -1.000000000000000000, 0.000000000000000000, -0.000000000000000000 ) ) ;
#29307=AXIS2_PLACEMENT_3D ( 'NONE', #25827, #37341, #37097 ) ;
#29314=DIRECTION ( 'NONE',  ( -1.000000000000000000, 0.000000000000000000, 0.000000000000000000 ) ) ;
#29317=CARTESIAN_POINT ( 'NONE',  ( -10.00000000000000000, 0.000000000000000000, 0.000000000000000000 ) ) ;
#29325=CARTESIAN_POINT ( 'NONE',  ( 10.00000000000000000, 39.04073710021344112, 15.48615015657596317 ) ) ;
#29328=CIRCLE ( 'NONE', #48085, 16.00000000000000000 ) ;
#29330=DIRECTION ( 'NONE',  ( -1.000000000000000000, -0.000000000000000000, 0.000000000000000000 ) ) ;
#29338=AXIS2_PLACEMENT_3D ( 'NONE', #34644, #16070, #23890 ) ;
#29340=CIRCLE ( 'NONE', #3553, 42.00000000000000000 ) ;
#29343=DIRECTION ( 'NONE',  ( -1.000000000000000000, -0.000000000000000000, -0.000000000000000000 ) ) ;
#29382=ORIENTED_EDGE ( 'NONE', *, *, #8449, .F. ) ;
#29392=ORIENTED_EDGE ( 'NONE', *, *, #44818, .T. ) ;
#29409=CIRCLE ( 'NONE', #25479, 12.50000000000000000 ) ;
#29436=DIRECTION ( 'NONE',  ( -1.000000000000000000, 0.000000000000000000, 0.000000000000000000 ) ) ;
#29450=ORIENTED_EDGE ( 'NONE', *, *, #34201, .T. ) ;
#29451=AXIS2_PLACEMENT_3D ( 'NONE', #29597, #18586, #210 ) ;
#29452=ADVANCED_FACE ( 'NONE', ( #8901 ), #46349, .T. ) ;
#29465=ORIENTED_EDGE ( 'NONE', *, *, #37252, .F. ) ;
#29472=FACE_OUTER_BOUND ( 'NONE', #39578, .T. ) ;
#29490=CARTESIAN_POINT ( 'NONE',  ( -10.00000000000000000, 0.000000000000000000, 0.000000000000000000 ) ) ;
#29493=CARTESIAN_POINT ( 'NONE',  ( -10.00000000000000000, 0.000000000000000000, 0.000000000000000000 ) ) ;
#29506=VERTEX_POINT ( 'NONE', #4994 ) ;
#29520=FACE_OUTER_BOUND ( 'NONE', #28796, .T. ) ;
#29526=FACE_OUTER_BOUND ( 'NONE', #41091, .T. ) ;
#29529=ORIENTED_EDGE ( 'NONE', *, *, #38976, .T. ) ;
#29556=EDGE_CURVE ( 'NONE', #34442, #45584, #12726, .T. ) ;
#29557=DIRECTION ( 'NONE',  ( -1.000000000000000000, 0.000000000000000000, 0.000000000000000000 ) ) ;
#29561=VERTEX_POINT ( 'NONE', #6207 ) ;
#29569=ADVANCED_FACE ( 'NONE', ( #10603 ), #6686, .T. ) ;
#29580=EDGE_LOOP ( 'NONE', ( #10366, #42361, #7799, #41501 ) ) ;
#29583=CARTESIAN_POINT ( 'NONE',  ( 10.00000000000000000, 26.08949754953062694, -27.05870788708203989 ) ) ;
#29584=DIRECTION ( 'NONE',  ( 0.000000000000000000, -0.7071067811865389130, -0.7071067811865563435 ) ) ;
#29597=CARTESIAN_POINT ( 'NONE',  ( 10.00000000000000000, 0.000000000000000000, 0.000000000000000000 ) ) ;
#29599=CARTESIAN_POINT ( 'NONE',  ( 0.000000000000000000, 17.80606268964540106, 33.00180498840052934 ) ) ;
#29603=AXIS2_PLACEMENT_3D ( 'NONE', #726, #15660, #958 ) ;
#29637=CIRCLE ( 'NONE', #25710, 37.49900000000000233 ) ;
#29651=ORIENTED_EDGE ( 'NONE', *, *, #42267, .T. ) ;
#29662=CYLINDRICAL_SURFACE ( 'NONE', #10637, 37.49900000000000233 ) ;
#29673=ORIENTED_EDGE ( 'NONE', *, *, #2168, .T. ) ;
#29674=ORIENTED_EDGE ( 'NONE', *, *, #3465, .T. ) ;
#29686=CIRCLE ( 'NONE', #25798, 16.00000000000000000 ) ;
#29704=DIRECTION ( 'NONE',  ( 0.000000000000000000, 0.000000000000000000, 1.000000000000000000 ) ) ;
#29706=ORIENTED_EDGE ( 'NONE', *, *, #27561, .F. ) ;
#29728=DIRECTION ( 'NONE',  ( 0.000000000000000000, 0.000000000000000000, 1.000000000000000000 ) ) ;
#29735=EDGE_CURVE ( 'NONE', #6127, #13396, #36164, .T. ) ;
#29747=AXIS2_PLACEMENT_3D ( 'NONE', #4906, #4670, #34274 ) ;
#29754=CYLINDRICAL_SURFACE ( 'NONE', #39113, 12.50000000000000000 ) ;
#29771=ADVANCED_FACE ( 'NONE', ( #36764 ), #48031, .T. ) ;
#29776=DIRECTION ( 'NONE',  ( -1.000000000000000000, 0.000000000000000000, -0.000000000000000000 ) ) ;
#29782=DIRECTION ( 'NONE',  ( 0.000000000000000000, 0.000000000000000000, 1.000000000000000000 ) ) ;
#29784=DIRECTION ( 'NONE',  ( 0.000000000000000000, 0.8910065241883657894, 0.4539904997395509678 ) ) ;
#29790=AXIS2_PLACEMENT_3D ( 'NONE', #38453, #24486, #25434 ) ;
#29807=CIRCLE ( 'NONE', #8705, 37.49900000000000944 ) ;
#29816=CARTESIAN_POINT ( 'NONE',  ( 10.00000000000000000, 35.47612816024556537, -22.48208911017461631 ) ) ;
#29821=AXIS2_PLACEMENT_3D ( 'NONE', #27185, #8560, #11767 ) ;
#29823=CARTESIAN_POINT ( 'NONE',  ( 10.00000000000000000, 26.79245525562761188, -32.34446384429941901 ) ) ;
#29824=CARTESIAN_POINT ( 'NONE',  ( 0.000000000000000000, -3.925862922256468046, 41.81611651403860463 ) ) ;
#29834=CARTESIAN_POINT ( 'NONE',  ( 0.000000000000000000, -33.17418723428319538, 17.67226234102814431 ) ) ;
#29856=ORIENTED_EDGE ( 'NONE', *, *, #24973, .F. ) ;
#29857=CARTESIAN_POINT ( 'NONE',  ( 10.00000000000000000, 0.000000000000000000, 0.000000000000000000 ) ) ;
#29858=AXIS2_PLACEMENT_3D ( 'NONE', #21029, #10504, #36674 ) ;
#29864=CIRCLE ( 'NONE', #16599, 37.49900000000000233 ) ;
#29868=ORIENTED_EDGE ( 'NONE', *, *, #30359, .T. ) ;
#29874=CARTESIAN_POINT ( 'NONE',  ( 10.00000000000000000, 0.000000000000000000, 0.000000000000000000 ) ) ;
#29878=DIRECTION ( 'NONE',  ( -1.000000000000000000, -0.000000000000000000, 0.000000000000000000 ) ) ;
#29880=ADVANCED_FACE ( 'NONE', ( #4465 ), #1748, .T. ) ;
#29887=VERTEX_POINT ( 'NONE', #38465 ) ;
#29896=CARTESIAN_POINT ( 'NONE',  ( 0.000000000000000000, -27.05870788708213226, -26.08949754953053102 ) ) ;
#29905=CARTESIAN_POINT ( 'NONE',  ( 0.000000000000000000, -37.01155633439053361, -6.555932627142825986 ) ) ;
#29921=DIRECTION ( 'NONE',  ( -1.000000000000000000, 0.000000000000000000, 0.000000000000000000 ) ) ;
#29922=ORIENTED_EDGE ( 'NONE', *, *, #34134, .T. ) ;
#29930=EDGE_LOOP ( 'NONE', ( #13928, #31284, #8366, #4175 ) ) ;
#29956=ORIENTED_EDGE ( 'NONE', *, *, #29172, .F. ) ;
#29957=CARTESIAN_POINT ( 'NONE',  ( 10.00000000000000000, 0.000000000000000000, 0.000000000000000000 ) ) ;
#29958=CIRCLE ( 'NONE', #12010, 16.00000000000000711 ) ;
#29992=VERTEX_POINT ( 'NONE', #47487 ) ;
#29997=CIRCLE ( 'NONE', #34667, 16.00000000000000355 ) ;
#30021=CARTESIAN_POINT ( 'NONE',  ( 0.000000000000000000, 35.38097989696512968, 12.42422080174651100 ) ) ;
#30023=CYLINDRICAL_SURFACE ( 'NONE', #2968, 42.00000000000000000 ) ;
#30025=DIRECTION ( 'NONE',  ( -1.000000000000000000, 0.000000000000000000, 0.000000000000000000 ) ) ;
#30035=DIRECTION ( 'NONE',  ( 1.000000000000000000, 0.000000000000000000, -0.000000000000000000 ) ) ;
#30037=CARTESIAN_POINT ( 'NONE',  ( 10.00000000000000000, 0.000000000000000000, 0.000000000000000000 ) ) ;
#30039=VERTEX_POINT ( 'NONE', #42870 ) ;
#30055=CARTESIAN_POINT ( 'NONE',  ( 0.000000000000000000, 30.84782396557248418, -21.32104025579081252 ) ) ;
#30058=ORIENTED_EDGE ( 'NONE', *, *, #2016, .F. ) ;
#30061=AXIS2_PLACEMENT_3D ( 'NONE', #26331, #374, #18958 ) ;
#30079=AXIS2_PLACEMENT_3D ( 'NONE', #2435, #35976, #13715 ) ;
#30082=LINE ( 'NONE', #44752, #3312 ) ;
#30083=VECTOR ( 'NONE', #44173, 1000.000000000000000 ) ;
#30095=CARTESIAN_POINT ( 'NONE',  ( 10.00000000000000000, 32.34446384429971744, 26.79245525562727082 ) ) ;
#30098=LINE ( 'NONE', #45026, #37504 ) ;
#30103=ORIENTED_EDGE ( 'NONE', *, *, #98, .T. ) ;
#30105=CARTESIAN_POINT ( 'NONE',  ( 0.000000000000000000, 0.000000000000000000, 0.000000000000000000 ) ) ;
#30115=DIRECTION ( 'NONE',  ( -1.000000000000000000, -0.000000000000000000, -0.000000000000000000 ) ) ;
#30130=CYLINDRICAL_SURFACE ( 'NONE', #43316, 16.00000000000000000 ) ;
#30132=EDGE_CURVE ( 'NONE', #17599, #21447, #8031, .T. ) ;
#30135=CARTESIAN_POINT ( 'NONE',  ( 10.00000000000000000, 10.96151621346487914, 35.95386929396260456 ) ) ;
#30138=CARTESIAN_POINT ( 'NONE',  ( 0.000000000000000000, 0.000000000000000000, 0.000000000000000000 ) ) ;
#30139=VERTEX_POINT ( 'NONE', #3907 ) ;
#30147=ADVANCED_FACE ( 'NONE', ( #7817 ), #220, .T. ) ;
#30148=DIRECTION ( 'NONE',  ( 1.000000000000000000, -0.000000000000000000, -0.000000000000000000 ) ) ;
#30150=AXIS2_PLACEMENT_3D ( 'NONE', #4000, #41212, #45583 ) ;
#30152=ORIENTED_EDGE ( 'NONE', *, *, #8392, .T. ) ;
#30167=CARTESIAN_POINT ( 'NONE',  ( 10.00000000000000000, 0.000000000000000000, 0.000000000000000000 ) ) ;
#30170=LINE ( 'NONE', #34060, #39574 ) ;
#30179=DIRECTION ( 'NONE',  ( 1.000000000000000000, -0.000000000000000000, -0.000000000000000000 ) ) ;
#30182=EDGE_CURVE ( 'NONE', #44237, #28297, #25281, .T. ) ;
#30196=CARTESIAN_POINT ( 'NONE',  ( 0.000000000000000000, -5.202137450156655518, 37.22597642581156663 ) ) ;
#30206=EDGE_CURVE ( 'NONE', #3893, #18061, #41688, .T. ) ;
#30207=VECTOR ( 'NONE', #33280, 1000.000000000000000 ) ;
#30213=CARTESIAN_POINT ( 'NONE',  ( 10.00000000000000000, -16.65560815589439159, 38.55633173627004595 ) ) ;
#30214=CARTESIAN_POINT ( 'NONE',  ( 10.00000000000000000, 6.736453364084091788, -36.88895765772625879 ) ) ;
#30215=LINE ( 'NONE', #3768, #11072 ) ;
#30220=DIRECTION ( 'NONE',  ( -1.000000000000000000, -0.000000000000000000, 0.000000000000000000 ) ) ;
#30224=ORIENTED_EDGE ( 'NONE', *, *, #44382, .F. ) ;
#30229=DIRECTION ( 'NONE',  ( -1.000000000000000000, 0.000000000000000000, 0.000000000000000000 ) ) ;
#30231=LINE ( 'NONE', #38055, #34695 ) ;
#30234=ORIENTED_EDGE ( 'NONE', *, *, #9541, .F. ) ;
#30239=EDGE_CURVE ( 'NONE', #38423, #29150, #11739, .T. ) ;
#30244=ORIENTED_EDGE ( 'NONE', *, *, #38976, .F. ) ;
#30258=ORIENTED_EDGE ( 'NONE', *, *, #12143, .F. ) ;
#30279=ORIENTED_EDGE ( 'NONE', *, *, #47591, .T. ) ;
#30301=EDGE_LOOP ( 'NONE', ( #15975, #2063, #1913, #39197 ) ) ;
#30302=ORIENTED_EDGE ( 'NONE', *, *, #1384, .T. ) ;
#30312=ORIENTED_EDGE ( 'NONE', *, *, #3010, .T. ) ;
#30314=CARTESIAN_POINT ( 'NONE',  ( 10.00000000000000000, 2.663952781846733675, -41.91543099594814947 ) ) ;
#30334=ORIENTED_EDGE ( 'NONE', *, *, #20597, .T. ) ;
#30342=DIRECTION ( 'NONE',  ( 0.000000000000000000, -0.7071067811865536790, 0.7071067811865413555 ) ) ;
#30357=EDGE_CURVE ( 'NONE', #15686, #22230, #28412, .T. ) ;
#30359=EDGE_CURVE ( 'NONE', #39281, #46639, #36232, .T. ) ;
#30364=ORIENTED_EDGE ( 'NONE', *, *, #30802, .T. ) ;
#30400=CARTESIAN_POINT ( 'NONE',  ( 10.00000000000000000, 35.53030884539102630, -12.26510123303222599 ) ) ;
#30409=EDGE_CURVE ( 'NONE', #36805, #28599, #13191, .T. ) ;
#30415=ORIENTED_EDGE ( 'NONE', *, *, #4114, .T. ) ;
#30417=SHAPE_DEFINITION_REPRESENTATION ( #35474, #9091 ) ;
#30425=CARTESIAN_POINT ( 'NONE',  ( 0.000000000000000000, -31.52238457039579345, -27.75498641678775158 ) ) ;
#30449=CARTESIAN_POINT ( 'NONE',  ( 5.000000000000000000, -15.48615015657555993, -39.04073710021360455 ) ) ;
#30456=DIRECTION ( 'NONE',  ( -1.000000000000000000, 0.000000000000000000, 0.000000000000000000 ) ) ;
#30468=CYLINDRICAL_SURFACE ( 'NONE', #34860, 16.00000000000000000 ) ;
#30475=DIRECTION ( 'NONE',  ( -1.000000000000000000, -0.000000000000000000, 0.000000000000000000 ) ) ;
#30478=CIRCLE ( 'NONE', #38303, 16.00000000000000355 ) ;
#30486=DIRECTION ( 'NONE',  ( 0.000000000000000000, -0.1564344650402382242, 0.9876883405951366601 ) ) ;
#30499=DIRECTION ( 'NONE',  ( -1.000000000000000000, 0.000000000000000000, 0.000000000000000000 ) ) ;
#30515=EDGE_CURVE ( 'NONE', #45549, #5995, #13599, .T. ) ;
#30519=VERTEX_POINT ( 'NONE', #37145 ) ;
#30537=CARTESIAN_POINT ( 'NONE',  ( 10.00000000000000000, -6.555932627142676772, 37.01155633439056203 ) ) ;
#30542=ORIENTED_EDGE ( 'NONE', *, *, #16317, .T. ) ;
#30544=ORIENTED_EDGE ( 'NONE', *, *, #33102, .F. ) ;
#30556=VERTEX_POINT ( 'NONE', #14875 ) ;
#30562=EDGE_CURVE ( 'NONE', #8858, #13574, #40194, .T. ) ;
#30565=DIRECTION ( 'NONE',  ( -1.000000000000000000, 0.000000000000000000, 0.000000000000000000 ) ) ;
#30568=DIRECTION ( 'NONE',  ( 0.000000000000000000, -0.3090169943749548342, 0.9510565162951511997 ) ) ;
#30574=ORIENTED_EDGE ( 'NONE', *, *, #46085, .T. ) ;
#30579=AXIS2_PLACEMENT_3D ( 'NONE', #30633, #41905, #8357 ) ;
#30584=VECTOR ( 'NONE', #35243, 1000.000000000000000 ) ;
#30590=CIRCLE ( 'NONE', #1668, 16.00000000000000355 ) ;
#30612=DIRECTION ( 'NONE',  ( 0.000000000000000000, 0.000000000000000000, 1.000000000000000000 ) ) ;
#30616=LINE ( 'NONE', #34509, #14903 ) ;
#30620=ORIENTED_EDGE ( 'NONE', *, *, #18720, .T. ) ;
#30625=AXIS2_PLACEMENT_3D ( 'NONE', #516, #26460, #15211 ) ;
#30631=DIRECTION ( 'NONE',  ( 0.000000000000000000, 0.000000000000000000, 1.000000000000000000 ) ) ;
#30633=CARTESIAN_POINT ( 'NONE',  ( 0.000000000000000000, -37.01155633439063308, 6.555932627142289526 ) ) ;
#30647=CARTESIAN_POINT ( 'NONE',  ( 0.000000000000000000, -16.23288003029521320, 33.80338159004277543 ) ) ;
#30652=ORIENTED_EDGE ( 'NONE', *, *, #7714, .T. ) ;
#30658=CIRCLE ( 'NONE', #4077, 16.00000000000000000 ) ;
#30664=EDGE_CURVE ( 'NONE', #43729, #48169, #6573, .T. ) ;
#30672=EDGE_LOOP ( 'NONE', ( #29856, #32948, #5944, #27020 ) ) ;
#30679=AXIS2_PLACEMENT_3D ( 'NONE', #15879, #26418, #37425 ) ;
#30681=ADVANCED_FACE ( 'NONE', ( #5002 ), #16746, .T. ) ;
#30682=DIRECTION ( 'NONE',  ( 0.000000000000000000, 0.000000000000000000, 1.000000000000000000 ) ) ;
#30694=ADVANCED_FACE ( 'NONE', ( #24324 ), #12590, .T. ) ;
#30699=EDGE_LOOP ( 'NONE', ( #15843, #8557, #18141, #5236 ) ) ;
#30700=CARTESIAN_POINT ( 'NONE',  ( 10.00000000000000000, 17.80606268964540462, 33.00180498840053644 ) ) ;
#30725=CIRCLE ( 'NONE', #45566, 37.49900000000000944 ) ;
#30732=ORIENTED_EDGE ( 'NONE', *, *, #77, .F. ) ;
#30763=DIRECTION ( 'NONE',  ( 0.000000000000000000, 0.3090169943749482839, -0.9510565162951533091 ) ) ;
#30766=DIRECTION ( 'NONE',  ( -1.000000000000000000, 0.000000000000000000, 0.000000000000000000 ) ) ;
#30768=CIRCLE ( 'NONE', #19799, 15.99999999999999645 ) ;
#30778=AXIS2_PLACEMENT_3D ( 'NONE', #46563, #10066, #28429 ) ;
#30780=ORIENTED_EDGE ( 'NONE', *, *, #31801, .T. ) ;
#30784=CARTESIAN_POINT ( 'NONE',  ( 0.000000000000000000, 0.000000000000000000, 0.000000000000000000 ) ) ;
#30785=ORIENTED_EDGE ( 'NONE', *, *, #46493, .T. ) ;
#30793=EDGE_CURVE ( 'NONE', #12477, #38938, #9678, .T. ) ;
#30802=EDGE_CURVE ( 'NONE', #38611, #35831, #3238, .T. ) ;
#30804=ORIENTED_EDGE ( 'NONE', *, *, #2764, .F. ) ;
#30817=CARTESIAN_POINT ( 'NONE',  ( 10.00000000000000000, 37.22597642581158084, -5.202137450156524068 ) ) ;
#30822=ORIENTED_EDGE ( 'NONE', *, *, #6626, .T. ) ;
#30832=DIRECTION ( 'NONE',  ( 0.000000000000000000, 0.000000000000000000, -1.000000000000000000 ) ) ;
#30834=EDGE_LOOP ( 'NONE', ( #19873, #736, #19107, #6171 ) ) ;
#30836=CIRCLE ( 'NONE', #19866, 16.00000000000000000 ) ;
#30837=LINE ( 'NONE', #643, #46480 ) ;
#30855=VERTEX_POINT ( 'NONE', #28727 ) ;
#30864=CARTESIAN_POINT ( 'NONE',  ( 10.00000000000000000, -35.47612816024506088, -22.48208911017539435 ) ) ;
#30869=DIRECTION ( 'NONE',  ( -1.000000000000000000, -0.000000000000000000, 0.000000000000000000 ) ) ;
#30871=CARTESIAN_POINT ( 'NONE',  ( 4.999999999999999112, -40.98264845739743123, -9.188173127307734944 ) ) ;
#30876=ORIENTED_EDGE ( 'NONE', *, *, #35259, .F. ) ;
#30878=ORIENTED_EDGE ( 'NONE', *, *, #20434, .F. ) ;
#30899=LINE ( 'NONE', #35272, #17799 ) ;
#30913=EDGE_CURVE ( 'NONE', #22056, #38126, #8793, .T. ) ;
#30914=VECTOR ( 'NONE', #38045, 1000.000000000000000 ) ;
#30917=EDGE_LOOP ( 'NONE', ( #34618, #1512, #45203, #18249 ) ) ;
#30929=ORIENTED_EDGE ( 'NONE', *, *, #12331, .F. ) ;
#30938=VERTEX_POINT ( 'NONE', #552 ) ;
#30942=CARTESIAN_POINT ( 'NONE',  ( 0.000000000000000000, 26.08949754953062694, -27.05870788708203989 ) ) ;
#30943=CIRCLE ( 'NONE', #7483, 15.99999999999999822 ) ;
#30944=FACE_OUTER_BOUND ( 'NONE', #20288, .T. ) ;
#30969=EDGE_CURVE ( 'NONE', #1904, #22493, #11809, .T. ) ;
#30982=DIRECTION ( 'NONE',  ( 1.000000000000000000, 0.000000000000000000, 0.000000000000000000 ) ) ;
#30987=DIRECTION ( 'NONE',  ( 0.000000000000000000, -0.8910065241883626808, -0.4539904997395570740 ) ) ;
#30988=ORIENTED_EDGE ( 'NONE', *, *, #30359, .F. ) ;
#30990=EDGE_LOOP ( 'NONE', ( #11282, #31997, #39944, #5163 ) ) ;
#31003=LINE ( 'NONE', #6017, #33127 ) ;
#31009=CYLINDRICAL_SURFACE ( 'NONE', #39996, 16.00000000000000000 ) ;
#31016=AXIS2_PLACEMENT_3D ( 'NONE', #28165, #24493, #31620 ) ;
#31018=CARTESIAN_POINT ( 'NONE',  ( 0.000000000000000000, 37.48860685352291000, -0.8828120875901940279 ) ) ;
#31019=CIRCLE ( 'NONE', #43515, 42.00000000000000000 ) ;
#31051=EDGE_LOOP ( 'NONE', ( #10258, #26929, #34457, #34814 ) ) ;
#31055=CARTESIAN_POINT ( 'NONE',  ( 10.00000000000000000, 0.000000000000000000, 0.000000000000000000 ) ) ;
#31081=FACE_OUTER_BOUND ( 'NONE', #11091, .T. ) ;
#31110=DIRECTION ( 'NONE',  ( -1.000000000000000000, -0.000000000000000000, -0.000000000000000000 ) ) ;
#31120=DIRECTION ( 'NONE',  ( -1.000000000000000000, -0.000000000000000000, -0.000000000000000000 ) ) ;
#31121=ADVANCED_FACE ( 'NONE', ( #5669 ), #16440, .T. ) ;
#31126=EDGE_CURVE ( 'NONE', #17075, #1904, #22109, .T. ) ;
#31127=DIRECTION ( 'NONE',  ( 0.000000000000000000, 0.8090169943749486725, -0.5877852522924713607 ) ) ;
#31135=DIRECTION ( 'NONE',  ( 0.000000000000000000, 0.000000000000000000, -1.000000000000000000 ) ) ;
#31141=EDGE_LOOP ( 'NONE', ( #18990, #35546, #556, #1170 ) ) ;
#31146=ADVANCED_FACE ( 'NONE', ( #31635 ), #16682, .T. ) ;
#31147=DIRECTION ( 'NONE',  ( -1.000000000000000000, 0.000000000000000000, 0.000000000000000000 ) ) ;
#31155=ORIENTED_EDGE ( 'NONE', *, *, #36824, .T. ) ;
#31162=ORIENTED_EDGE ( 'NONE', *, *, #40768, .T. ) ;
#31168=CARTESIAN_POINT ( 'NONE',  ( 0.000000000000000000, 26.79245525562714292, 32.34446384429980981 ) ) ;
#31182=DIRECTION ( 'NONE',  ( 0.000000000000000000, 0.000000000000000000, 1.000000000000000000 ) ) ;
#31185=ADVANCED_FACE ( 'NONE', ( #21059 ), #10047, .T. ) ;
#31189=CARTESIAN_POINT ( 'NONE',  ( 10.00000000000000000, 0.000000000000000000, 0.000000000000000000 ) ) ;
#31194=EDGE_CURVE ( 'NONE', #18006, #29561, #1282, .T. ) ;
#31200=DIRECTION ( 'NONE',  ( -1.000000000000000000, 0.000000000000000000, -0.000000000000000000 ) ) ;
#31215=CARTESIAN_POINT ( 'NONE',  ( 10.00000000000000000, 30.80686688397041451, -21.53537804866048688 ) ) ;
#31248=AXIS2_PLACEMENT_3D ( 'NONE', #22116, #37297, #21870 ) ;
#31271=CARTESIAN_POINT ( 'NONE',  ( 10.00000000000000000, 0.000000000000000000, 0.000000000000000000 ) ) ;
#31284=ORIENTED_EDGE ( 'NONE', *, *, #45761, .T. ) ;
#31304=LINE ( 'NONE', #27378, #40717 ) ;
#31306=DIRECTION ( 'NONE',  ( 0.000000000000000000, 0.000000000000000000, 1.000000000000000000 ) ) ;
#31310=DIRECTION ( 'NONE',  ( 1.000000000000000000, -0.000000000000000000, -0.000000000000000000 ) ) ;
#31311=CARTESIAN_POINT ( 'NONE',  ( 0.000000000000000000, -37.22597642581161637, 5.202137450156258502 ) ) ;
#31316=VECTOR ( 'NONE', #25072, 1000.000000000000000 ) ;
#31330=EDGE_CURVE ( 'NONE', #43018, #39693, #9561, .T. ) ;
#31333=CIRCLE ( 'NONE', #21134, 37.49900000000000233 ) ;
#31340=ORIENTED_EDGE ( 'NONE', *, *, #45109, .F. ) ;
#31343=ORIENTED_EDGE ( 'NONE', *, *, #21586, .T. ) ;
#31365=DIRECTION ( 'NONE',  ( -1.000000000000000000, -0.000000000000000000, 0.000000000000000000 ) ) ;
#31366=DIRECTION ( 'NONE',  ( -1.000000000000000000, 0.000000000000000000, 0.000000000000000000 ) ) ;
#31368=CARTESIAN_POINT ( 'NONE',  ( 10.00000000000000000, 0.000000000000000000, 0.000000000000000000 ) ) ;
#31371=DIRECTION ( 'NONE',  ( -1.000000000000000000, -0.000000000000000000, -0.000000000000000000 ) ) ;
#31375=VERTEX_POINT ( 'NONE', #37448 ) ;
#31382=ORIENTED_EDGE ( 'NONE', *, *, #34966, .T. ) ;
#31402=AXIS2_PLACEMENT_3D ( 'NONE', #44476, #25385, #47649 ) ;
#31405=CARTESIAN_POINT ( 'NONE',  ( 5.000000000000000000, 16.65560815589464028, -38.55633173626993226 ) ) ;
#31406=ORIENTED_EDGE ( 'NONE', *, *, #25522, .F. ) ;
#31409=CIRCLE ( 'NONE', #43100, 16.00000000000000000 ) ;
#31418=DIRECTION ( 'NONE',  ( -1.000000000000000000, 0.000000000000000000, -0.000000000000000000 ) ) ;
#31427=CARTESIAN_POINT ( 'NONE',  ( -10.00000000000000000, 0.000000000000000000, 0.000000000000000000 ) ) ;
#31457=EDGE_CURVE ( 'NONE', #21073, #26395, #8931, .T. ) ;
#31461=DIRECTION ( 'NONE',  ( -1.000000000000000000, 0.000000000000000000, -0.000000000000000000 ) ) ;
#31467=CYLINDRICAL_SURFACE ( 'NONE', #13742, 42.00000000000000000 ) ;
#31475=VECTOR ( 'NONE', #10020, 1000.000000000000000 ) ;
#31500=ORIENTED_EDGE ( 'NONE', *, *, #2987, .F. ) ;
#31507=ORIENTED_EDGE ( 'NONE', *, *, #31578, .T. ) ;
#31511=CIRCLE ( 'NONE', #37747, 42.00000000000000000 ) ;
#31516=DIRECTION ( 'NONE',  ( -1.000000000000000000, -0.000000000000000000, 0.000000000000000000 ) ) ;
#31517=ADVANCED_FACE ( 'NONE', ( #19319 ), #20045, .T. ) ;
#31530=ORIENTED_EDGE ( 'NONE', *, *, #34918, .F. ) ;
#31533=CARTESIAN_POINT ( 'NONE',  ( 10.00000000000000000, 10.41901085202135668, -40.68715046381917944 ) ) ;
#31546=DIRECTION ( 'NONE',  ( 0.000000000000000000, 0.000000000000000000, 1.000000000000000000 ) ) ;
#31551=AXIS2_PLACEMENT_3D ( 'NONE', #40076, #14368, #6787 ) ;
#31553=DIRECTION ( 'NONE',  ( -1.000000000000000000, -0.000000000000000000, 0.000000000000000000 ) ) ;
#31572=DIRECTION ( 'NONE',  ( 1.000000000000000000, 0.000000000000000000, 0.000000000000000000 ) ) ;
#31575=ORIENTED_EDGE ( 'NONE', *, *, #12459, .T. ) ;
#31578=EDGE_CURVE ( 'NONE', #16794, #23303, #30837, .T. ) ;
#31596=CARTESIAN_POINT ( 'NONE',  ( 0.000000000000000000, 0.000000000000000000, 0.000000000000000000 ) ) ;
#31603=CARTESIAN_POINT ( 'NONE',  ( 10.00000000000000000, 27.75498641678742473, 31.52238457039609898 ) ) ;
#31608=CARTESIAN_POINT ( 'NONE',  ( 10.00000000000000000, 36.88895765772642932, -6.736453364083163642 ) ) ;
#31614=AXIS2_PLACEMENT_3D ( 'NONE', #27520, #35335, #13079 ) ;
#31619=DIRECTION ( 'NONE',  ( -1.000000000000000000, -0.000000000000000000, 0.000000000000000000 ) ) ;
#31620=DIRECTION ( 'NONE',  ( 0.000000000000000000, 0.000000000000000000, 1.000000000000000000 ) ) ;
#31635=FACE_OUTER_BOUND ( 'NONE', #42404, .T. ) ;
#31636=AXIS2_PLACEMENT_3D ( 'NONE', #6336, #44260, #10735 ) ;
#31656=AXIS2_PLACEMENT_3D ( 'NONE', #38788, #31200, #46121 ) ;
#31665=ORIENTED_EDGE ( 'NONE', *, *, #34201, .F. ) ;
#31678=AXIS2_PLACEMENT_3D ( 'NONE', #3043, #43688, #17967 ) ;
#31679=CARTESIAN_POINT ( 'NONE',  ( 10.00000000000000000, 37.58145647212453611, 16.68533520207917675 ) ) ;
#31696=DIRECTION ( 'NONE',  ( 0.000000000000000000, 0.000000000000000000, 1.000000000000000000 ) ) ;
#31702=CIRCLE ( 'NONE', #41060, 16.00000000000000355 ) ;
#31704=CARTESIAN_POINT ( 'NONE',  ( 10.00000000000000000, 10.96151621346487914, 35.95386929396260456 ) ) ;
#31707=ORIENTED_EDGE ( 'NONE', *, *, #27736, .T. ) ;
#31710=CIRCLE ( 'NONE', #37163, 37.49900000000000944 ) ;
#31718=CARTESIAN_POINT ( 'NONE',  ( 10.00000000000000000, 12.26510123303259725, 35.53030884539089840 ) ) ;
#31743=ORIENTED_EDGE ( 'NONE', *, *, #12557, .T. ) ;
#31747=DIRECTION ( 'NONE',  ( 0.000000000000000000, 0.000000000000000000, 1.000000000000000000 ) ) ;
#31771=ORIENTED_EDGE ( 'NONE', *, *, #26417, .T. ) ;
#31784=ORIENTED_EDGE ( 'NONE', *, *, #13372, .F. ) ;
#31787=ORIENTED_EDGE ( 'NONE', *, *, #14648, .F. ) ;
#31788=CARTESIAN_POINT ( 'NONE',  ( 10.00000000000000000, -16.23288003029473359, -33.80338159004301701 ) ) ;
#31801=EDGE_CURVE ( 'NONE', #30039, #8075, #18325, .T. ) ;
#31804=LINE ( 'NONE', #4864, #5079 ) ;
#31805=EDGE_CURVE ( 'NONE', #5554, #8790, #3490, .T. ) ;
#31809=DIRECTION ( 'NONE',  ( -1.000000000000000000, 0.000000000000000000, 0.000000000000000000 ) ) ;
#31816=CARTESIAN_POINT ( 'NONE',  ( 10.00000000000000000, 22.74946021919133088, 29.81001611431016229 ) ) ;
#31823=VERTEX_POINT ( 'NONE', #12395 ) ;
#31826=VECTOR ( 'NONE', #39567, 1000.000000000000000 ) ;
#31827=CARTESIAN_POINT ( 'NONE',  ( -3.308722450212110699E-21, 16.95692799528845640, -2.500000000000000000 ) ) ;
#31837=CARTESIAN_POINT ( 'NONE',  ( 10.00000000000000000, -17.67226234102801286, -33.17418723428327354 ) ) ;
#31842=CIRCLE ( 'NONE', #2885, 37.49900000000000944 ) ;
#31848=DIRECTION ( 'NONE',  ( -1.000000000000000000, 0.000000000000000000, -0.000000000000000000 ) ) ;
#31858=DIRECTION ( 'NONE',  ( -1.000000000000000000, -0.000000000000000000, -0.000000000000000000 ) ) ;
#31859=DIRECTION ( 'NONE',  ( -1.000000000000000000, 0.000000000000000000, 0.000000000000000000 ) ) ;
#31876=ORIENTED_EDGE ( 'NONE', *, *, #20434, .T. ) ;
#31881=CIRCLE ( 'NONE', #10750, 16.00000000000000355 ) ;
#31887=FACE_OUTER_BOUND ( 'NONE', #42639, .T. ) ;
#31888=ORIENTED_EDGE ( 'NONE', *, *, #36579, .F. ) ;
#31899=ADVANCED_FACE ( 'NONE', ( #13845 ), #36342, .T. ) ;
#31907=ORIENTED_EDGE ( 'NONE', *, *, #35204, .F. ) ;
#31908=CARTESIAN_POINT ( 'NONE',  ( 0.000000000000000000, 0.000000000000000000, 0.000000000000000000 ) ) ;
#31926=DIRECTION ( 'NONE',  ( 0.000000000000000000, 0.000000000000000000, -1.000000000000000000 ) ) ;
#31932=AXIS2_PLACEMENT_3D ( 'NONE', #716, #45499, #15651 ) ;
#31944=ADVANCED_FACE ( 'NONE', ( #47116 ), #36580, .T. ) ;
#31945=EDGE_CURVE ( 'NONE', #34492, #648, #42595, .T. ) ;
#31953=EDGE_LOOP ( 'NONE', ( #1313, #17867, #37946, #31575 ) ) ;
#31954=EDGE_CURVE ( 'NONE', #21662, #36119, #5773, .T. ) ;
#31955=ORIENTED_EDGE ( 'NONE', *, *, #15963, .F. ) ;
#31971=DIRECTION ( 'NONE',  ( -1.000000000000000000, -0.000000000000000000, 0.000000000000000000 ) ) ;
#31981=FACE_OUTER_BOUND ( 'NONE', #32710, .T. ) ;
#31993=VERTEX_POINT ( 'NONE', #2326 ) ;
#31995=AXIS2_PLACEMENT_3D ( 'NONE', #12766, #27704, #24031 ) ;
#31997=ORIENTED_EDGE ( 'NONE', *, *, #14247, .T. ) ;
#31999=AXIS2_PLACEMENT_3D ( 'NONE', #45715, #41090, #11942 ) ;
#32012=DIRECTION ( 'NONE',  ( 0.000000000000000000, 0.000000000000000000, 1.000000000000000000 ) ) ;
#32034=LINE ( 'NONE', #32263, #5722 ) ;
#32035=CARTESIAN_POINT ( 'NONE',  ( 10.00000000000000000, -3.925862922255855647, -41.81611651403866858 ) ) ;
#32053=EDGE_CURVE ( 'NONE', #47967, #4600, #34789, .T. ) ;
#32055=ORIENTED_EDGE ( 'NONE', *, *, #28590, .F. ) ;
#32059=ORIENTED_EDGE ( 'NONE', *, *, #35798, .F. ) ;
#32071=CARTESIAN_POINT ( 'NONE',  ( 10.00000000000000000, 5.202137450156389953, 37.22597642581160216 ) ) ;
#32076=CARTESIAN_POINT ( 'NONE',  ( 10.00000000000000000, -22.74946021919110706, -29.81001611431033282 ) ) ;
#32082=DIRECTION ( 'NONE',  ( 0.000000000000000000, -0.7071067811865535679, 0.7071067811865413555 ) ) ;
#32085=FACE_OUTER_BOUND ( 'NONE', #34068, .T. ) ;
#32093=CARTESIAN_POINT ( 'NONE',  ( 0.000000000000000000, 0.000000000000000000, 0.000000000000000000 ) ) ;
#32099=ORIENTED_EDGE ( 'NONE', *, *, #12501, .T. ) ;
#32109=AXIS2_PLACEMENT_3D ( 'NONE', #24300, #16002, #5702 ) ;
#32117=ORIENTED_EDGE ( 'NONE', *, *, #24262, .F. ) ;
#32134=VECTOR ( 'NONE', #17054, 1000.000000000000000 ) ;
#32139=VECTOR ( 'NONE', #7556, 1000.000000000000000 ) ;
#32140=FACE_OUTER_BOUND ( 'NONE', #28388, .T. ) ;
#32146=AXIS2_PLACEMENT_3D ( 'NONE', #2430, #2918, #6600 ) ;
#32151=CIRCLE ( 'NONE', #19609, 16.00000000000000355 ) ;
#32160=ORIENTED_EDGE ( 'NONE', *, *, #4442, .F. ) ;
#32175=EDGE_CURVE ( 'NONE', #1742, #337, #29340, .T. ) ;
#32213=CARTESIAN_POINT ( 'NONE',  ( 0.000000000000000000, 0.000000000000000000, 0.000000000000000000 ) ) ;
#32243=CARTESIAN_POINT ( 'NONE',  ( 0.000000000000000000, 0.000000000000000000, 0.000000000000000000 ) ) ;
#32245=ORIENTED_EDGE ( 'NONE', *, *, #21828, .T. ) ;
#32262=DIRECTION ( 'NONE',  ( 0.000000000000000000, 0.8090169943749487835, -0.5877852522924713607 ) ) ;
#32263=CARTESIAN_POINT ( 'NONE',  ( 5.000000000000000000, -31.52238457039619490, 27.75498641678731104 ) ) ;
#32289=ORIENTED_EDGE ( 'NONE', *, *, #31126, .F. ) ;
#32294=DIRECTION ( 'NONE',  ( 0.000000000000000000, 0.000000000000000000, -1.000000000000000000 ) ) ;
#32297=ORIENTED_EDGE ( 'NONE', *, *, #21833, .T. ) ;
#32300=AXIS2_PLACEMENT_3D ( 'NONE', #18263, #10448, #21466 ) ;
#32303=VECTOR ( 'NONE', #40863, 1000.000000000000000 ) ;
#32312=CARTESIAN_POINT ( 'NONE',  ( 10.00000000000000000, 0.000000000000000000, 0.000000000000000000 ) ) ;
#32313=DIRECTION ( 'NONE',  ( -1.000000000000000000, 0.000000000000000000, -0.000000000000000000 ) ) ;
#32362=VERTEX_POINT ( 'NONE', #30213 ) ;
#32390=DIRECTION ( 'NONE',  ( -1.000000000000000000, 0.000000000000000000, -0.000000000000000000 ) ) ;
#32398=AXIS2_PLACEMENT_3D ( 'NONE', #28048, #1614, #8468 ) ;
#32403=EDGE_CURVE ( 'NONE', #39728, #46150, #39524, .T. ) ;
#32404=CARTESIAN_POINT ( 'NONE',  ( 0.000000000000000000, -22.64427369931148348, -30.00120703465229965 ) ) ;
#32408=VECTOR ( 'NONE', #39427, 1000.000000000000000 ) ;
#32411=CARTESIAN_POINT ( 'NONE',  ( 0.000000000000000000, 0.000000000000000000, 0.000000000000000000 ) ) ;
#32422=VERTEX_POINT ( 'NONE', #26528 ) ;
#32427=CARTESIAN_POINT ( 'NONE',  ( 10.00000000000000000, -6.736453364083817341, 36.88895765772630142 ) ) ;
#32430=ORIENTED_EDGE ( 'NONE', *, *, #33289, .T. ) ;
#32439=DIRECTION ( 'NONE',  ( 0.000000000000000000, 0.000000000000000000, -1.000000000000000000 ) ) ;
#32443=EDGE_CURVE ( 'NONE', #36248, #46672, #41070, .T. ) ;
#32457=CARTESIAN_POINT ( 'NONE',  ( 10.00000000000000000, 0.000000000000000000, 0.000000000000000000 ) ) ;
#32460=CARTESIAN_POINT ( 'NONE',  ( 10.00000000000000000, 12.42422080174688404, -35.38097989696498047 ) ) ;
#32461=CIRCLE ( 'NONE', #12174, 42.00000000000000000 ) ;
#32467=AXIS2_PLACEMENT_3D ( 'NONE', #22271, #36935, #37194 ) ;
#32469=ORIENTED_EDGE ( 'NONE', *, *, #98, .F. ) ;
#32474=ORIENTED_EDGE ( 'NONE', *, *, #45236, .T. ) ;
#32480=VERTEX_POINT ( 'NONE', #32893 ) ;
#32483=ORIENTED_EDGE ( 'NONE', *, *, #33533, .F. ) ;
#32507=CIRCLE ( 'NONE', #47354, 42.00000000000000000 ) ;
#32509=EDGE_CURVE ( 'NONE', #30519, #17771, #35637, .T. ) ;
#32512=AXIS2_PLACEMENT_3D ( 'NONE', #29905, #48023, #40456 ) ;
#32524=ORIENTED_EDGE ( 'NONE', *, *, #12594, .F. ) ;
#32534=ADVANCED_FACE ( 'NONE', ( #40985 ), #7680, .T. ) ;
#32558=FACE_OUTER_BOUND ( 'NONE', #25121, .T. ) ;
#32570=DIRECTION ( 'NONE',  ( -1.000000000000000000, -0.000000000000000000, -0.000000000000000000 ) ) ;
#32576=CIRCLE ( 'NONE', #22416, 16.00000000000000000 ) ;
#32586=ORIENTED_EDGE ( 'NONE', *, *, #21558, .T. ) ;
#32592=EDGE_CURVE ( 'NONE', #26338, #11209, #17628, .T. ) ;
#32602=EDGE_LOOP ( 'NONE', ( #12, #26207, #10929, #5165 ) ) ;
#32616=AXIS2_PLACEMENT_3D ( 'NONE', #802, #23092, #7677 ) ;
#32619=EDGE_CURVE ( 'NONE', #8511, #39399, #5947, .T. ) ;
#32622=AXIS2_PLACEMENT_3D ( 'NONE', #22209, #18285, #7028 ) ;
#32635=LINE ( 'NONE', #24580, #25382 ) ;
#32642=ORIENTED_EDGE ( 'NONE', *, *, #32509, .F. ) ;
#32653=DIRECTION ( 'NONE',  ( -1.000000000000000000, -0.000000000000000000, -0.000000000000000000 ) ) ;
#32662=DIRECTION ( 'NONE',  ( -1.000000000000000000, -0.000000000000000000, -0.000000000000000000 ) ) ;
#32663=CARTESIAN_POINT ( 'NONE',  ( 10.00000000000000000, -33.17418723428319538, 17.67226234102814431 ) ) ;
#32664=DIRECTION ( 'NONE',  ( -1.000000000000000000, 0.000000000000000000, -0.000000000000000000 ) ) ;
#32667=PLANE ( 'NONE',  #7972 ) ;
#32696=CARTESIAN_POINT ( 'NONE',  ( -10.00000000000000000, 0.000000000000000000, 0.000000000000000000 ) ) ;
#32704=LINE ( 'NONE', #39827, #45981 ) ;
#32705=CARTESIAN_POINT ( 'NONE',  ( 0.000000000000000000, 1.530808498934191521E-15, -12.50000000000000000 ) ) ;
#32709=DIRECTION ( 'NONE',  ( 0.000000000000000000, 0.000000000000000000, -1.000000000000000000 ) ) ;
#32710=EDGE_LOOP ( 'NONE', ( #7550, #26712, #36186, #37243 ) ) ;
#32718=EDGE_LOOP ( 'NONE', ( #27361, #43960, #33327, #30152 ) ) ;
#32720=DIRECTION ( 'NONE',  ( 0.000000000000000000, -0.9510565162951565288, 0.3090169943749382364 ) ) ;
#32724=CARTESIAN_POINT ( 'NONE',  ( 0.000000000000000000, 0.000000000000000000, 0.000000000000000000 ) ) ;
#32732=FACE_OUTER_BOUND ( 'NONE', #35998, .T. ) ;
#32742=AXIS2_PLACEMENT_3D ( 'NONE', #33950, #11468, #19266 ) ;
#32750=EDGE_LOOP ( 'NONE', ( #43329, #23872, #37228, #3449 ) ) ;
#32756=CARTESIAN_POINT ( 'NONE',  ( 10.00000000000000000, 0.000000000000000000, 0.000000000000000000 ) ) ;
#32771=CARTESIAN_POINT ( 'NONE',  ( 10.00000000000000000, 0.000000000000000000, 37.49900000000000233 ) ) ;
#32777=EDGE_CURVE ( 'NONE', #15686, #34754, #15349, .T. ) ;
#32779=DIRECTION ( 'NONE',  ( 0.000000000000000000, 0.000000000000000000, 1.000000000000000000 ) ) ;
#32788=CYLINDRICAL_SURFACE ( 'NONE', #2933, 42.00000000000000000 ) ;
#32795=ADVANCED_FACE ( 'NONE', ( #36513 ), #268, .T. ) ;
#32798=VERTEX_POINT ( 'NONE', #21596 ) ;
#32812=LINE ( 'NONE', #2956, #47678 ) ;
#32837=CARTESIAN_POINT ( 'NONE',  ( 10.00000000000000000, 37.22597642581158084, 10.79786254984347593 ) ) ;
#32843=CARTESIAN_POINT ( 'NONE',  ( 10.00000000000000178, 0.000000000000000000, 0.000000000000000000 ) ) ;
#32854=EDGE_CURVE ( 'NONE', #38423, #842, #41822, .T. ) ;
#32857=DIRECTION ( 'NONE',  ( 0.000000000000000000, 0.000000000000000000, 1.000000000000000000 ) ) ;
#32862=DIRECTION ( 'NONE',  ( -1.000000000000000000, 0.000000000000000000, 0.000000000000000000 ) ) ;
#32864=VERTEX_POINT ( 'NONE', #25975 ) ;
#32867=ORIENTED_EDGE ( 'NONE', *, *, #45483, .F. ) ;
#32868=EDGE_CURVE ( 'NONE', #9900, #22230, #33078, .T. ) ;
#32875=FACE_OUTER_BOUND ( 'NONE', #27727, .T. ) ;
#32882=CIRCLE ( 'NONE', #21954, 37.49900000000000233 ) ;
#32893=CARTESIAN_POINT ( 'NONE',  ( 0.000000000000000000, -25.88420570971381807, -27.13269053701123212 ) ) ;
#32900=CARTESIAN_POINT ( 'NONE',  ( 10.00000000000000000, -26.08949754953044220, 27.05870788708222818 ) ) ;
#32934=FACE_OUTER_BOUND ( 'NONE', #21729, .T. ) ;
#32939=ORIENTED_EDGE ( 'NONE', *, *, #7229, .T. ) ;
#32948=ORIENTED_EDGE ( 'NONE', *, *, #12885, .T. ) ;
#32958=AXIS2_PLACEMENT_3D ( 'NONE', #42925, #46838, #16970 ) ;
#32960=FACE_OUTER_BOUND ( 'NONE', #28802, .T. ) ;
#32968=CARTESIAN_POINT ( 'NONE',  ( 0.000000000000000000, 16.65560815589464028, -38.55633173626993226 ) ) ;
#32972=CARTESIAN_POINT ( 'NONE',  ( 10.00000000000000000, 0.000000000000000000, 0.000000000000000000 ) ) ;
#32980=EDGE_CURVE ( 'NONE', #42340, #8001, #23054, .T. ) ;
#32987=ORIENTED_EDGE ( 'NONE', *, *, #31805, .F. ) ;
#32989=DIRECTION ( 'NONE',  ( -1.000000000000000000, -0.000000000000000000, -0.000000000000000000 ) ) ;
#33003=CARTESIAN_POINT ( 'NONE',  ( 10.00000000000000000, -12.42422080174663712, 35.38097989696507994 ) ) ;
#33007=AXIS2_PLACEMENT_3D ( 'NONE', #24316, #1569, #1807 ) ;
#33009=CARTESIAN_POINT ( 'NONE',  ( 10.00000000000000000, 0.000000000000000000, 0.000000000000000000 ) ) ;
#33014=DIRECTION ( 'NONE',  ( 0.000000000000000000, 0.000000000000000000, 1.000000000000000000 ) ) ;
#33015=ORIENTED_EDGE ( 'NONE', *, *, #16396, .F. ) ;
#33037=ORIENTED_EDGE ( 'NONE', *, *, #9495, .T. ) ;
#33048=AXIS2_PLACEMENT_3D ( 'NONE', #22274, #14925, #44779 ) ;
#33052=ORIENTED_EDGE ( 'NONE', *, *, #10176, .T. ) ;
#33055=ORIENTED_EDGE ( 'NONE', *, *, #41029, .F. ) ;
#33064=ORIENTED_EDGE ( 'NONE', *, *, #32854, .T. ) ;
#33065=CARTESIAN_POINT ( 'NONE',  ( 10.00000000000000000, 0.000000000000000000, 0.000000000000000000 ) ) ;
#33071=ADVANCED_FACE ( 'NONE', ( #16658 ), #35501, .T. ) ;
#33078=LINE ( 'NONE', #22323, #20713 ) ;
#33085=EDGE_CURVE ( 'NONE', #35643, #46491, #24954, .T. ) ;
#33091=DIRECTION ( 'NONE',  ( -1.000000000000000000, 0.000000000000000000, 0.000000000000000000 ) ) ;
#33094=AXIS2_PLACEMENT_3D ( 'NONE', #6728, #10392, #21404 ) ;
#33102=EDGE_CURVE ( 'NONE', #21677, #26799, #23824, .T. ) ;
#33125=CARTESIAN_POINT ( 'NONE',  ( 10.00000000000000000, 12.42422080174639021, 35.38097989696516521 ) ) ;
#33127=VECTOR ( 'NONE', #5039, 1000.000000000000000 ) ;
#33128=DIRECTION ( 'NONE',  ( 0.000000000000000000, 0.5877852522924744694, -0.8090169943749465631 ) ) ;
#33131=DIRECTION ( 'NONE',  ( 0.000000000000000000, 0.000000000000000000, 1.000000000000000000 ) ) ;
#33141=CARTESIAN_POINT ( 'NONE',  ( 10.00000000000000000, -37.22597642581153821, -5.202137450156795850 ) ) ;
#33147=AXIS2_PLACEMENT_3D ( 'NONE', #27814, #21161, #16786 ) ;
#33148=ADVANCED_FACE ( 'NONE', ( #2673 ), #13001, .T. ) ;
#33154=EDGE_CURVE ( 'NONE', #32480, #42780, #45734, .T. ) ;
#33156=DIRECTION ( 'NONE',  ( 0.000000000000000000, 0.000000000000000000, 1.000000000000000000 ) ) ;
#33159=VERTEX_POINT ( 'NONE', #20815 ) ;
#33187=DIRECTION ( 'NONE',  ( 0.000000000000000000, 0.000000000000000000, 1.000000000000000000 ) ) ;
#33190=DIRECTION ( 'NONE',  ( 0.000000000000000000, 0.000000000000000000, 1.000000000000000000 ) ) ;
#33191=ORIENTED_EDGE ( 'NONE', *, *, #18313, .T. ) ;
#33204=AXIS2_PLACEMENT_3D ( 'NONE', #45325, #22577, #4698 ) ;
#33236=VERTEX_POINT ( 'NONE', #44044 ) ;
#33242=ORIENTED_EDGE ( 'NONE', *, *, #24833, .F. ) ;
#33259=FACE_OUTER_BOUND ( 'NONE', #25879, .T. ) ;
#33260=LINE ( 'NONE', #43562, #31475 ) ;
#33267=ORIENTED_EDGE ( 'NONE', *, *, #20166, .F. ) ;
#33270=LINE ( 'NONE', #44286, #17384 ) ;
#33278=CARTESIAN_POINT ( 'NONE',  ( 10.00000000000000000, 30.84782396557248418, -21.32104025579081252 ) ) ;
#33280=DIRECTION ( 'NONE',  ( -1.000000000000000000, 0.000000000000000000, -0.000000000000000000 ) ) ;
#33281=CARTESIAN_POINT ( 'NONE',  ( 0.000000000000000000, -40.98264845739755202, 9.188173127307159405 ) ) ;
#33289=EDGE_CURVE ( 'NONE', #30039, #44237, #3652, .T. ) ;
#33312=EDGE_CURVE ( 'NONE', #47328, #41024, #35596, .T. ) ;
#33327=ORIENTED_EDGE ( 'NONE', *, *, #42174, .T. ) ;
#33346=CARTESIAN_POINT ( 'NONE',  ( 0.000000000000000000, 35.53030884539102630, -12.26510123303222599 ) ) ;
#33352=ORIENTED_EDGE ( 'NONE', *, *, #11516, .F. ) ;
#33359=CARTESIAN_POINT ( 'NONE',  ( 10.00000000000000000, 0.000000000000000000, 0.000000000000000000 ) ) ;
#33361=EDGE_CURVE ( 'NONE', #11716, #22548, #32461, .T. ) ;
#33380=AXIS2_PLACEMENT_3D ( 'NONE', #15298, #7926, #26304 ) ;
#33383=DIRECTION ( 'NONE',  ( -1.000000000000000000, 0.000000000000000000, 0.000000000000000000 ) ) ;
#33384=CIRCLE ( 'NONE', #22462, 42.00000000000000000 ) ;
#33386=ORIENTED_EDGE ( 'NONE', *, *, #8668, .F. ) ;
#33390=CARTESIAN_POINT ( 'NONE',  ( 0.000000000000000000, 6.555932627142952995, -37.01155633439051940 ) ) ;
#33402=DIRECTION ( 'NONE',  ( -1.000000000000000000, 0.000000000000000000, 0.000000000000000000 ) ) ;
#33405=DIRECTION ( 'NONE',  ( -1.000000000000000000, -0.000000000000000000, -0.000000000000000000 ) ) ;
#33412=CARTESIAN_POINT ( 'NONE',  ( 10.00000000000000000, 0.000000000000000000, 0.000000000000000000 ) ) ;
#33431=CARTESIAN_POINT ( 'NONE',  ( 50.00005079999999680, 0.000000000000000000, 0.000000000000000000 ) ) ;
#33436=EDGE_CURVE ( 'NONE', #648, #27310, #44964, .T. ) ;
#33437=CARTESIAN_POINT ( 'NONE',  ( 0.000000000000000000, 0.000000000000000000, 0.000000000000000000 ) ) ;
#33439=FACE_OUTER_BOUND ( 'NONE', #19828, .T. ) ;
#33445=DIRECTION ( 'NONE',  ( 0.000000000000000000, 0.000000000000000000, 1.000000000000000000 ) ) ;
#33447=DIRECTION ( 'NONE',  ( 0.000000000000000000, -0.1564344650402382242, 0.9876883405951366601 ) ) ;
#33462=CARTESIAN_POINT ( 'NONE',  ( 0.000000000000000000, -0.6853352020793173072, 37.58145647212453611 ) ) ;
#33464=CARTESIAN_POINT ( 'NONE',  ( 10.00000000000000000, 37.48860685352291000, 0.8828120875901893649 ) ) ;
#33468=DIRECTION ( 'NONE',  ( 0.000000000000000000, 0.000000000000000000, 1.000000000000000000 ) ) ;
#33481=EDGE_LOOP ( 'NONE', ( #21738, #19685, #6857, #47078 ) ) ;
#33486=CARTESIAN_POINT ( 'NONE',  ( 0.000000000000000000, -33.80338159004273280, -16.23288003029533044 ) ) ;
#33492=DIRECTION ( 'NONE',  ( 0.000000000000000000, -0.9510565162951500895, -0.3090169943749583314 ) ) ;
#33496=CIRCLE ( 'NONE', #42884, 15.99999999999999822 ) ;
#33507=CARTESIAN_POINT ( 'NONE',  ( -10.00000000000000000, 0.000000000000000000, 0.000000000000000000 ) ) ;
#33509=CARTESIAN_POINT ( 'NONE',  ( 10.00000000000000000, -37.01155633439063308, 6.555932627142289526 ) ) ;
#33513=VECTOR ( 'NONE', #14465, 1000.000000000000000 ) ;
#33529=ADVANCED_FACE ( 'NONE', ( #28766 ), #14314, .T. ) ;
#33533=EDGE_CURVE ( 'NONE', #15851, #8001, #10617, .T. ) ;
#33539=VERTEX_POINT ( 'NONE', #25316 ) ;
#33543=CARTESIAN_POINT ( 'NONE',  ( 4.999999999999999112, 10.41901085202078292, 40.68715046381932865 ) ) ;
#33566=CARTESIAN_POINT ( 'NONE',  ( 10.00000000000000000, 25.88420570971438650, -27.13269053701069566 ) ) ;
#33568=DIRECTION ( 'NONE',  ( 0.000000000000000000, 0.000000000000000000, 1.000000000000000000 ) ) ;
#33580=CARTESIAN_POINT ( 'NONE',  ( -10.00000000000000000, 0.000000000000000000, 0.000000000000000000 ) ) ;
#33581=FACE_OUTER_BOUND ( 'NONE', #13962, .T. ) ;
#33584=ORIENTED_EDGE ( 'NONE', *, *, #18765, .F. ) ;
#33589=ORIENTED_EDGE ( 'NONE', *, *, #3709, .F. ) ;
#33597=CIRCLE ( 'NONE', #20303, 16.00000000000000000 ) ;
#33619=DIRECTION ( 'NONE',  ( -1.000000000000000000, -0.000000000000000000, -0.000000000000000000 ) ) ;
#33622=CARTESIAN_POINT ( 'NONE',  ( 10.00000000000000000, 30.84782396557218931, 21.32104025579126017 ) ) ;
#33627=DIRECTION ( 'NONE',  ( 1.000000000000000000, 0.000000000000000000, 0.000000000000000000 ) ) ;
#33635=DIRECTION ( 'NONE',  ( 0.000000000000000000, 0.000000000000000000, 1.000000000000000000 ) ) ;
#33638=DIRECTION ( 'NONE',  ( 0.000000000000000000, 0.000000000000000000, 1.000000000000000000 ) ) ;
#33655=CARTESIAN_POINT ( 'NONE',  ( 10.00000000000000000, 36.13751322684449718, -21.40280677340333071 ) ) ;
#33694=CARTESIAN_POINT ( 'NONE',  ( 4.999999999999999112, -16.65560815589383381, -38.55633173627028754 ) ) ;
#33699=CYLINDRICAL_SURFACE ( 'NONE', #24752, 37.49900000000000233 ) ;
#33707=EDGE_LOOP ( 'NONE', ( #2420, #4886, #13342, #812 ) ) ;
#33721=CARTESIAN_POINT ( 'NONE',  ( 0.000000000000000000, 16.65560815589411092, 38.55633173627015253 ) ) ;
#33733=CARTESIAN_POINT ( 'NONE',  ( 50.00005079999999680, 12.24744871391588852, 2.500000000000003553 ) ) ;
#33735=ORIENTED_EDGE ( 'NONE', *, *, #18767, .T. ) ;
#33742=FACE_OUTER_BOUND ( 'NONE', #28941, .T. ) ;
#33759=ORIENTED_EDGE ( 'NONE', *, *, #9430, .T. ) ;
#33763=CARTESIAN_POINT ( 'NONE',  ( 0.000000000000000000, 26.79245525562762253, -32.34446384429942611 ) ) ;
#33769=ORIENTED_EDGE ( 'NONE', *, *, #17208, .T. ) ;
#33777=DIRECTION ( 'NONE',  ( -1.000000000000000000, 0.000000000000000000, 0.000000000000000000 ) ) ;
#33779=ORIENTED_EDGE ( 'NONE', *, *, #42005, .T. ) ;
#33802=CARTESIAN_POINT ( 'NONE',  ( 0.000000000000000000, 41.91543099594818500, -2.663952781846294915 ) ) ;
#33823=LINE ( 'NONE', #37748, #12809 ) ;
#33830=DIRECTION ( 'NONE',  ( -1.000000000000000000, -0.000000000000000000, 0.000000000000000000 ) ) ;
#33840=DIRECTION ( 'NONE',  ( 1.000000000000000000, 0.000000000000000000, -0.000000000000000000 ) ) ;
#33841=CARTESIAN_POINT ( 'NONE',  ( 10.00000000000000000, -0.8828120875903202602, 37.48860685352291000 ) ) ;
#33859=DIRECTION ( 'NONE',  ( -1.000000000000000000, -0.000000000000000000, 0.000000000000000000 ) ) ;
#33863=DIRECTION ( 'NONE',  ( -1.000000000000000000, 0.000000000000000000, 0.000000000000000000 ) ) ;
#33875=AXIS2_PLACEMENT_3D ( 'NONE', #45839, #33830, #23539 ) ;
#33884=CYLINDRICAL_SURFACE ( 'NONE', #26008, 15.99999999999999645 ) ;
#33911=VERTEX_POINT ( 'NONE', #24079 ) ;
#33912=EDGE_CURVE ( 'NONE', #28886, #13717, #39594, .T. ) ;
#33917=DIRECTION ( 'NONE',  ( 0.000000000000000000, 0.000000000000000000, 1.000000000000000000 ) ) ;
#33919=CARTESIAN_POINT ( 'NONE',  ( 10.00000000000000000, 0.000000000000000000, 0.000000000000000000 ) ) ;
#33931=CIRCLE ( 'NONE', #4250, 16.00000000000000000 ) ;
#33938=VECTOR ( 'NONE', #9985, 1000.000000000000000 ) ;
#33940=DIRECTION ( 'NONE',  ( 0.000000000000000000, -0.3090169943749548342, 0.9510565162951511997 ) ) ;
#33943=DIRECTION ( 'NONE',  ( 0.000000000000000000, 0.000000000000000000, 1.000000000000000000 ) ) ;
#33949=ORIENTED_EDGE ( 'NONE', *, *, #45210, .F. ) ;
#33950=CARTESIAN_POINT ( 'NONE',  ( 0.000000000000000000, 33.79645857604513992, -16.45098606841138178 ) ) ;
#33956=CIRCLE ( 'NONE', #1950, 16.00000000000000000 ) ;
#33958=EDGE_CURVE ( 'NONE', #41511, #20399, #39739, .T. ) ;
#33959=EDGE_LOOP ( 'NONE', ( #42800, #13340, #13705, #5837 ) ) ;
#33985=CARTESIAN_POINT ( 'NONE',  ( 10.00000000000000000, 0.000000000000000000, 0.000000000000000000 ) ) ;
#33989=ORIENTED_EDGE ( 'NONE', *, *, #12601, .T. ) ;
#33996=DIRECTION ( 'NONE',  ( 0.000000000000000000, 0.000000000000000000, -1.000000000000000000 ) ) ;
#34000=VECTOR ( 'NONE', #23333, 1000.000000000000000 ) ;
#34004=ORIENTED_EDGE ( 'NONE', *, *, #37260, .F. ) ;
#34019=EDGE_CURVE ( 'NONE', #1962, #33236, #35665, .T. ) ;
#34029=FACE_OUTER_BOUND ( 'NONE', #23200, .T. ) ;
#34030=ORIENTED_EDGE ( 'NONE', *, *, #549, .F. ) ;
#34039=FACE_OUTER_BOUND ( 'NONE', #37947, .T. ) ;
#34046=DIRECTION ( 'NONE',  ( 0.000000000000000000, 0.3090169943749410120, 0.9510565162951557516 ) ) ;
#34054=FACE_OUTER_BOUND ( 'NONE', #9488, .T. ) ;
#34056=EDGE_CURVE ( 'NONE', #18005, #35465, #29409, .T. ) ;
#34060=CARTESIAN_POINT ( 'NONE',  ( 10.00000000000000000, 21.32104025579158701, -30.84782396557194772 ) ) ;
#34066=DIRECTION ( 'NONE',  ( 0.000000000000000000, 0.7071067811865439090, 0.7071067811865512365 ) ) ;
#34068=EDGE_LOOP ( 'NONE', ( #35880, #16539, #9171, #39515 ) ) ;
#34075=MECHANICAL_DESIGN_GEOMETRIC_PRESENTATION_REPRESENTATION('',(#9872),#27849);
#34077=AXIS2_PLACEMENT_3D ( 'NONE', #35483, #47680, #14171 ) ;
#34081=VECTOR ( 'NONE', #40678, 1000.000000000000000 ) ;
#34089=DIRECTION ( 'NONE',  ( -1.000000000000000000, 0.000000000000000000, 0.000000000000000000 ) ) ;
#34100=VERTEX_POINT ( 'NONE', #25985 ) ;
#34102=VERTEX_POINT ( 'NONE', #40930 ) ;
#34120=CIRCLE ( 'NONE', #35705, 42.00000000000000000 ) ;
#34121=CARTESIAN_POINT ( 'NONE',  ( -10.00000000000000000, 0.000000000000000000, 0.000000000000000000 ) ) ;
#34127=DIRECTION ( 'NONE',  ( -1.000000000000000000, 0.000000000000000000, 0.000000000000000000 ) ) ;
#34128=CARTESIAN_POINT ( 'NONE',  ( 5.000000000000000000, 32.34446384429971744, 26.79245525562726016 ) ) ;
#34133=AXIS2_PLACEMENT_3D ( 'NONE', #38664, #20277, #35209 ) ;
#34134=EDGE_CURVE ( 'NONE', #32362, #33911, #41413, .T. ) ;
#34142=EDGE_CURVE ( 'NONE', #22817, #48195, #17656, .T. ) ;
#34155=CARTESIAN_POINT ( 'NONE',  ( 0.000000000000000000, -33.00180498840060039, 17.80606268964528027 ) ) ;
#34156=ORIENTED_EDGE ( 'NONE', *, *, #30239, .F. ) ;
#34157=ORIENTED_EDGE ( 'NONE', *, *, #9449, .T. ) ;
#34158=CIRCLE ( 'NONE', #45890, 16.00000000000000000 ) ;
#34169=DIRECTION ( 'NONE',  ( 0.000000000000000000, 0.000000000000000000, -1.000000000000000000 ) ) ;
#34182=DIRECTION ( 'NONE',  ( 0.000000000000000000, 0.000000000000000000, 1.000000000000000000 ) ) ;
#34197=EDGE_CURVE ( 'NONE', #36905, #28265, #14745, .T. ) ;
#34201=EDGE_CURVE ( 'NONE', #26799, #42769, #19839, .T. ) ;
#34211=CARTESIAN_POINT ( 'NONE',  ( 10.00000000000000000, 27.13269053701132094, -25.88420570971372570 ) ) ;
#34235=LINE ( 'NONE', #15646, #16045 ) ;
#34242=CARTESIAN_POINT ( 'NONE',  ( -10.00000000000000000, 0.000000000000000000, 0.000000000000000000 ) ) ;
#34247=CARTESIAN_POINT ( 'NONE',  ( 5.000000000000000000, -21.40280677340398086, 36.13751322684410638 ) ) ;
#34248=ORIENTED_EDGE ( 'NONE', *, *, #46822, .F. ) ;
#34249=ADVANCED_FACE ( 'NONE', ( #15699 ), #8110, .T. ) ;
#34254=ORIENTED_EDGE ( 'NONE', *, *, #30206, .F. ) ;
#34260=DIRECTION ( 'NONE',  ( -1.000000000000000000, -0.000000000000000000, 0.000000000000000000 ) ) ;
#34263=ORIENTED_EDGE ( 'NONE', *, *, #13915, .F. ) ;
#34265=ORIENTED_EDGE ( 'NONE', *, *, #6916, .F. ) ;
#34274=DIRECTION ( 'NONE',  ( 0.000000000000000000, 0.000000000000000000, 1.000000000000000000 ) ) ;
#34275=ORIENTED_EDGE ( 'NONE', *, *, #10331, .F. ) ;
#34283=FACE_OUTER_BOUND ( 'NONE', #3217, .T. ) ;
#34286=CARTESIAN_POINT ( 'NONE',  ( 10.00000000000000000, -22.74946021919153694, 29.81001611431000597 ) ) ;
#34293=CARTESIAN_POINT ( 'NONE',  ( 10.00000000000000000, 22.74946021919133088, 29.81001611431016229 ) ) ;
#34295=EDGE_CURVE ( 'NONE', #9289, #28089, #34120, .T. ) ;
#34304=ORIENTED_EDGE ( 'NONE', *, *, #30182, .T. ) ;
#34309=EDGE_CURVE ( 'NONE', #8338, #29506, #12264, .T. ) ;
#34314=AXIS2_PLACEMENT_3D ( 'NONE', #43674, #14552, #39540 ) ;
#34318=CARTESIAN_POINT ( 'NONE',  ( 10.00000000000000178, 1.530808498934191521E-15, -12.50000000000000000 ) ) ;
#34323=CARTESIAN_POINT ( 'NONE',  ( 10.00000000000000000, 29.81001611431041098, -22.74946021919100403 ) ) ;
#34325=ORIENTED_EDGE ( 'NONE', *, *, #42005, .F. ) ;
#34328=ORIENTED_EDGE ( 'NONE', *, *, #44864, .F. ) ;
#34336=CYLINDRICAL_SURFACE ( 'NONE', #25219, 16.00000000000000000 ) ;
#34346=CYLINDRICAL_SURFACE ( 'NONE', #5990, 37.49900000000000233 ) ;
#34385=ORIENTED_EDGE ( 'NONE', *, *, #29221, .T. ) ;
#34388=CARTESIAN_POINT ( 'NONE',  ( 0.000000000000000000, 0.000000000000000000, 0.000000000000000000 ) ) ;
#34410=DIRECTION ( 'NONE',  ( 0.000000000000000000, -0.9510565162951565288, 0.3090169943749384029 ) ) ;
#34420=AXIS2_PLACEMENT_3D ( 'NONE', #11786, #41179, #11554 ) ;
#34432=ORIENTED_EDGE ( 'NONE', *, *, #36370, .T. ) ;
#34442=VERTEX_POINT ( 'NONE', #2934 ) ;
#34457=ORIENTED_EDGE ( 'NONE', *, *, #26329, .T. ) ;
#34466=CARTESIAN_POINT ( 'NONE',  ( 10.00000000000000000, -35.92658777277517856, 10.74501242461269257 ) ) ;
#34476=VERTEX_POINT ( 'NONE', #33278 ) ;
#34486=ORIENTED_EDGE ( 'NONE', *, *, #8759, .F. ) ;
#34491=CIRCLE ( 'NONE', #23568, 37.49900000000001654 ) ;
#34492=VERTEX_POINT ( 'NONE', #6856 ) ;
#34496=CARTESIAN_POINT ( 'NONE',  ( 10.00000000000000000, 0.000000000000000000, 0.000000000000000000 ) ) ;
#34499=VERTEX_POINT ( 'NONE', #18591 ) ;
#34500=DIRECTION ( 'NONE',  ( 0.000000000000000000, 0.000000000000000000, 1.000000000000000000 ) ) ;
#34501=ORIENTED_EDGE ( 'NONE', *, *, #18760, .F. ) ;
#34509=CARTESIAN_POINT ( 'NONE',  ( 5.000000000000000000, 35.47612816024523852, 22.48208911017513145 ) ) ;
#34516=CARTESIAN_POINT ( 'NONE',  ( 10.00000000000000000, 0.000000000000000000, 0.000000000000000000 ) ) ;
#34524=DIRECTION ( 'NONE',  ( -1.000000000000000000, 0.000000000000000000, 0.000000000000000000 ) ) ;
#34533=ORIENTED_EDGE ( 'NONE', *, *, #18566, .T. ) ;
#34560=CIRCLE ( 'NONE', #5631, 16.00000000000000000 ) ;
#34564=DIRECTION ( 'NONE',  ( -1.000000000000000000, -0.000000000000000000, -0.000000000000000000 ) ) ;
#34587=DIRECTION ( 'NONE',  ( -1.000000000000000000, 0.000000000000000000, 0.000000000000000000 ) ) ;
#34600=ORIENTED_EDGE ( 'NONE', *, *, #43707, .F. ) ;
#34612=CIRCLE ( 'NONE', #22157, 16.00000000000000355 ) ;
#34618=ORIENTED_EDGE ( 'NONE', *, *, #20497, .T. ) ;
#34622=CARTESIAN_POINT ( 'NONE',  ( 10.00000000000000000, 25.88420570971400991, 27.13269053701105449 ) ) ;
#34633=DIRECTION ( 'NONE',  ( 0.000000000000000000, 0.5877852522924741363, -0.8090169943749465631 ) ) ;
#34636=DIRECTION ( 'NONE',  ( -1.000000000000000000, 0.000000000000000000, 0.000000000000000000 ) ) ;
#34644=CARTESIAN_POINT ( 'NONE',  ( 10.00000000000000000, 0.000000000000000000, 0.000000000000000000 ) ) ;
#34657=DIRECTION ( 'NONE',  ( 0.000000000000000000, 0.000000000000000000, 1.000000000000000000 ) ) ;
#34663=( NAMED_UNIT ( * ) PLANE_ANGLE_UNIT ( ) SI_UNIT ( $, .RADIAN. ) );
#34667=AXIS2_PLACEMENT_3D ( 'NONE', #6192, #39732, #28708 ) ;
#34688=EDGE_CURVE ( 'NONE', #29506, #36854, #6049, .T. ) ;
#34695=VECTOR ( 'NONE', #34127, 1000.000000000000000 ) ;
#34701=ORIENTED_EDGE ( 'NONE', *, *, #3588, .F. ) ;
#34704=DIRECTION ( 'NONE',  ( 0.000000000000000000, 0.3090169943749482839, -0.9510565162951533091 ) ) ;
#34708=EDGE_CURVE ( 'NONE', #36840, #15559, #31842, .T. ) ;
#34722=ORIENTED_EDGE ( 'NONE', *, *, #10160, .T. ) ;
#34725=ORIENTED_EDGE ( 'NONE', *, *, #6934, .F. ) ;
#34733=DIRECTION ( 'NONE',  ( -1.000000000000000000, 0.000000000000000000, -0.000000000000000000 ) ) ;
#34741=VERTEX_POINT ( 'NONE', #15415 ) ;
#34753=ADVANCED_FACE ( 'NONE', ( #17314 ), #16861, .T. ) ;
#34754=VERTEX_POINT ( 'NONE', #24192 ) ;
#34759=DIRECTION ( 'NONE',  ( 0.000000000000000000, 0.000000000000000000, 1.000000000000000000 ) ) ;
#34770=CARTESIAN_POINT ( 'NONE',  ( 0.000000000000000000, 0.000000000000000000, 0.000000000000000000 ) ) ;
#34786=DIRECTION ( 'NONE',  ( 1.000000000000000000, -0.000000000000000000, -0.000000000000000000 ) ) ;
#34789=CIRCLE ( 'NONE', #13693, 16.00000000000000000 ) ;
#34793=ORIENTED_EDGE ( 'NONE', *, *, #36424, .F. ) ;
#34796=AXIS2_PLACEMENT_3D ( 'NONE', #27635, #4873, #24199 ) ;
#34798=VERTEX_POINT ( 'NONE', #43285 ) ;
#34799=AXIS2_PLACEMENT_3D ( 'NONE', #46345, #27763, #42688 ) ;
#34805=EDGE_CURVE ( 'NONE', #26939, #17075, #37273, .T. ) ;
#34809=CARTESIAN_POINT ( 'NONE',  ( 10.00000000000000000, 0.000000000000000000, 0.000000000000000000 ) ) ;
#34812=ORIENTED_EDGE ( 'NONE', *, *, #2078, .F. ) ;
#34814=ORIENTED_EDGE ( 'NONE', *, *, #2445, .T. ) ;
#34835=EDGE_LOOP ( 'NONE', ( #3115, #47544, #27338, #29651 ) ) ;
#34849=CIRCLE ( 'NONE', #41123, 37.49900000000000944 ) ;
#34860=AXIS2_PLACEMENT_3D ( 'NONE', #37077, #18709, #3549 ) ;
#34861=ORIENTED_EDGE ( 'NONE', *, *, #24813, .T. ) ;
#34876=VERTEX_POINT ( 'NONE', #1938 ) ;
#34880=DIRECTION ( 'NONE',  ( 1.000000000000000000, 0.000000000000000000, 0.000000000000000000 ) ) ;
#34881=VECTOR ( 'NONE', #1421, 1000.000000000000000 ) ;
#34882=ORIENTED_EDGE ( 'NONE', *, *, #31954, .F. ) ;
#34883=ORIENTED_EDGE ( 'NONE', *, *, #40954, .F. ) ;
#34893=LINE ( 'NONE', #5042, #22096 ) ;
#34902=DIRECTION ( 'NONE',  ( 1.000000000000000000, 0.000000000000000000, 0.000000000000000000 ) ) ;
#34904=DIRECTION ( 'NONE',  ( -1.000000000000000000, -0.000000000000000000, -0.000000000000000000 ) ) ;
#34910=VECTOR ( 'NONE', #16803, 1000.000000000000000 ) ;
#34918=EDGE_CURVE ( 'NONE', #16794, #18736, #2910, .T. ) ;
#34936=CARTESIAN_POINT ( 'NONE',  ( 10.00000000000000000, 2.663952781846149254, 41.91543099594818500 ) ) ;
#34946=EDGE_LOOP ( 'NONE', ( #3167, #9462, #34993, #8076 ) ) ;
#34948=DIRECTION ( 'NONE',  ( -1.000000000000000000, 0.000000000000000000, -0.000000000000000000 ) ) ;
#34952=FACE_OUTER_BOUND ( 'NONE', #30699, .T. ) ;
#34956=DIRECTION ( 'NONE',  ( 0.000000000000000000, 1.000000000000000000, 3.469446951953614189E-15 ) ) ;
#34957=VERTEX_POINT ( 'NONE', #33464 ) ;
#34966=EDGE_CURVE ( 'NONE', #7292, #36854, #16995, .T. ) ;
#34979=DIRECTION ( 'NONE',  ( 0.000000000000000000, 0.000000000000000000, 1.000000000000000000 ) ) ;
#34992=ORIENTED_EDGE ( 'NONE', *, *, #33436, .T. ) ;
#34993=ORIENTED_EDGE ( 'NONE', *, *, #36454, .T. ) ;
#34998=DIRECTION ( 'NONE',  ( -1.000000000000000000, -0.000000000000000000, 0.000000000000000000 ) ) ;
#35007=DIRECTION ( 'NONE',  ( 0.000000000000000000, 0.4539904997395414754, 0.8910065241883706744 ) ) ;
#35008=CARTESIAN_POINT ( 'NONE',  ( 0.000000000000000000, 0.000000000000000000, 0.000000000000000000 ) ) ;
#35019=DIRECTION ( 'NONE',  ( -1.000000000000000000, 0.000000000000000000, -0.000000000000000000 ) ) ;
#35021=VECTOR ( 'NONE', #23508, 1000.000000000000000 ) ;
#35022=LINE ( 'NONE', #28401, #47360 ) ;
#35038=DIRECTION ( 'NONE',  ( 0.000000000000000000, -0.4539904997395542430, 0.8910065241883641241 ) ) ;
#35039=ADVANCED_FACE ( 'NONE', ( #32732 ), #14143, .T. ) ;
#35049=EDGE_CURVE ( 'NONE', #44578, #24728, #2163, .T. ) ;
#35051=DIRECTION ( 'NONE',  ( -1.000000000000000000, 0.000000000000000000, 0.000000000000000000 ) ) ;
#35065=EDGE_LOOP ( 'NONE', ( #24032, #5327, #6566, #8719 ) ) ;
#35066=ORIENTED_EDGE ( 'NONE', *, *, #21162, .F. ) ;
#35079=CIRCLE ( 'NONE', #8517, 42.00000000000000000 ) ;
#35098=ORIENTED_EDGE ( 'NONE', *, *, #38484, .T. ) ;
#35106=ORIENTED_EDGE ( 'NONE', *, *, #24588, .T. ) ;
#35109=VERTEX_POINT ( 'NONE', #19004 ) ;
#35121=VECTOR ( 'NONE', #31516, 1000.000000000000000 ) ;
#35126=LINE ( 'NONE', #8226, #6548 ) ;
#35135=( NAMED_UNIT ( * ) PLANE_ANGLE_UNIT ( ) SI_UNIT ( $, .RADIAN. ) );
#35138=DIRECTION ( 'NONE',  ( 0.000000000000000000, -0.9876883405951393247, 0.1564344650402204329 ) ) ;
#35157=DIRECTION ( 'NONE',  ( -1.000000000000000000, -0.000000000000000000, 0.000000000000000000 ) ) ;
#35159=EDGE_CURVE ( 'NONE', #9450, #26893, #31881, .T. ) ;
#35162=CARTESIAN_POINT ( 'NONE',  ( 10.00000000000000000, 0.000000000000000000, 0.000000000000000000 ) ) ;
#35164=ORIENTED_EDGE ( 'NONE', *, *, #32403, .T. ) ;
#35172=EDGE_CURVE ( 'NONE', #46920, #3686, #35767, .T. ) ;
#35175=DIRECTION ( 'NONE',  ( 0.000000000000000000, -0.3090169943749349057, -0.9510565162951577500 ) ) ;
#35182=DIRECTION ( 'NONE',  ( -1.000000000000000000, -0.000000000000000000, 0.000000000000000000 ) ) ;
#35190=CYLINDRICAL_SURFACE ( 'NONE', #42301, 37.49900000000000233 ) ;
#35193=CARTESIAN_POINT ( 'NONE',  ( 10.00000000000000000, 0.000000000000000000, 0.000000000000000000 ) ) ;
#35197=DIRECTION ( 'NONE',  ( -1.000000000000000000, -0.000000000000000000, 0.000000000000000000 ) ) ;
#35204=EDGE_CURVE ( 'NONE', #20595, #43018, #13134, .T. ) ;
#35207=CIRCLE ( 'NONE', #14100, 16.00000000000000000 ) ;
#35209=DIRECTION ( 'NONE',  ( 0.000000000000000000, 0.9510565162951544194, -0.3090169943749447867 ) ) ;
#35224=AXIS2_PLACEMENT_3D ( 'NONE', #13451, #29343, #6583 ) ;
#35225=ORIENTED_EDGE ( 'NONE', *, *, #4458, .F. ) ;
#35229=CIRCLE ( 'NONE', #21148, 16.00000000000000000 ) ;
#35240=DIRECTION ( 'NONE',  ( -1.000000000000000000, 0.000000000000000000, 0.000000000000000000 ) ) ;
#35243=DIRECTION ( 'NONE',  ( -1.000000000000000000, 0.000000000000000000, 0.000000000000000000 ) ) ;
#35256=CARTESIAN_POINT ( 'NONE',  ( 10.00000000000000000, -10.41901085202107247, 40.68715046381925049 ) ) ;
#35259=EDGE_CURVE ( 'NONE', #27310, #5836, #10786, .T. ) ;
#35272=CARTESIAN_POINT ( 'NONE',  ( 5.000000000000000000, 41.91543099594818500, 2.663952781846291362 ) ) ;
#35275=ORIENTED_EDGE ( 'NONE', *, *, #20449, .F. ) ;
#35282=FACE_OUTER_BOUND ( 'NONE', #35065, .T. ) ;
#35284=ORIENTED_EDGE ( 'NONE', *, *, #4531, .T. ) ;
#35286=VECTOR ( 'NONE', #1133, 1000.000000000000000 ) ;
#35296=ORIENTED_EDGE ( 'NONE', *, *, #29556, .T. ) ;
#35307=CARTESIAN_POINT ( 'NONE',  ( 0.000000000000000000, 25.88420570971400991, 27.13269053701105449 ) ) ;
#35312=AXIS2_PLACEMENT_3D ( 'NONE', #29874, #3939, #34500 ) ;
#35335=DIRECTION ( 'NONE',  ( -1.000000000000000000, 0.000000000000000000, -0.000000000000000000 ) ) ;
#35370=CARTESIAN_POINT ( 'NONE',  ( 10.00000000000000000, 37.22597642581158084, -5.202137450156524068 ) ) ;
#35373=ORIENTED_EDGE ( 'NONE', *, *, #24315, .T. ) ;
#35381=CARTESIAN_POINT ( 'NONE',  ( -10.00000000000000000, 0.000000000000000000, 0.000000000000000000 ) ) ;
#35383=DIRECTION ( 'NONE',  ( -1.000000000000000000, 0.000000000000000000, 0.000000000000000000 ) ) ;
#35387=ORIENTED_EDGE ( 'NONE', *, *, #44273, .F. ) ;
#35424=CARTESIAN_POINT ( 'NONE',  ( 10.00000000000000000, 0.6853352020790449695, 37.58145647212454321 ) ) ;
#35427=DIRECTION ( 'NONE',  ( -1.000000000000000000, -0.000000000000000000, -0.000000000000000000 ) ) ;
#35443=DIRECTION ( 'NONE',  ( 0.000000000000000000, 0.000000000000000000, 1.000000000000000000 ) ) ;
#35465=VERTEX_POINT ( 'NONE', #40941 ) ;
#35474=PRODUCT_DEFINITION_SHAPE ( 'NONE', 'NONE',  #46888 ) ;
#35476=EDGE_CURVE ( 'NONE', #34754, #28089, #30899, .T. ) ;
#35483=CARTESIAN_POINT ( 'NONE',  ( 10.00000000000000000, 35.53030884539102630, -12.26510123303222599 ) ) ;
#35493=DIRECTION ( 'NONE',  ( -1.000000000000000000, -0.000000000000000000, -0.000000000000000000 ) ) ;
#35494=EDGE_LOOP ( 'NONE', ( #36620, #24282, #12688, #19894 ) ) ;
#35501=CYLINDRICAL_SURFACE ( 'NONE', #47272, 16.00000000000000000 ) ;
#35502=ORIENTED_EDGE ( 'NONE', *, *, #9596, .T. ) ;
#35513=AXIS2_PLACEMENT_3D ( 'NONE', #2767, #25266, #18425 ) ;
#35518=CARTESIAN_POINT ( 'NONE',  ( 10.00000000000000000, 21.53537804866081373, 30.80686688397018358 ) ) ;
#35546=ORIENTED_EDGE ( 'NONE', *, *, #13372, .T. ) ;
#35560=DIRECTION ( 'NONE',  ( 0.000000000000000000, -0.8090169943749531134, 0.5877852522924653655 ) ) ;
#35562=CIRCLE ( 'NONE', #14458, 16.00000000000000000 ) ;
#35596=CIRCLE ( 'NONE', #12933, 42.00000000000000000 ) ;
#35606=ORIENTED_EDGE ( 'NONE', *, *, #33436, .F. ) ;
#35612=LINE ( 'NONE', #34622, #3560 ) ;
#35627=CARTESIAN_POINT ( 'NONE',  ( 0.000000000000000000, 0.000000000000000000, 0.000000000000000000 ) ) ;
#35637=CIRCLE ( 'NONE', #12198, 16.00000000000000000 ) ;
#35643=VERTEX_POINT ( 'NONE', #24968 ) ;
#35654=AXIS2_PLACEMENT_3D ( 'NONE', #539, #26247, #11562 ) ;
#35665=CIRCLE ( 'NONE', #23152, 15.99999999999999822 ) ;
#35672=DIRECTION ( 'NONE',  ( -1.000000000000000000, -0.000000000000000000, -0.000000000000000000 ) ) ;
#35687=LINE ( 'NONE', #42552, #51 ) ;
#35703=DIRECTION ( 'NONE',  ( -1.000000000000000000, 0.000000000000000000, -0.000000000000000000 ) ) ;
#35705=AXIS2_PLACEMENT_3D ( 'NONE', #16426, #5181, #12043 ) ;
#35710=CIRCLE ( 'NONE', #47409, 42.00000000000000000 ) ;
#35712=CARTESIAN_POINT ( 'NONE',  ( 10.00000000000000000, -33.79645857604525361, 16.45098606841114730 ) ) ;
#35716=CIRCLE ( 'NONE', #34133, 16.00000000000000355 ) ;
#35717=DIRECTION ( 'NONE',  ( -1.000000000000000000, -0.000000000000000000, -0.000000000000000000 ) ) ;
#35718=VERTEX_POINT ( 'NONE', #46703 ) ;
#35743=ORIENTED_EDGE ( 'NONE', *, *, #19943, .T. ) ;
#35746=DIRECTION ( 'NONE',  ( 0.000000000000000000, 0.000000000000000000, 1.000000000000000000 ) ) ;
#35757=CARTESIAN_POINT ( 'NONE',  ( 0.000000000000000000, -12.42422080174614862, -35.38097989696524337 ) ) ;
#35763=VECTOR ( 'NONE', #40665, 1000.000000000000000 ) ;
#35764=DIRECTION ( 'NONE',  ( 1.000000000000000000, 0.000000000000000000, 0.000000000000000000 ) ) ;
#35767=CIRCLE ( 'NONE', #14666, 16.00000000000000355 ) ;
#35773=DIRECTION ( 'NONE',  ( 0.000000000000000000, 0.000000000000000000, 1.000000000000000000 ) ) ;
#35776=ORIENTED_EDGE ( 'NONE', *, *, #14034, .T. ) ;
#35788=DIRECTION ( 'NONE',  ( -1.000000000000000000, -0.000000000000000000, -0.000000000000000000 ) ) ;
#35798=EDGE_CURVE ( 'NONE', #13193, #19386, #10820, .T. ) ;
#35811=ORIENTED_EDGE ( 'NONE', *, *, #6626, .F. ) ;
#35821=CIRCLE ( 'NONE', #31932, 16.00000000000000000 ) ;
#35831=VERTEX_POINT ( 'NONE', #15866 ) ;
#35833=ORIENTED_EDGE ( 'NONE', *, *, #6149, .T. ) ;
#35839=CARTESIAN_POINT ( 'NONE',  ( 10.00000000000000000, -27.05870788708250885, 26.08949754953014022 ) ) ;
#35862=AXIS2_PLACEMENT_3D ( 'NONE', #48229, #40886, #36954 ) ;
#35869=ADVANCED_FACE ( 'NONE', ( #24662 ), #39609, .T. ) ;
#35878=CARTESIAN_POINT ( 'NONE',  ( 0.000000000000000000, 25.88420570971438650, -27.13269053701069566 ) ) ;
#35880=ORIENTED_EDGE ( 'NONE', *, *, #1863, .T. ) ;
#35897=DIRECTION ( 'NONE',  ( 1.000000000000000000, 0.000000000000000000, 0.000000000000000000 ) ) ;
#35906=DIRECTION ( 'NONE',  ( -1.000000000000000000, 0.000000000000000000, 0.000000000000000000 ) ) ;
#35913=CARTESIAN_POINT ( 'NONE',  ( 10.00000000000000000, -16.23288003029473359, -33.80338159004301701 ) ) ;
#35916=CARTESIAN_POINT ( 'NONE',  ( 0.000000000000000000, 16.45098606841126454, 33.79645857604518966 ) ) ;
#35925=VECTOR ( 'NONE', #11254, 1000.000000000000000 ) ;
#35942=CYLINDRICAL_SURFACE ( 'NONE', #14807, 16.00000000000000000 ) ;
#35948=EDGE_LOOP ( 'NONE', ( #41855, #519, #32469, #47404 ) ) ;
#35956=CARTESIAN_POINT ( 'NONE',  ( 0.000000000000000000, 35.53030884539084866, 12.26510123303271982 ) ) ;
#35963=ORIENTED_EDGE ( 'NONE', *, *, #34019, .T. ) ;
#35964=ADVANCED_FACE ( 'NONE', ( #1699 ), #17102, .T. ) ;
#35965=CIRCLE ( 'NONE', #9407, 15.99999999999999822 ) ;
#35976=DIRECTION ( 'NONE',  ( -1.000000000000000000, 0.000000000000000000, -0.000000000000000000 ) ) ;
#35998=EDGE_LOOP ( 'NONE', ( #39324, #15877, #33267, #26647 ) ) ;
#36009=DIRECTION ( 'NONE',  ( -1.000000000000000000, 0.000000000000000000, 0.000000000000000000 ) ) ;
#36015=EDGE_CURVE ( 'NONE', #42769, #28690, #19427, .T. ) ;
#36016=LINE ( 'NONE', #47288, #45458 ) ;
#36026=ORIENTED_EDGE ( 'NONE', *, *, #27163, .T. ) ;
#36046=LINE ( 'NONE', #2507, #12943 ) ;
#36049=EDGE_CURVE ( 'NONE', #40832, #12600, #46810, .T. ) ;
#36054=ORIENTED_EDGE ( 'NONE', *, *, #42077, .F. ) ;
#36055=FACE_OUTER_BOUND ( 'NONE', #44076, .T. ) ;
#36063=AXIS2_PLACEMENT_3D ( 'NONE', #20549, #35493, #33917 ) ;
#36065=EDGE_CURVE ( 'NONE', #18356, #41330, #44458, .T. ) ;
#36081=ORIENTED_EDGE ( 'NONE', *, *, #46966, .F. ) ;
#36097=CARTESIAN_POINT ( 'NONE',  ( 10.00000000000000000, -31.52238457039619490, 27.75498641678731104 ) ) ;
#36119=VERTEX_POINT ( 'NONE', #38417 ) ;
#36164=CIRCLE ( 'NONE', #24432, 37.49900000000000233 ) ;
#36176=ORIENTED_EDGE ( 'NONE', *, *, #33312, .T. ) ;
#36184=EDGE_CURVE ( 'NONE', #33159, #42195, #17859, .T. ) ;
#36186=ORIENTED_EDGE ( 'NONE', *, *, #281, .F. ) ;
#36197=CARTESIAN_POINT ( 'NONE',  ( 0.000000000000000000, 38.55633173627034438, -16.65560815589369881 ) ) ;
#36198=CIRCLE ( 'NONE', #11970, 16.00000000000000000 ) ;
#36201=DIRECTION ( 'NONE',  ( -1.000000000000000000, 0.000000000000000000, 0.000000000000000000 ) ) ;
#36219=CARTESIAN_POINT ( 'NONE',  ( 10.00000000000000000, -35.38097989696520074, 12.42422080174625520 ) ) ;
#36224=ADVANCED_FACE ( 'NONE', ( #21966 ), #6104, .T. ) ;
#36232=CIRCLE ( 'NONE', #14331, 16.00000000000000000 ) ;
#36237=AXIS2_PLACEMENT_3D ( 'NONE', #40553, #36399, #22188 ) ;
#36239=ADVANCED_FACE ( 'NONE', ( #21012 ), #35942, .T. ) ;
#36248=VERTEX_POINT ( 'NONE', #30055 ) ;
#36277=CIRCLE ( 'NONE', #41735, 37.49900000000000233 ) ;
#36305=CIRCLE ( 'NONE', #41001, 42.00000000000000000 ) ;
#36315=EDGE_CURVE ( 'NONE', #29561, #10410, #29637, .T. ) ;
#36323=ORIENTED_EDGE ( 'NONE', *, *, #16844, .F. ) ;
#36333=ORIENTED_EDGE ( 'NONE', *, *, #28185, .T. ) ;
#36342=CYLINDRICAL_SURFACE ( 'NONE', #8203, 37.49900000000000233 ) ;
#36343=DIRECTION ( 'NONE',  ( 0.000000000000000000, 1.000000000000000000, -9.787530781167598712E-16 ) ) ;
#36345=DIRECTION ( 'NONE',  ( 1.000000000000000000, 0.000000000000000000, 0.000000000000000000 ) ) ;
#36347=ORIENTED_EDGE ( 'NONE', *, *, #25674, .T. ) ;
#36365=EDGE_CURVE ( 'NONE', #26919, #25452, #1526, .T. ) ;
#36368=ORIENTED_EDGE ( 'NONE', *, *, #18767, .F. ) ;
#36370=EDGE_CURVE ( 'NONE', #22230, #27073, #41390, .T. ) ;
#36371=ORIENTED_EDGE ( 'NONE', *, *, #10370, .F. ) ;
#36383=DIRECTION ( 'NONE',  ( 0.000000000000000000, 0.000000000000000000, 1.000000000000000000 ) ) ;
#36389=DIRECTION ( 'NONE',  ( 0.000000000000000000, -0.9876883405951358830, -0.1564344650402421932 ) ) ;
#36399=DIRECTION ( 'NONE',  ( -1.000000000000000000, 0.000000000000000000, 0.000000000000000000 ) ) ;
#36409=CIRCLE ( 'NONE', #45784, 16.00000000000000355 ) ;
#36424=EDGE_CURVE ( 'NONE', #15559, #41267, #9221, .T. ) ;
#36426=ORIENTED_EDGE ( 'NONE', *, *, #10160, .F. ) ;
#36436=ORIENTED_EDGE ( 'NONE', *, *, #18765, .T. ) ;
#36441=CARTESIAN_POINT ( 'NONE',  ( 10.00000000000000000, -33.00180498840060039, 17.80606268964528027 ) ) ;
#36446=DIRECTION ( 'NONE',  ( -1.000000000000000000, -0.000000000000000000, 0.000000000000000000 ) ) ;
#36447=CYLINDRICAL_SURFACE ( 'NONE', #16643, 16.00000000000000000 ) ;
#36454=EDGE_CURVE ( 'NONE', #21714, #17599, #16818, .T. ) ;
#36473=AXIS2_PLACEMENT_3D ( 'NONE', #19717, #16083, #26371 ) ;
#36479=AXIS2_PLACEMENT_3D ( 'NONE', #4578, #30766, #33940 ) ;
#36483=VERTEX_POINT ( 'NONE', #8490 ) ;
#36486=CIRCLE ( 'NONE', #46681, 16.00000000000000000 ) ;
#36504=CIRCLE ( 'NONE', #21669, 42.00000000000000000 ) ;
#36507=CYLINDRICAL_SURFACE ( 'NONE', #28570, 16.00000000000000000 ) ;
#36513=FACE_OUTER_BOUND ( 'NONE', #23681, .T. ) ;
#36514=ADVANCED_FACE ( 'NONE', ( #19991 ), #16329, .T. ) ;
#36547=EDGE_LOOP ( 'NONE', ( #31665, #30822, #10545, #46526 ) ) ;
#36563=CARTESIAN_POINT ( 'NONE',  ( 10.00000000000000000, -17.67226234102849958, 33.17418723428301774 ) ) ;
#36579=EDGE_CURVE ( 'NONE', #2845, #26639, #4661, .T. ) ;
#36580=CYLINDRICAL_SURFACE ( 'NONE', #31678, 37.49900000000000233 ) ;
#36605=DIRECTION ( 'NONE',  ( 0.000000000000000000, 0.000000000000000000, 1.000000000000000000 ) ) ;
#36615=DIRECTION ( 'NONE',  ( 0.000000000000000000, -0.4539904997395540764, 0.8910065241883642351 ) ) ;
#36619=ORIENTED_EDGE ( 'NONE', *, *, #3871, .F. ) ;
#36620=ORIENTED_EDGE ( 'NONE', *, *, #21698, .T. ) ;
#36621=CARTESIAN_POINT ( 'NONE',  ( 0.000000000000000000, 33.17418723428307459, 17.67226234102837878 ) ) ;
#36629=CARTESIAN_POINT ( 'NONE',  ( 10.00000000000000000, -37.58145647212455032, 0.6853352020789044152 ) ) ;
#36651=DIRECTION ( 'NONE',  ( -1.000000000000000000, 0.000000000000000000, 0.000000000000000000 ) ) ;
#36660=CIRCLE ( 'NONE', #19429, 15.99999999999999645 ) ;
#36669=CARTESIAN_POINT ( 'NONE',  ( 0.000000000000000000, 9.188173127307898369, -40.98264845739739570 ) ) ;
#36672=ORIENTED_EDGE ( 'NONE', *, *, #9565, .F. ) ;
#36674=DIRECTION ( 'NONE',  ( 0.000000000000000000, 0.000000000000000000, 1.000000000000000000 ) ) ;
#36680=ADVANCED_FACE ( 'NONE', ( #4050 ), #22881, .T. ) ;
#36700=AXIS2_PLACEMENT_3D ( 'NONE', #18914, #22603, #43259 ) ;
#36702=DIRECTION ( 'NONE',  ( -1.000000000000000000, -0.000000000000000000, -0.000000000000000000 ) ) ;
#36728=ORIENTED_EDGE ( 'NONE', *, *, #30793, .F. ) ;
#36745=DIRECTION ( 'NONE',  ( 0.000000000000000000, 0.000000000000000000, 1.000000000000000000 ) ) ;
#36757=VECTOR ( 'NONE', #28686, 1000.000000000000000 ) ;
#36764=FACE_OUTER_BOUND ( 'NONE', #21168, .T. ) ;
#36765=CARTESIAN_POINT ( 'NONE',  ( -10.00000000000000000, 0.000000000000000000, 0.000000000000000000 ) ) ;
#36789=AXIS2_PLACEMENT_3D ( 'NONE', #22612, #26294, #37784 ) ;
#36805=VERTEX_POINT ( 'NONE', #46562 ) ;
#36807=CARTESIAN_POINT ( 'NONE',  ( 0.000000000000000000, 0.000000000000000000, 0.000000000000000000 ) ) ;
#36811=ORIENTED_EDGE ( 'NONE', *, *, #42708, .T. ) ;
#36816=ADVANCED_FACE ( 'NONE', ( #35282 ), #15787, .T. ) ;
#36824=EDGE_CURVE ( 'NONE', #33159, #18007, #17157, .T. ) ;
#36826=CARTESIAN_POINT ( 'NONE',  ( 0.000000000000000000, 0.000000000000000000, 0.000000000000000000 ) ) ;
#36838=ADVANCED_FACE ( 'NONE', ( #31887 ), #27056, .T. ) ;
#36840=VERTEX_POINT ( 'NONE', #9822 ) ;
#36854=VERTEX_POINT ( 'NONE', #1760 ) ;
#36875=CARTESIAN_POINT ( 'NONE',  ( 10.00000000000000000, 35.92658777277511462, 10.74501242461295014 ) ) ;
#36885=DIRECTION ( 'NONE',  ( -1.000000000000000000, -0.000000000000000000, -0.000000000000000000 ) ) ;
#36887=ORIENTED_EDGE ( 'NONE', *, *, #32053, .F. ) ;
#36903=ORIENTED_EDGE ( 'NONE', *, *, #7345, .T. ) ;
#36905=VERTEX_POINT ( 'NONE', #5674 ) ;
#36914=AXIS2_PLACEMENT_3D ( 'NONE', #33580, #42, #288 ) ;
#36916=DIRECTION ( 'NONE',  ( 0.000000000000000000, -0.4539904997395540764, 0.8910065241883642351 ) ) ;
#36917=AXIS2_PLACEMENT_3D ( 'NONE', #46042, #8348, #45303 ) ;
#36922=ORIENTED_EDGE ( 'NONE', *, *, #28616, .T. ) ;
#36935=DIRECTION ( 'NONE',  ( -1.000000000000000000, -0.000000000000000000, -0.000000000000000000 ) ) ;
#36936=VERTEX_POINT ( 'NONE', #37211 ) ;
#36947=ADVANCED_FACE ( 'NONE', ( #21791 ), #18366, .T. ) ;
#36950=EDGE_CURVE ( 'NONE', #47647, #8291, #25697, .T. ) ;
#36954=DIRECTION ( 'NONE',  ( 0.000000000000000000, 0.000000000000000000, 1.000000000000000000 ) ) ;
#36955=AXIS2_PLACEMENT_3D ( 'NONE', #45195, #640, #26590 ) ;
#36959=EDGE_LOOP ( 'NONE', ( #19941, #12421, #14651, #47326 ) ) ;
#36961=ORIENTED_EDGE ( 'NONE', *, *, #1551, .T. ) ;
#36965=VECTOR ( 'NONE', #9027, 1000.000000000000000 ) ;
#36992=CARTESIAN_POINT ( 'NONE',  ( 0.000000000000000000, 6.736453364084091788, -36.88895765772625879 ) ) ;
#36993=VERTEX_POINT ( 'NONE', #10553 ) ;
#36999=VERTEX_POINT ( 'NONE', #6877 ) ;
#37001=DIRECTION ( 'NONE',  ( 0.000000000000000000, -0.9876883405951358830, -0.1564344650402420822 ) ) ;
#37028=EDGE_CURVE ( 'NONE', #36483, #47876, #2711, .T. ) ;
#37031=AXIS2_PLACEMENT_3D ( 'NONE', #32404, #25520, #14524 ) ;
#37035=VERTEX_POINT ( 'NONE', #17875 ) ;
#37038=AXIS2_PLACEMENT_3D ( 'NONE', #36629, #14367, #10705 ) ;
#37042=CARTESIAN_POINT ( 'NONE',  ( 10.00000000000000000, 37.16516213103285082, -4.992566952384588141 ) ) ;
#37054=AXIS2_PLACEMENT_3D ( 'NONE', #12458, #23703, #27626 ) ;
#37061=CIRCLE ( 'NONE', #40180, 16.00000000000000000 ) ;
#37077=CARTESIAN_POINT ( 'NONE',  ( 10.00000000000000000, -37.01155633439063308, 6.555932627142289526 ) ) ;
#37082=ORIENTED_EDGE ( 'NONE', *, *, #39580, .F. ) ;
#37097=DIRECTION ( 'NONE',  ( 0.000000000000000000, 0.4539904997395412534, 0.8910065241883706744 ) ) ;
#37107=ORIENTED_EDGE ( 'NONE', *, *, #18566, .F. ) ;
#37120=ORIENTED_EDGE ( 'NONE', *, *, #14658, .F. ) ;
#37136=DIRECTION ( 'NONE',  ( 0.000000000000000000, -0.5877852522924624790, -0.8090169943749552228 ) ) ;
#37145=CARTESIAN_POINT ( 'NONE',  ( 0.000000000000000000, 33.80338159004307386, -16.23288003029461279 ) ) ;
#37146=CARTESIAN_POINT ( 'NONE',  ( -10.00000000000000000, 0.000000000000000000, 0.000000000000000000 ) ) ;
#37153=DIRECTION ( 'NONE',  ( 0.000000000000000000, 0.000000000000000000, -1.000000000000000000 ) ) ;
#37163=AXIS2_PLACEMENT_3D ( 'NONE', #31596, #43325, #24718 ) ;
#37176=ADVANCED_FACE ( 'NONE', ( #4172 ), #15435, .T. ) ;
#37177=CIRCLE ( 'NONE', #15322, 37.49900000000000944 ) ;
#37194=DIRECTION ( 'NONE',  ( 0.000000000000000000, 0.000000000000000000, 1.000000000000000000 ) ) ;
#37203=CIRCLE ( 'NONE', #1266, 37.49900000000001654 ) ;
#37211=CARTESIAN_POINT ( 'NONE',  ( 10.00000000000000000, -35.38097989696503021, -12.42422080174676147 ) ) ;
#37215=ORIENTED_EDGE ( 'NONE', *, *, #9842, .T. ) ;
#37225=LINE ( 'NONE', #40431, #8204 ) ;
#37226=DIRECTION ( 'NONE',  ( 0.000000000000000000, 0.000000000000000000, 1.000000000000000000 ) ) ;
#37228=ORIENTED_EDGE ( 'NONE', *, *, #978, .T. ) ;
#37229=CARTESIAN_POINT ( 'NONE',  ( 5.000000000000000000, -27.75498641678764855, 31.52238457039590358 ) ) ;
#37235=EDGE_LOOP ( 'NONE', ( #11, #21325, #16745, #43303 ) ) ;
#37243=ORIENTED_EDGE ( 'NONE', *, *, #39522, .T. ) ;
#37252=EDGE_CURVE ( 'NONE', #7054, #38938, #8601, .T. ) ;
#37254=CARTESIAN_POINT ( 'NONE',  ( 10.00000000000000000, 0.000000000000000000, 0.000000000000000000 ) ) ;
#37260=EDGE_CURVE ( 'NONE', #10554, #2634, #21111, .T. ) ;
#37273=CIRCLE ( 'NONE', #5246, 16.00000000000000000 ) ;
#37274=CARTESIAN_POINT ( 'NONE',  ( 10.00000000000000000, -33.17418723428294669, -17.67226234102862747 ) ) ;
#37278=VERTEX_POINT ( 'NONE', #43062 ) ;
#37279=AXIS2_PLACEMENT_3D ( 'NONE', #32213, #24621, #1623 ) ;
#37281=AXIS2_PLACEMENT_3D ( 'NONE', #24141, #46175, #34657 ) ;
#37283=DIRECTION ( 'NONE',  ( -1.000000000000000000, 0.000000000000000000, 0.000000000000000000 ) ) ;
#37297=DIRECTION ( 'NONE',  ( -1.000000000000000000, -0.000000000000000000, 0.000000000000000000 ) ) ;
#37326=DIRECTION ( 'NONE',  ( -1.000000000000000000, -0.000000000000000000, -0.000000000000000000 ) ) ;
#37327=DIRECTION ( 'NONE',  ( 1.000000000000000000, 0.000000000000000000, -0.000000000000000000 ) ) ;
#37329=CYLINDRICAL_SURFACE ( 'NONE', #7220, 37.49900000000000233 ) ;
#37331=EDGE_LOOP ( 'NONE', ( #12384, #11146, #34992, #31771 ) ) ;
#37333=ORIENTED_EDGE ( 'NONE', *, *, #39759, .T. ) ;
#37334=AXIS2_PLACEMENT_3D ( 'NONE', #43527, #21001, #2389 ) ;
#37341=DIRECTION ( 'NONE',  ( -1.000000000000000000, 0.000000000000000000, 0.000000000000000000 ) ) ;
#37357=DIRECTION ( 'NONE',  ( 0.000000000000000000, 0.9876883405951372152, 0.1564344650402346160 ) ) ;
#37366=CARTESIAN_POINT ( 'NONE',  ( 10.00000000000000000, -16.45098606841149902, 33.79645857604508308 ) ) ;
#37373=EDGE_LOOP ( 'NONE', ( #34722, #466, #34793, #6418 ) ) ;
#37383=DIRECTION ( 'NONE',  ( -1.000000000000000000, -0.000000000000000000, 0.000000000000000000 ) ) ;
#37396=AXIS2_PLACEMENT_3D ( 'NONE', #35424, #16585, #12440 ) ;
#37417=VERTEX_POINT ( 'NONE', #22234 ) ;
#37420=DIRECTION ( 'NONE',  ( -1.000000000000000000, 0.000000000000000000, -0.000000000000000000 ) ) ;
#37425=DIRECTION ( 'NONE',  ( 0.000000000000000000, 0.000000000000000000, 1.000000000000000000 ) ) ;
#37430=CARTESIAN_POINT ( 'NONE',  ( 5.000000000000000000, -32.34446384429989507, 26.79245525562703278 ) ) ;
#37435=CARTESIAN_POINT ( 'NONE',  ( 10.00000000000000000, -37.48860685352290290, -0.8828120875904512665 ) ) ;
#37448=CARTESIAN_POINT ( 'NONE',  ( 10.00000000000000000, 10.41901085202078114, 40.68715046381932865 ) ) ;
#37450=CARTESIAN_POINT ( 'NONE',  ( -10.00000000000000000, 0.000000000000000000, 0.000000000000000000 ) ) ;
#37453=COLOUR_RGB ( '', 0.09019608, 0.27058824, 0.51372549) ;
#37483=CARTESIAN_POINT ( 'NONE',  ( 5.000000000000000000, 31.52238457039637609, -27.75498641678709788 ) ) ;
#37490=CARTESIAN_POINT ( 'NONE',  ( 0.000000000000000000, -40.68715046381921496, -10.41901085202121280 ) ) ;
#37504=VECTOR ( 'NONE', #41358, 1000.000000000000000 ) ;
#37505=CARTESIAN_POINT ( 'NONE',  ( 0.000000000000000000, 3.925862922256160736, 41.81611651403863306 ) ) ;
#37506=AXIS2_PLACEMENT_3D ( 'NONE', #29213, #14045, #10367 ) ;
#37515=ORIENTED_EDGE ( 'NONE', *, *, #6405, .F. ) ;
#37525=ORIENTED_EDGE ( 'NONE', *, *, #22104, .F. ) ;
#37526=CARTESIAN_POINT ( 'NONE',  ( -10.00000000000000000, 0.000000000000000000, 0.000000000000000000 ) ) ;
#37533=CARTESIAN_POINT ( 'NONE',  ( 0.000000000000000000, -41.81611651403864727, 3.925862922256025289 ) ) ;
#37534=ORIENTED_EDGE ( 'NONE', *, *, #30913, .F. ) ;
#37540=FACE_OUTER_BOUND ( 'NONE', #45633, .T. ) ;
#37548=CIRCLE ( 'NONE', #1, 42.00000000000000000 ) ;
#37558=ORIENTED_EDGE ( 'NONE', *, *, #41564, .T. ) ;
#37574=ADVANCED_FACE ( 'NONE', ( #45457 ), #22479, .T. ) ;
#37586=ORIENTED_EDGE ( 'NONE', *, *, #44712, .T. ) ;
#37602=CYLINDRICAL_SURFACE ( 'NONE', #7273, 37.49900000000000233 ) ;
#37614=AXIS2_PLACEMENT_3D ( 'NONE', #34496, #8556, #46260 ) ;
#37620=CARTESIAN_POINT ( 'NONE',  ( 10.00000000000000000, -5.202137450156129717, -37.22597642581163768 ) ) ;
#37626=EDGE_CURVE ( 'NONE', #37278, #25452, #26504, .T. ) ;
#37628=( NAMED_UNIT ( * ) SI_UNIT ( $, .STERADIAN. ) SOLID_ANGLE_UNIT ( ) );
#37650=DIRECTION ( 'NONE',  ( 0.000000000000000000, 0.4539904997395477482, -0.8910065241883673437 ) ) ;
#37660=CARTESIAN_POINT ( 'NONE',  ( 10.00000000000000000, -37.58145647212453611, -0.6853352020794456489 ) ) ;
#37674=DIRECTION ( 'NONE',  ( 1.000000000000000000, 0.000000000000000000, 0.000000000000000000 ) ) ;
#37692=ORIENTED_EDGE ( 'NONE', *, *, #24259, .T. ) ;
#37705=AXIS2_PLACEMENT_3D ( 'NONE', #19102, #11771, #37226 ) ;
#37708=DIRECTION ( 'NONE',  ( 0.000000000000000000, -0.5877852522924624790, -0.8090169943749553338 ) ) ;
#37715=CARTESIAN_POINT ( 'NONE',  ( 4.999999999999999112, -3.925862922256468046, 41.81611651403860463 ) ) ;
#37718=VECTOR ( 'NONE', #39291, 1000.000000000000000 ) ;
#37725=AXIS2_PLACEMENT_3D ( 'NONE', #39077, #17264, #13137 ) ;
#37735=DIRECTION ( 'NONE',  ( -1.000000000000000000, 0.000000000000000000, -0.000000000000000000 ) ) ;
#37747=AXIS2_PLACEMENT_3D ( 'NONE', #43336, #47239, #39424 ) ;
#37748=CARTESIAN_POINT ( 'NONE',  ( 4.999999999999999112, -2.663952781846440576, 41.91543099594817789 ) ) ;
#37749=ORIENTED_EDGE ( 'NONE', *, *, #14859, .F. ) ;
#37751=DIRECTION ( 'NONE',  ( 1.000000000000000000, 0.000000000000000000, 0.000000000000000000 ) ) ;
#37752=CIRCLE ( 'NONE', #22087, 16.00000000000000000 ) ;
#37764=CYLINDRICAL_SURFACE ( 'NONE', #18391, 16.00000000000000000 ) ;
#37771=CARTESIAN_POINT ( 'NONE',  ( 0.000000000000000000, 21.32104025579158701, -30.84782396557194772 ) ) ;
#37781=AXIS2_PLACEMENT_3D ( 'NONE', #6811, #36651, #7036 ) ;
#37784=DIRECTION ( 'NONE',  ( 0.000000000000000000, 0.000000000000000000, 1.000000000000000000 ) ) ;
#37798=AXIS2_PLACEMENT_3D ( 'NONE', #3990, #41205, #41928 ) ;
#37812=VECTOR ( 'NONE', #12962, 1000.000000000000000 ) ;
#37821=VECTOR ( 'NONE', #7577, 1000.000000000000000 ) ;
#37823=CIRCLE ( 'NONE', #1893, 16.00000000000000355 ) ;
#37830=ADVANCED_FACE ( 'NONE', ( #32934 ), #40308, .T. ) ;
#37831=DIRECTION ( 'NONE',  ( -1.000000000000000000, 0.000000000000000000, 0.000000000000000000 ) ) ;
#37838=VERTEX_POINT ( 'NONE', #48114 ) ;
#37851=ORIENTED_EDGE ( 'NONE', *, *, #45319, .F. ) ;
#37855=CIRCLE ( 'NONE', #1086, 42.00000000000000000 ) ;
#37860=ADVANCED_FACE ( 'NONE', ( #13623 ), #10428, .T. ) ;
#37865=EDGE_LOOP ( 'NONE', ( #1077, #13229, #5250, #39043 ) ) ;
#37871=EDGE_CURVE ( 'NONE', #3376, #46202, #38277, .T. ) ;
#37881=DIRECTION ( 'NONE',  ( -1.000000000000000000, 0.000000000000000000, -0.000000000000000000 ) ) ;
#37905=CARTESIAN_POINT ( 'NONE',  ( 10.00000000000000000, -16.45098606841102651, -33.79645857604531045 ) ) ;
#37913=ORIENTED_EDGE ( 'NONE', *, *, #32175, .T. ) ;
#37918=CARTESIAN_POINT ( 'NONE',  ( 5.000000000000000000, -35.47612816024539484, 22.48208911017487921 ) ) ;
#37935=AXIS2_PLACEMENT_3D ( 'NONE', #47568, #6712, #25772 ) ;
#37946=ORIENTED_EDGE ( 'NONE', *, *, #10176, .F. ) ;
#37947=EDGE_LOOP ( 'NONE', ( #28300, #39874, #43231, #16950 ) ) ;
#37959=FACE_OUTER_BOUND ( 'NONE', #44617, .T. ) ;
#37976=ADVANCED_BREP_SHAPE_REPRESENTATION ( '', ( #2442, #11636 ), #10100 ) ;
#37983=DIRECTION ( 'NONE',  ( -1.000000000000000000, 0.000000000000000000, -0.000000000000000000 ) ) ;
#37991=LINE ( 'NONE', #45825, #8967 ) ;
#37993=VECTOR ( 'NONE', #30229, 1000.000000000000000 ) ;
#38045=DIRECTION ( 'NONE',  ( -1.000000000000000000, 0.000000000000000000, 0.000000000000000000 ) ) ;
#38055=CARTESIAN_POINT ( 'NONE',  ( 10.00000000000000000, 12.42422080174639021, 35.38097989696516521 ) ) ;
#38060=CARTESIAN_POINT ( 'NONE',  ( 5.000000000000000000, -35.47612816024506088, -22.48208911017539435 ) ) ;
#38069=ORIENTED_EDGE ( 'NONE', *, *, #21987, .T. ) ;
#38070=AXIS2_PLACEMENT_3D ( 'NONE', #45148, #30456, #15765 ) ;
#38086=ORIENTED_EDGE ( 'NONE', *, *, #3179, .F. ) ;
#38126=VERTEX_POINT ( 'NONE', #27061 ) ;
#38137=CARTESIAN_POINT ( 'NONE',  ( 10.00000000000000000, 27.05870788708267582, -26.08949754952995903 ) ) ;
#38152=LINE ( 'NONE', #26895, #72 ) ;
#38161=DIRECTION ( 'NONE',  ( 0.000000000000000000, 0.3090169943749411230, 0.9510565162951555296 ) ) ;
#38164=DIRECTION ( 'NONE',  ( 0.000000000000000000, 0.000000000000000000, 1.000000000000000000 ) ) ;
#38180=DIRECTION ( 'NONE',  ( 0.000000000000000000, -0.1564344650402170189, -0.9876883405951399908 ) ) ;
#38181=VECTOR ( 'NONE', #21865, 1000.000000000000000 ) ;
#38184=ORIENTED_EDGE ( 'NONE', *, *, #3002, .T. ) ;
#38206=ORIENTED_EDGE ( 'NONE', *, *, #20619, .F. ) ;
#38214=VERTEX_POINT ( 'NONE', #33125 ) ;
#38242=EDGE_CURVE ( 'NONE', #39757, #46672, #3018, .T. ) ;
#38248=EDGE_CURVE ( 'NONE', #45189, #26808, #3109, .T. ) ;
#38268=CARTESIAN_POINT ( 'NONE',  ( 4.999999999999999112, -41.91543099594816368, -2.663952781846588014 ) ) ;
#38277=CIRCLE ( 'NONE', #17156, 16.00000000000000000 ) ;
#38287=DIRECTION ( 'NONE',  ( -1.000000000000000000, -0.000000000000000000, -0.000000000000000000 ) ) ;
#38294=EDGE_CURVE ( 'NONE', #42217, #38611, #30478, .T. ) ;
#38300=ADVANCED_FACE ( 'NONE', ( #32875 ), #9636, .T. ) ;
#38303=AXIS2_PLACEMENT_3D ( 'NONE', #17463, #28741, #17942 ) ;
#38306=CARTESIAN_POINT ( 'NONE',  ( 10.00000000000000000, 10.74501242461333028, -35.92658777277499382 ) ) ;
#38314=AXIS2_PLACEMENT_3D ( 'NONE', #2552, #24840, #10876 ) ;
#38336=ORIENTED_EDGE ( 'NONE', *, *, #38294, .F. ) ;
#38354=EDGE_CURVE ( 'NONE', #32798, #2634, #10859, .T. ) ;
#38366=DIRECTION ( 'NONE',  ( -1.000000000000000000, 0.000000000000000000, 0.000000000000000000 ) ) ;
#38368=EDGE_LOOP ( 'NONE', ( #3529, #47984, #43227, #38504 ) ) ;
#38386=DIRECTION ( 'NONE',  ( 0.000000000000000000, 1.000000000000000000, -9.787530781167598712E-16 ) ) ;
#38394=AXIS2_PLACEMENT_3D ( 'NONE', #9483, #5586, #38887 ) ;
#38402=DIRECTION ( 'NONE',  ( 0.000000000000000000, -0.4539904997395541320, 0.8910065241883640130 ) ) ;
#38409=ORIENTED_EDGE ( 'NONE', *, *, #5709, .F. ) ;
#38411=CIRCLE ( 'NONE', #27483, 16.00000000000000000 ) ;
#38417=CARTESIAN_POINT ( 'NONE',  ( 0.000000000000000000, -21.32104025579091910, -30.84782396557241313 ) ) ;
#38423=VERTEX_POINT ( 'NONE', #41680 ) ;
#38424=CIRCLE ( 'NONE', #35312, 42.00000000000000000 ) ;
#38435=CARTESIAN_POINT ( 'NONE',  ( 0.000000000000000000, -9.188173127307592836, 40.98264845739746676 ) ) ;
#38437=VERTEX_POINT ( 'NONE', #44388 ) ;
#38448=DIRECTION ( 'NONE',  ( 0.000000000000000000, 0.000000000000000000, 1.000000000000000000 ) ) ;
#38453=CARTESIAN_POINT ( 'NONE',  ( 10.00000000000000000, 0.000000000000000000, 0.000000000000000000 ) ) ;
#38465=CARTESIAN_POINT ( 'NONE',  ( 10.00000000000000000, 41.81611651403867569, -3.925862922255714871 ) ) ;
#38469=CARTESIAN_POINT ( 'NONE',  ( 0.000000000000000000, -12.26510123303284594, 35.53030884539080603 ) ) ;
#38480=EDGE_LOOP ( 'NONE', ( #9628, #1650, #20131, #41529 ) ) ;
#38482=CIRCLE ( 'NONE', #3284, 16.00000000000000000 ) ;
#38484=EDGE_CURVE ( 'NONE', #30556, #6444, #4715, .T. ) ;
#38489=CARTESIAN_POINT ( 'NONE',  ( 10.00000000000000000, 21.40280677340372151, 36.13751322684426981 ) ) ;
#38502=ORIENTED_EDGE ( 'NONE', *, *, #3310, .F. ) ;
#38504=ORIENTED_EDGE ( 'NONE', *, *, #10609, .T. ) ;
#38509=EDGE_CURVE ( 'NONE', #648, #500, #1770, .T. ) ;
#38523=CARTESIAN_POINT ( 'NONE',  ( 10.00000000000000000, 22.74946021919175720, -29.81001611430984255 ) ) ;
#38542=ORIENTED_EDGE ( 'NONE', *, *, #28888, .T. ) ;
#38547=AXIS2_PLACEMENT_3D ( 'NONE', #7887, #37751, #45327 ) ;
#38557=AXIS2_PLACEMENT_3D ( 'NONE', #24894, #35906, #25844 ) ;
#38570=CIRCLE ( 'NONE', #14347, 16.00000000000000000 ) ;
#38591=EDGE_CURVE ( 'NONE', #27090, #24152, #31333, .T. ) ;
#38605=EDGE_CURVE ( 'NONE', #10383, #337, #27237, .T. ) ;
#38611=VERTEX_POINT ( 'NONE', #38489 ) ;
#38616=VECTOR ( 'NONE', #37283, 1000.000000000000000 ) ;
#38626=AXIS2_PLACEMENT_3D ( 'NONE', #31427, #38998, #28212 ) ;
#38649=CIRCLE ( 'NONE', #42554, 42.00000000000000000 ) ;
#38662=DIRECTION ( 'NONE',  ( -1.000000000000000000, -0.000000000000000000, -0.000000000000000000 ) ) ;
#38663=DIRECTION ( 'NONE',  ( 1.000000000000000000, 0.000000000000000000, 0.000000000000000000 ) ) ;
#38664=CARTESIAN_POINT ( 'NONE',  ( 10.00000000000000000, -5.202137450156655518, 37.22597642581156663 ) ) ;
#38666=EDGE_CURVE ( 'NONE', #15492, #15162, #2241, .T. ) ;
#38675=DIRECTION ( 'NONE',  ( 0.000000000000000000, 0.4539904997395479702, -0.8910065241883673437 ) ) ;
#38677=DIRECTION ( 'NONE',  ( 0.000000000000000000, 0.000000000000000000, -1.000000000000000000 ) ) ;
#38679=EDGE_CURVE ( 'NONE', #500, #21510, #20337, .T. ) ;
#38685=ORIENTED_EDGE ( 'NONE', *, *, #45367, .T. ) ;
#38698=EDGE_CURVE ( 'NONE', #14780, #842, #32812, .T. ) ;
#38700=ORIENTED_EDGE ( 'NONE', *, *, #24217, .F. ) ;
#38741=CIRCLE ( 'NONE', #32512, 16.00000000000000000 ) ;
#38753=EDGE_CURVE ( 'NONE', #5836, #29992, #5940, .T. ) ;
#38788=CARTESIAN_POINT ( 'NONE',  ( 10.00000000000000000, -5.202137450156129717, -37.22597642581163768 ) ) ;
#38798=AXIS2_PLACEMENT_3D ( 'NONE', #33346, #27696, #31135 ) ;
#38804=VERTEX_POINT ( 'NONE', #21799 ) ;
#38826=FACE_OUTER_BOUND ( 'NONE', #31051, .T. ) ;
#38844=DIRECTION ( 'NONE',  ( -1.000000000000000000, 0.000000000000000000, 0.000000000000000000 ) ) ;
#38866=AXIS2_PLACEMENT_3D ( 'NONE', #42985, #9434, #24371 ) ;
#38876=DIRECTION ( 'NONE',  ( -1.000000000000000000, 0.000000000000000000, 0.000000000000000000 ) ) ;
#38879=CARTESIAN_POINT ( 'NONE',  ( 10.00000000000000178, 12.24744871391589029, 2.500000000000004441 ) ) ;
#38887=DIRECTION ( 'NONE',  ( 0.000000000000000000, 0.000000000000000000, 1.000000000000000000 ) ) ;
#38894=DIRECTION ( 'NONE',  ( -1.000000000000000000, 0.000000000000000000, 0.000000000000000000 ) ) ;
#38901=CIRCLE ( 'NONE', #12345, 42.00000000000000000 ) ;
#38924=VERTEX_POINT ( 'NONE', #34936 ) ;
#38935=CARTESIAN_POINT ( 'NONE',  ( 10.00000000000000000, -0.8828120875898013420, -37.48860685352291711 ) ) ;
#38938=VERTEX_POINT ( 'NONE', #13152 ) ;
#38956=AXIS2_PLACEMENT_3D ( 'NONE', #12508, #16414, #27439 ) ;
#38959=LINE ( 'NONE', #16912, #18444 ) ;
#38962=LINE ( 'NONE', #5419, #13653 ) ;
#38975=AXIS2_PLACEMENT_3D ( 'NONE', #40466, #44605, #14517 ) ;
#38976=EDGE_CURVE ( 'NONE', #2457, #13396, #23931, .T. ) ;
#38993=ORIENTED_EDGE ( 'NONE', *, *, #11424, .T. ) ;
#38998=DIRECTION ( 'NONE',  ( -1.000000000000000000, -0.000000000000000000, -0.000000000000000000 ) ) ;
#38999=CYLINDRICAL_SURFACE ( 'NONE', #48, 37.49900000000000233 ) ;
#39006=DIRECTION ( 'NONE',  ( -1.000000000000000000, -0.000000000000000000, 0.000000000000000000 ) ) ;
#39026=ORIENTED_EDGE ( 'NONE', *, *, #26687, .T. ) ;
#39043=ORIENTED_EDGE ( 'NONE', *, *, #42753, .F. ) ;
#39049=VECTOR ( 'NONE', #43370, 1000.000000000000000 ) ;
#39055=LINE ( 'NONE', #5771, #1894 ) ;
#39065=EDGE_CURVE ( 'NONE', #41267, #34876, #18027, .T. ) ;
#39073=VERTEX_POINT ( 'NONE', #32705 ) ;
#39077=CARTESIAN_POINT ( 'NONE',  ( 10.00000000000000000, 0.000000000000000000, 0.000000000000000000 ) ) ;
#39078=ADVANCED_FACE ( 'NONE', ( #29526 ), #3079, .T. ) ;
#39099=ORIENTED_EDGE ( 'NONE', *, *, #6866, .T. ) ;
#39112=DIRECTION ( 'NONE',  ( -1.000000000000000000, 0.000000000000000000, 0.000000000000000000 ) ) ;
#39113=AXIS2_PLACEMENT_3D ( 'NONE', #33431, #26086, #41034 ) ;
#39114=CARTESIAN_POINT ( 'NONE',  ( 10.00000000000000000, 40.68715046381944234, -10.41901085202036192 ) ) ;
#39118=CARTESIAN_POINT ( 'NONE',  ( 10.00000000000000000, -36.88895765772628010, -6.736453364083947015 ) ) ;
#39142=DIRECTION ( 'NONE',  ( -1.000000000000000000, -0.000000000000000000, 0.000000000000000000 ) ) ;
#39151=ORIENTED_EDGE ( 'NONE', *, *, #13915, .T. ) ;
#39196=VECTOR ( 'NONE', #19049, 1000.000000000000000 ) ;
#39197=ORIENTED_EDGE ( 'NONE', *, *, #32868, .T. ) ;
#39204=CIRCLE ( 'NONE', #29057, 37.49900000000000233 ) ;
#39220=VECTOR ( 'NONE', #3039, 1000.000000000000000 ) ;
#39222=CIRCLE ( 'NONE', #43139, 16.00000000000000000 ) ;
#39238=LINE ( 'NONE', #20628, #13605 ) ;
#39243=DIRECTION ( 'NONE',  ( 0.000000000000000000, -8.881784197001252323E-16, 1.000000000000000000 ) ) ;
#39260=DIRECTION ( 'NONE',  ( -1.000000000000000000, 0.000000000000000000, 0.000000000000000000 ) ) ;
#39281=VERTEX_POINT ( 'NONE', #34155 ) ;
#39283=CIRCLE ( 'NONE', #18164, 42.00000000000000000 ) ;
#39291=DIRECTION ( 'NONE',  ( -1.000000000000000000, 0.000000000000000000, 0.000000000000000000 ) ) ;
#39305=CARTESIAN_POINT ( 'NONE',  ( 4.999999999999999112, -10.41901085202050581, -40.68715046381939970 ) ) ;
#39308=DIRECTION ( 'NONE',  ( 0.000000000000000000, -0.8090169943749531134, 0.5877852522924653655 ) ) ;
#39324=ORIENTED_EDGE ( 'NONE', *, *, #38666, .T. ) ;
#39325=CIRCLE ( 'NONE', #13543, 37.49900000000000944 ) ;
#39354=AXIS2_PLACEMENT_3D ( 'NONE', #21776, #36702, #40624 ) ;
#39356=CARTESIAN_POINT ( 'NONE',  ( 0.000000000000000000, 0.000000000000000000, 0.000000000000000000 ) ) ;
#39358=DIRECTION ( 'NONE',  ( -1.000000000000000000, -0.000000000000000000, 0.000000000000000000 ) ) ;
#39362=VECTOR ( 'NONE', #13646, 1000.000000000000000 ) ;
#39363=AXIS2_PLACEMENT_3D ( 'NONE', #37146, #14643, #33468 ) ;
#39380=CIRCLE ( 'NONE', #37798, 37.49900000000001654 ) ;
#39399=VERTEX_POINT ( 'NONE', #9649 ) ;
#39405=VERTEX_POINT ( 'NONE', #6009 ) ;
#39412=LINE ( 'NONE', #20301, #47830 ) ;
#39422=ORIENTED_EDGE ( 'NONE', *, *, #41984, .F. ) ;
#39424=DIRECTION ( 'NONE',  ( 0.000000000000000000, 0.000000000000000000, 1.000000000000000000 ) ) ;
#39427=DIRECTION ( 'NONE',  ( -1.000000000000000000, 0.000000000000000000, 0.000000000000000000 ) ) ;
#39431=EDGE_CURVE ( 'NONE', #36936, #3893, #45912, .T. ) ;
#39442=DIRECTION ( 'NONE',  ( 0.000000000000000000, 0.000000000000000000, 1.000000000000000000 ) ) ;
#39468=AXIS2_PLACEMENT_3D ( 'NONE', #41028, #21686, #36605 ) ;
#39477=EDGE_CURVE ( 'NONE', #6451, #16066, #38411, .T. ) ;
#39505=CARTESIAN_POINT ( 'NONE',  ( -10.00000000000000000, 0.000000000000000000, 0.000000000000000000 ) ) ;
#39506=CARTESIAN_POINT ( 'NONE',  ( 10.00000000000000000, 15.48615015657582283, 39.04073710021349797 ) ) ;
#39510=CARTESIAN_POINT ( 'NONE',  ( 4.999999999999999112, 40.68715046381927891, 10.41901085202092858 ) ) ;
#39515=ORIENTED_EDGE ( 'NONE', *, *, #48228, .T. ) ;
#39521=ORIENTED_EDGE ( 'NONE', *, *, #6048, .F. ) ;
#39522=EDGE_CURVE ( 'NONE', #11209, #21073, #29004, .T. ) ;
#39524=CIRCLE ( 'NONE', #19975, 15.99999999999999822 ) ;
#39526=CIRCLE ( 'NONE', #45774, 15.99999999999999822 ) ;
#39530=EDGE_LOOP ( 'NONE', ( #20971, #3208, #47563, #29529 ) ) ;
#39535=CYLINDRICAL_SURFACE ( 'NONE', #20335, 16.00000000000000000 ) ;
#39540=DIRECTION ( 'NONE',  ( 0.000000000000000000, 0.000000000000000000, 1.000000000000000000 ) ) ;
#39548=ADVANCED_FACE ( 'NONE', ( #44160 ), #44398, .T. ) ;
#39553=DIRECTION ( 'NONE',  ( 0.000000000000000000, 0.000000000000000000, 1.000000000000000000 ) ) ;
#39562=CARTESIAN_POINT ( 'NONE',  ( 0.000000000000000000, 0.000000000000000000, 0.000000000000000000 ) ) ;
#39567=DIRECTION ( 'NONE',  ( 1.000000000000000000, 0.000000000000000000, -0.000000000000000000 ) ) ;
#39572=ORIENTED_EDGE ( 'NONE', *, *, #18760, .T. ) ;
#39574=VECTOR ( 'NONE', #37735, 1000.000000000000000 ) ;
#39576=CIRCLE ( 'NONE', #3602, 42.00000000000000000 ) ;
#39578=EDGE_LOOP ( 'NONE', ( #41025, #104, #26973, #2029 ) ) ;
#39580=EDGE_CURVE ( 'NONE', #41107, #13266, #42359, .T. ) ;
#39587=ORIENTED_EDGE ( 'NONE', *, *, #20229, .T. ) ;
#39588=CIRCLE ( 'NONE', #16933, 16.00000000000000000 ) ;
#39594=CIRCLE ( 'NONE', #9081, 16.00000000000000000 ) ;
#39600=CYLINDRICAL_SURFACE ( 'NONE', #21974, 42.00000000000000000 ) ;
#39607=ORIENTED_EDGE ( 'NONE', *, *, #48286, .F. ) ;
#39609=CYLINDRICAL_SURFACE ( 'NONE', #44429, 16.00000000000000000 ) ;
#39612=DIRECTION ( 'NONE',  ( -1.000000000000000000, 0.000000000000000000, -0.000000000000000000 ) ) ;
#39614=VECTOR ( 'NONE', #19106, 1000.000000000000000 ) ;
#39633=VECTOR ( 'NONE', #12756, 1000.000000000000000 ) ;
#39643=ADVANCED_FACE ( 'NONE', ( #13573 ), #14052, .T. ) ;
#39644=CIRCLE ( 'NONE', #9930, 42.00000000000000000 ) ;
#39660=DIRECTION ( 'NONE',  ( 0.000000000000000000, 0.7071067811865487940, -0.7071067811865462405 ) ) ;
#39661=ORIENTED_EDGE ( 'NONE', *, *, #35049, .F. ) ;
#39670=CARTESIAN_POINT ( 'NONE',  ( 0.000000000000000000, 37.22597642581158084, 10.79786254984347593 ) ) ;
#39684=CARTESIAN_POINT ( 'NONE',  ( 0.000000000000000000, 22.48208911017551515, -35.47612816024499693 ) ) ;
#39688=DIRECTION ( 'NONE',  ( -1.000000000000000000, 0.000000000000000000, -0.000000000000000000 ) ) ;
#39690=DIRECTION ( 'NONE',  ( -1.000000000000000000, -0.000000000000000000, -0.000000000000000000 ) ) ;
#39691=EDGE_CURVE ( 'NONE', #15851, #21692, #17325, .T. ) ;
#39693=VERTEX_POINT ( 'NONE', #572 ) ;
#39728=VERTEX_POINT ( 'NONE', #37771 ) ;
#39731=DIRECTION ( 'NONE',  ( -1.000000000000000000, -0.000000000000000000, 0.000000000000000000 ) ) ;
#39732=DIRECTION ( 'NONE',  ( -1.000000000000000000, -0.000000000000000000, 0.000000000000000000 ) ) ;
#39738=CARTESIAN_POINT ( 'NONE',  ( 0.000000000000000000, -10.74501242461307982, 35.92658777277507198 ) ) ;
#39739=LINE ( 'NONE', #17687, #27078 ) ;
#39752=EDGE_LOOP ( 'NONE', ( #38685, #5956, #43573, #45706 ) ) ;
#39757=VERTEX_POINT ( 'NONE', #34323 ) ;
#39759=EDGE_CURVE ( 'NONE', #22715, #42340, #41944, .T. ) ;
#39762=VECTOR ( 'NONE', #39358, 1000.000000000000000 ) ;
#39768=ORIENTED_EDGE ( 'NONE', *, *, #9485, .F. ) ;
#39769=CARTESIAN_POINT ( 'NONE',  ( 10.00000000000000000, -37.22597642581153821, -5.202137450156795850 ) ) ;
#39770=CARTESIAN_POINT ( 'NONE',  ( 10.00000000000000000, 39.04073710021366139, -15.48615015657542848 ) ) ;
#39773=ORIENTED_EDGE ( 'NONE', *, *, #9674, .F. ) ;
#39787=DIRECTION ( 'NONE',  ( 0.000000000000000000, 0.8090169943749486725, -0.5877852522924714718 ) ) ;
#39791=EDGE_LOOP ( 'NONE', ( #12744, #27791, #18645, #16122 ) ) ;
#39803=CARTESIAN_POINT ( 'NONE',  ( 10.00000000000000000, -27.75498641678764855, 31.52238457039589647 ) ) ;
#39812=EDGE_CURVE ( 'NONE', #25548, #31823, #5611, .T. ) ;
#39827=CARTESIAN_POINT ( 'NONE',  ( 10.00000000000000000, -37.48860685352291711, 0.8828120875899322373 ) ) ;
#39828=DIRECTION ( 'NONE',  ( -1.000000000000000000, 0.000000000000000000, 0.000000000000000000 ) ) ;
#39839=DIRECTION ( 'NONE',  ( -1.000000000000000000, 0.000000000000000000, 0.000000000000000000 ) ) ;
#39842=CARTESIAN_POINT ( 'NONE',  ( 0.000000000000000000, -21.40280677340398086, 36.13751322684410638 ) ) ;
#39874=ORIENTED_EDGE ( 'NONE', *, *, #35204, .T. ) ;
#39888=AXIS2_PLACEMENT_3D ( 'NONE', #2714, #10797, #6643 ) ;
#39893=DIRECTION ( 'NONE',  ( -1.000000000000000000, -0.000000000000000000, -0.000000000000000000 ) ) ;
#39899=DIRECTION ( 'NONE',  ( 0.000000000000000000, 0.000000000000000000, 1.000000000000000000 ) ) ;
#39911=ADVANCED_FACE ( 'NONE', ( #23247 ), #45770, .T. ) ;
#39936=CARTESIAN_POINT ( 'NONE',  ( 10.00000000000000000, 21.53537804866126137, -30.80686688396986028 ) ) ;
#39943=EDGE_CURVE ( 'NONE', #10918, #1493, #25273, .T. ) ;
#39944=ORIENTED_EDGE ( 'NONE', *, *, #13158, .F. ) ;
#39956=CARTESIAN_POINT ( 'NONE',  ( 10.00000000000000000, 22.48208911017500355, 35.47612816024531668 ) ) ;
#39961=AXIS2_PLACEMENT_3D ( 'NONE', #9069, #23746, #982 ) ;
#39967=ORIENTED_EDGE ( 'NONE', *, *, #1344, .F. ) ;
#39975=AXIS2_PLACEMENT_3D ( 'NONE', #31368, #46283, #1990 ) ;
#39976=DIRECTION ( 'NONE',  ( 0.000000000000000000, -0.7071067811865536790, 0.7071067811865414665 ) ) ;
#39978=FACE_OUTER_BOUND ( 'NONE', #6276, .T. ) ;
#39989=DIRECTION ( 'NONE',  ( 0.000000000000000000, -0.8090169943749531134, 0.5877852522924653655 ) ) ;
#39996=AXIS2_PLACEMENT_3D ( 'NONE', #16069, #8469, #23393 ) ;
#40017=LINE ( 'NONE', #48075, #46528 ) ;
#40019=LINE ( 'NONE', #40269, #39220 ) ;
#40026=CARTESIAN_POINT ( 'NONE',  ( 0.000000000000000000, 0.6853352020790449695, 37.58145647212454321 ) ) ;
#40032=DIRECTION ( 'NONE',  ( -1.000000000000000000, 0.000000000000000000, 0.000000000000000000 ) ) ;
#40033=DIRECTION ( 'NONE',  ( -1.000000000000000000, 0.000000000000000000, 0.000000000000000000 ) ) ;
#40041=CARTESIAN_POINT ( 'NONE',  ( 10.00000000000000000, -40.98264845739743834, -9.188173127307738497 ) ) ;
#40045=EDGE_LOOP ( 'NONE', ( #31743, #2777, #1931, #30312 ) ) ;
#40051=AXIS2_PLACEMENT_3D ( 'NONE', #35381, #34904, #31747 ) ;
#40066=DIRECTION ( 'NONE',  ( -1.000000000000000000, -0.000000000000000000, 0.000000000000000000 ) ) ;
#40075=DIRECTION ( 'NONE',  ( 0.000000000000000000, 0.000000000000000000, 1.000000000000000000 ) ) ;
#40076=CARTESIAN_POINT ( 'NONE',  ( 0.000000000000000000, 0.000000000000000000, 0.000000000000000000 ) ) ;
#40085=CARTESIAN_POINT ( 'NONE',  ( 10.00000000000000000, -12.42422080174614862, -35.38097989696524337 ) ) ;
#40093=AXIS2_PLACEMENT_3D ( 'NONE', #14002, #1607, #28921 ) ;
#40098=APPLICATION_CONTEXT ( 'automotive_design' ) ;
#40120=ADVANCED_FACE ( 'NONE', ( #24821 ), #5015, .T. ) ;
#40121=CARTESIAN_POINT ( 'NONE',  ( 10.00000000000000000, 3.925862922256160736, 41.81611651403863306 ) ) ;
#40143=DIRECTION ( 'NONE',  ( -1.000000000000000000, -0.000000000000000000, -0.000000000000000000 ) ) ;
#40161=ORIENTED_EDGE ( 'NONE', *, *, #3815, .F. ) ;
#40170=EDGE_CURVE ( 'NONE', #34957, #9900, #43249, .T. ) ;
#40174=CARTESIAN_POINT ( 'NONE',  ( 4.999999999999999112, -41.81611651403859042, -3.925862922256606602 ) ) ;
#40180=AXIS2_PLACEMENT_3D ( 'NONE', #30196, #45116, #22359 ) ;
#40186=ORIENTED_EDGE ( 'NONE', *, *, #41925, .T. ) ;
#40194=CIRCLE ( 'NONE', #306, 37.49900000000000233 ) ;
#40195=DIRECTION ( 'NONE',  ( -1.000000000000000000, -0.000000000000000000, -0.000000000000000000 ) ) ;
#40200=ORIENTED_EDGE ( 'NONE', *, *, #7571, .F. ) ;
#40214=DIRECTION ( 'NONE',  ( -1.000000000000000000, 0.000000000000000000, 0.000000000000000000 ) ) ;
#40218=DIRECTION ( 'NONE',  ( 0.000000000000000000, 0.000000000000000000, 1.000000000000000000 ) ) ;
#40239=AXIS2_PLACEMENT_3D ( 'NONE', #42930, #40695, #32857 ) ;
#40251=AXIS2_PLACEMENT_3D ( 'NONE', #31704, #46619, #43178 ) ;
#40259=CARTESIAN_POINT ( 'NONE',  ( 10.00000000000000000, 0.000000000000000000, 0.000000000000000000 ) ) ;
#40269=CARTESIAN_POINT ( 'NONE',  ( 5.000000000000000000, 22.48208911017551870, -35.47612816024499693 ) ) ;
#40308=CYLINDRICAL_SURFACE ( 'NONE', #46877, 16.00000000000000000 ) ;
#40314=ORIENTED_EDGE ( 'NONE', *, *, #6149, .F. ) ;
#40337=LINE ( 'NONE', #21712, #17300 ) ;
#40342=DIRECTION ( 'NONE',  ( -1.000000000000000000, -0.000000000000000000, 0.000000000000000000 ) ) ;
#40355=VERTEX_POINT ( 'NONE', #30425 ) ;
#40359=DIRECTION ( 'NONE',  ( 0.000000000000000000, -1.000000000000000000, -1.047444401652940007E-14 ) ) ;
#40363=EDGE_CURVE ( 'NONE', #47876, #8701, #37061, .T. ) ;
#40368=CIRCLE ( 'NONE', #20020, 42.00000000000000000 ) ;
#40376=DIRECTION ( 'NONE',  ( -1.000000000000000000, 0.000000000000000000, 0.000000000000000000 ) ) ;
#40378=ORIENTED_EDGE ( 'NONE', *, *, #3179, .T. ) ;
#40384=ORIENTED_EDGE ( 'NONE', *, *, #1034, .T. ) ;
#40391=FACE_OUTER_BOUND ( 'NONE', #30917, .T. ) ;
#40403=DIRECTION ( 'NONE',  ( -1.000000000000000000, -0.000000000000000000, -0.000000000000000000 ) ) ;
#40406=VERTEX_POINT ( 'NONE', #27003 ) ;
#40414=EDGE_CURVE ( 'NONE', #34957, #15686, #26014, .T. ) ;
#40415=VERTEX_POINT ( 'NONE', #3746 ) ;
#40416=AXIS2_PLACEMENT_3D ( 'NONE', #14360, #22433, #7505 ) ;
#40431=CARTESIAN_POINT ( 'NONE',  ( 10.00000000000000000, -25.88420570971419821, 27.13269053701087330 ) ) ;
#40450=ORIENTED_EDGE ( 'NONE', *, *, #19829, .T. ) ;
#40455=ORIENTED_EDGE ( 'NONE', *, *, #36950, .F. ) ;
#40456=DIRECTION ( 'NONE',  ( 0.000000000000000000, -0.5877852522924802425, 0.8090169943749422332 ) ) ;
#40457=DIRECTION ( 'NONE',  ( 0.000000000000000000, 0.1564344650402311743, -0.9876883405951377704 ) ) ;
#40460=ADVANCED_FACE ( 'NONE', ( #12316 ), #42892, .T. ) ;
#40466=CARTESIAN_POINT ( 'NONE',  ( 10.00000000000000000, 0.000000000000000000, 0.000000000000000000 ) ) ;
#40471=AXIS2_PLACEMENT_3D ( 'NONE', #12759, #1268, #19591 ) ;
#40490=ORIENTED_EDGE ( 'NONE', *, *, #25904, .T. ) ;
#40523=CIRCLE ( 'NONE', #17863, 37.49900000000001654 ) ;
#40524=DIRECTION ( 'NONE',  ( -1.000000000000000000, -0.000000000000000000, 0.000000000000000000 ) ) ;
#40531=ORIENTED_EDGE ( 'NONE', *, *, #15283, .T. ) ;
#40537=ORIENTED_EDGE ( 'NONE', *, *, #2472, .T. ) ;
#40547=EDGE_LOOP ( 'NONE', ( #40910, #28077, #27489, #28972 ) ) ;
#40552=ORIENTED_EDGE ( 'NONE', *, *, #23974, .F. ) ;
#40553=CARTESIAN_POINT ( 'NONE',  ( 0.000000000000000000, 0.000000000000000000, 0.000000000000000000 ) ) ;
#40565=EDGE_CURVE ( 'NONE', #47238, #15972, #8138, .T. ) ;
#40593=CARTESIAN_POINT ( 'NONE',  ( 10.00000000000000000, 0.000000000000000000, 0.000000000000000000 ) ) ;
#40604=DIRECTION ( 'NONE',  ( 0.000000000000000000, 0.000000000000000000, 1.000000000000000000 ) ) ;
#40612=AXIS2_PLACEMENT_3D ( 'NONE', #13262, #28428, #35773 ) ;
#40624=DIRECTION ( 'NONE',  ( 0.000000000000000000, 0.000000000000000000, 1.000000000000000000 ) ) ;
#40625=CARTESIAN_POINT ( 'NONE',  ( 0.000000000000000000, 39.04073710021366139, -15.48615015657542315 ) ) ;
#40635=CIRCLE ( 'NONE', #8595, 16.00000000000000355 ) ;
#40638=ORIENTED_EDGE ( 'NONE', *, *, #11154, .T. ) ;
#40665=DIRECTION ( 'NONE',  ( 1.000000000000000000, 0.000000000000000000, -0.000000000000000000 ) ) ;
#40666=ORIENTED_EDGE ( 'NONE', *, *, #32619, .T. ) ;
#40670=ORIENTED_EDGE ( 'NONE', *, *, #47263, .F. ) ;
#40678=DIRECTION ( 'NONE',  ( -1.000000000000000000, 0.000000000000000000, 0.000000000000000000 ) ) ;
#40679=CIRCLE ( 'NONE', #45348, 42.00000000000000000 ) ;
#40681=CARTESIAN_POINT ( 'NONE',  ( 10.00000000000000000, -4.992566952385247170, 37.16516213103275845 ) ) ;
#40689=DIRECTION ( 'NONE',  ( -1.000000000000000000, -0.000000000000000000, -0.000000000000000000 ) ) ;
#40691=CARTESIAN_POINT ( 'NONE',  ( 0.000000000000000000, -22.48208911017474065, -35.47612816024548721 ) ) ;
#40695=DIRECTION ( 'NONE',  ( -1.000000000000000000, -0.000000000000000000, -0.000000000000000000 ) ) ;
#40704=AXIS2_PLACEMENT_3D ( 'NONE', #31189, #27509, #20152 ) ;
#40717=VECTOR ( 'NONE', #42305, 1000.000000000000000 ) ;
#40721=CARTESIAN_POINT ( 'NONE',  ( 10.00000000000000000, 0.000000000000000000, 0.000000000000000000 ) ) ;
#40726=CARTESIAN_POINT ( 'NONE',  ( 0.000000000000000000, 0.000000000000000000, 0.000000000000000000 ) ) ;
#40729=EDGE_CURVE ( 'NONE', #8618, #39073, #11755, .T. ) ;
#40732=LINE ( 'NONE', #48076, #46148 ) ;
#40760=ADVANCED_FACE ( 'NONE', ( #15441 ), #4182, .T. ) ;
#40768=EDGE_CURVE ( 'NONE', #9305, #40415, #27415, .T. ) ;
#40778=CARTESIAN_POINT ( 'NONE',  ( 0.000000000000000000, -35.92658777277517856, 10.74501242461269257 ) ) ;
#40797=CARTESIAN_POINT ( 'NONE',  ( 10.00000000000000000, 16.23288003029497162, 33.80338159004289622 ) ) ;
#40798=DIRECTION ( 'NONE',  ( -1.000000000000000000, 0.000000000000000000, -0.000000000000000000 ) ) ;
#40802=ORIENTED_EDGE ( 'NONE', *, *, #6866, .F. ) ;
#40805=CYLINDRICAL_SURFACE ( 'NONE', #27517, 37.49900000000000233 ) ;
#40807=EDGE_CURVE ( 'NONE', #8701, #31375, #7365, .T. ) ;
#40808=DIRECTION ( 'NONE',  ( 0.000000000000000000, -0.3090169943749349057, -0.9510565162951576390 ) ) ;
#40814=CARTESIAN_POINT ( 'NONE',  ( 0.000000000000000000, 0.000000000000000000, 0.000000000000000000 ) ) ;
#40832=VERTEX_POINT ( 'NONE', #41152 ) ;
#40845=DIRECTION ( 'NONE',  ( -1.000000000000000000, 0.000000000000000000, 0.000000000000000000 ) ) ;
#40859=CARTESIAN_POINT ( 'NONE',  ( 10.00000000000000000, -37.22597642581153821, 10.79786254984320415 ) ) ;
#40863=DIRECTION ( 'NONE',  ( 0.000000000000000000, 1.000000000000000000, -9.787530781167598712E-16 ) ) ;
#40864=CARTESIAN_POINT ( 'NONE',  ( 0.000000000000000000, -26.79245525562690844, -32.34446384430000876 ) ) ;
#40870=CARTESIAN_POINT ( 'NONE',  ( 0.000000000000000000, 0.000000000000000000, 0.000000000000000000 ) ) ;
#40886=DIRECTION ( 'NONE',  ( -1.000000000000000000, 0.000000000000000000, 0.000000000000000000 ) ) ;
#40888=AXIS2_PLACEMENT_3D ( 'NONE', #20493, #35427, #16842 ) ;
#40906=ORIENTED_EDGE ( 'NONE', *, *, #36315, .F. ) ;
#40907=FACE_OUTER_BOUND ( 'NONE', #18103, .T. ) ;
#40909=AXIS2_PLACEMENT_3D ( 'NONE', #31215, #19934, #1350 ) ;
#40910=ORIENTED_EDGE ( 'NONE', *, *, #19208, .T. ) ;
#40913=ORIENTED_EDGE ( 'NONE', *, *, #18880, .F. ) ;
#40929=VECTOR ( 'NONE', #711, 1000.000000000000000 ) ;
#40930=CARTESIAN_POINT ( 'NONE',  ( 0.000000000000000000, 0.000000000000000000, 12.50000000000000000 ) ) ;
#40932=DIRECTION ( 'NONE',  ( -1.000000000000000000, -0.000000000000000000, 0.000000000000000000 ) ) ;
#40937=VECTOR ( 'NONE', #44951, 1000.000000000000000 ) ;
#40941=CARTESIAN_POINT ( 'NONE',  ( 10.00000000000000178, 0.000000000000000000, 12.50000000000000000 ) ) ;
#40943=ORIENTED_EDGE ( 'NONE', *, *, #18834, .T. ) ;
#40954=EDGE_CURVE ( 'NONE', #337, #22817, #69, .T. ) ;
#40963=CARTESIAN_POINT ( 'NONE',  ( 10.00000000000000000, 37.48860685352291000, 0.8828120875901893649 ) ) ;
#40970=VECTOR ( 'NONE', #14324, 1000.000000000000000 ) ;
#40977=EDGE_CURVE ( 'NONE', #23982, #35643, #24298, .T. ) ;
#40981=ORIENTED_EDGE ( 'NONE', *, *, #24021, .T. ) ;
#40985=FACE_OUTER_BOUND ( 'NONE', #12327, .T. ) ;
#40988=CARTESIAN_POINT ( 'NONE',  ( 10.00000000000000000, -35.95386929396264009, 10.96151621346475658 ) ) ;
#40990=ORIENTED_EDGE ( 'NONE', *, *, #12577, .F. ) ;
#41001=AXIS2_PLACEMENT_3D ( 'NONE', #11563, #3722, #8768 ) ;
#41024=VERTEX_POINT ( 'NONE', #36669 ) ;
#41025=ORIENTED_EDGE ( 'NONE', *, *, #1669, .T. ) ;
#41028=CARTESIAN_POINT ( 'NONE',  ( 10.00000000000000000, 0.000000000000000000, 0.000000000000000000 ) ) ;
#41029=EDGE_CURVE ( 'NONE', #500, #19660, #43065, .T. ) ;
#41034=DIRECTION ( 'NONE',  ( 0.000000000000000000, 0.000000000000000000, 1.000000000000000000 ) ) ;
#41036=ORIENTED_EDGE ( 'NONE', *, *, #37626, .T. ) ;
#41057=EDGE_LOOP ( 'NONE', ( #41315, #20349, #14845, #4505 ) ) ;
#41059=CARTESIAN_POINT ( 'NONE',  ( 0.000000000000000000, 5.202137450156389953, 37.22597642581160216 ) ) ;
#41060=AXIS2_PLACEMENT_3D ( 'NONE', #17219, #31461, #33128 ) ;
#41064=VERTEX_POINT ( 'NONE', #40121 ) ;
#41070=CIRCLE ( 'NONE', #44969, 37.49900000000000944 ) ;
#41076=EDGE_CURVE ( 'NONE', #42450, #22226, #2408, .T. ) ;
#41090=DIRECTION ( 'NONE',  ( -1.000000000000000000, -0.000000000000000000, 0.000000000000000000 ) ) ;
#41091=EDGE_LOOP ( 'NONE', ( #39521, #2124, #23934, #48238 ) ) ;
#41093=VERTEX_POINT ( 'NONE', #36441 ) ;
#41107=VERTEX_POINT ( 'NONE', #2654 ) ;
#41123=AXIS2_PLACEMENT_3D ( 'NONE', #42599, #8558, #9059 ) ;
#41152=CARTESIAN_POINT ( 'NONE',  ( 0.000000000000000000, 29.81001611431009479, 22.74946021919143391 ) ) ;
#41156=CARTESIAN_POINT ( 'NONE',  ( 0.000000000000000000, 35.92658777277510040, 10.74501242461294659 ) ) ;
#41165=ORIENTED_EDGE ( 'NONE', *, *, #7571, .T. ) ;
#41166=LINE ( 'NONE', #26706, #9383 ) ;
#41168=ADVANCED_FACE ( 'NONE', ( #13927 ), #28849, .T. ) ;
#41171=AXIS2_PLACEMENT_3D ( 'NONE', #27386, #27625, #12227 ) ;
#41179=DIRECTION ( 'NONE',  ( -1.000000000000000000, 0.000000000000000000, 0.000000000000000000 ) ) ;
#41188=DIRECTION ( 'NONE',  ( 0.000000000000000000, 0.000000000000000000, 1.000000000000000000 ) ) ;
#41195=DIRECTION ( 'NONE',  ( -1.000000000000000000, 0.000000000000000000, 0.000000000000000000 ) ) ;
#41199=CIRCLE ( 'NONE', #40416, 16.00000000000000000 ) ;
#41205=DIRECTION ( 'NONE',  ( -1.000000000000000000, 0.000000000000000000, -0.000000000000000000 ) ) ;
#41212=DIRECTION ( 'NONE',  ( -1.000000000000000000, -0.000000000000000000, -0.000000000000000000 ) ) ;
#41225=VERTEX_POINT ( 'NONE', #3874 ) ;
#41227=EDGE_CURVE ( 'NONE', #17771, #18736, #15613, .T. ) ;
#41230=DIRECTION ( 'NONE',  ( -1.000000000000000000, 0.000000000000000000, 0.000000000000000000 ) ) ;
#41235=CARTESIAN_POINT ( 'NONE',  ( 10.00000000000000000, -37.01155633439053361, -6.555932627142825986 ) ) ;
#41240=CARTESIAN_POINT ( 'NONE',  ( 5.000000000000000000, -39.04073710021356192, 15.48615015657568073 ) ) ;
#41247=DIRECTION ( 'NONE',  ( -1.000000000000000000, 0.000000000000000000, 0.000000000000000000 ) ) ;
#41249=CARTESIAN_POINT ( 'NONE',  ( 10.00000000000000000, 36.88895765772633695, 6.736453364083687667 ) ) ;
#41253=ORIENTED_EDGE ( 'NONE', *, *, #9905, .T. ) ;
#41256=CIRCLE ( 'NONE', #20137, 16.00000000000000000 ) ;
#41258=ORIENTED_EDGE ( 'NONE', *, *, #3128, .T. ) ;
#41267=VERTEX_POINT ( 'NONE', #33486 ) ;
#41277=ORIENTED_EDGE ( 'NONE', *, *, #25003, .T. ) ;
#41287=CARTESIAN_POINT ( 'NONE',  ( 0.000000000000000000, 0.000000000000000000, 0.000000000000000000 ) ) ;
#41310=CYLINDRICAL_SURFACE ( 'NONE', #39363, 42.00000000000000000 ) ;
#41315=ORIENTED_EDGE ( 'NONE', *, *, #21935, .T. ) ;
#41326=AXIS2_PLACEMENT_3D ( 'NONE', #35193, #43519, #31306 ) ;
#41330=VERTEX_POINT ( 'NONE', #16830 ) ;
#41341=CARTESIAN_POINT ( 'NONE',  ( 10.00000000000000000, -6.736453364083292428, -36.88895765772640800 ) ) ;
#41358=DIRECTION ( 'NONE',  ( -1.000000000000000000, -0.000000000000000000, 0.000000000000000000 ) ) ;
#41364=DIRECTION ( 'NONE',  ( 0.000000000000000000, -0.3090169943749549453, 0.9510565162951511997 ) ) ;
#41366=CIRCLE ( 'NONE', #34314, 42.00000000000000000 ) ;
#41390=CIRCLE ( 'NONE', #32742, 16.00000000000000000 ) ;
#41398=DIRECTION ( 'NONE',  ( -1.000000000000000000, 0.000000000000000000, -0.000000000000000000 ) ) ;
#41402=ORIENTED_EDGE ( 'NONE', *, *, #19165, .F. ) ;
#41409=DIRECTION ( 'NONE',  ( 0.000000000000000000, 0.4539904997395414754, 0.8910065241883706744 ) ) ;
#41413=LINE ( 'NONE', #10595, #22357 ) ;
#41431=CARTESIAN_POINT ( 'NONE',  ( 10.00000000000000000, 16.95692799528845640, -2.500000000000000000 ) ) ;
#41432=ORIENTED_EDGE ( 'NONE', *, *, #33102, .T. ) ;
#41437=DIRECTION ( 'NONE',  ( -1.000000000000000000, 0.000000000000000000, 0.000000000000000000 ) ) ;
#41452=ORIENTED_EDGE ( 'NONE', *, *, #34295, .T. ) ;
#41453=CARTESIAN_POINT ( 'NONE',  ( 10.00000000000000000, -17.80606268964516659, -33.00180498840066434 ) ) ;
#41460=CARTESIAN_POINT ( 'NONE',  ( 10.00000000000000000, -0.6853352020787742971, -37.58145647212455032 ) ) ;
#41465=CARTESIAN_POINT ( 'NONE',  ( 0.000000000000000000, -33.79645857604525361, 16.45098606841114730 ) ) ;
#41478=DIRECTION ( 'NONE',  ( 0.000000000000000000, 0.000000000000000000, 1.000000000000000000 ) ) ;
#41482=LINE ( 'NONE', #34128, #9846 ) ;
#41483=ORIENTED_EDGE ( 'NONE', *, *, #23228, .T. ) ;
#41501=ORIENTED_EDGE ( 'NONE', *, *, #4695, .F. ) ;
#41507=EDGE_CURVE ( 'NONE', #1214, #6623, #7142, .T. ) ;
#41511=VERTEX_POINT ( 'NONE', #43253 ) ;
#41513=ORIENTED_EDGE ( 'NONE', *, *, #20381, .T. ) ;
#41515=DIRECTION ( 'NONE',  ( 0.000000000000000000, 0.000000000000000000, 1.000000000000000000 ) ) ;
#41526=EDGE_CURVE ( 'NONE', #46150, #23361, #15734, .T. ) ;
#41529=ORIENTED_EDGE ( 'NONE', *, *, #243, .T. ) ;
#41531=AXIS2_PLACEMENT_3D ( 'NONE', #36563, #25061, #13829 ) ;
#41539=DIRECTION ( 'NONE',  ( -1.000000000000000000, -0.000000000000000000, 0.000000000000000000 ) ) ;
#41541=ORIENTED_EDGE ( 'NONE', *, *, #21784, .T. ) ;
#41554=ADVANCED_FACE ( 'NONE', ( #5820 ), #39600, .T. ) ;
#41556=AXIS2_PLACEMENT_3D ( 'NONE', #40721, #17232, #6717 ) ;
#41564=EDGE_CURVE ( 'NONE', #6127, #23361, #31409, .T. ) ;
#41570=ORIENTED_EDGE ( 'NONE', *, *, #32854, .F. ) ;
#41572=ADVANCED_FACE ( 'NONE', ( #33439, #15081 ), #132, .F. ) ;
#41573=ORIENTED_EDGE ( 'NONE', *, *, #30182, .F. ) ;
#41591=DIRECTION ( 'NONE',  ( 0.000000000000000000, 0.000000000000000000, -1.000000000000000000 ) ) ;
#41609=EDGE_CURVE ( 'NONE', #18326, #38804, #29807, .T. ) ;
#41622=FACE_BOUND ( 'NONE', #24519, .T. ) ;
#41632=CARTESIAN_POINT ( 'NONE',  ( 10.00000000000000000, 37.22597642581150268, 5.202137450157037435 ) ) ;
#41661=CIRCLE ( 'NONE', #47899, 15.99999999999999822 ) ;
#41671=CIRCLE ( 'NONE', #15077, 37.49900000000000944 ) ;
#41674=AXIS2_PLACEMENT_3D ( 'NONE', #32663, #7200, #47587 ) ;
#41680=CARTESIAN_POINT ( 'NONE',  ( 10.00000000000000000, 27.75498641678786527, -31.52238457039571173 ) ) ;
#41688=CIRCLE ( 'NONE', #26067, 37.49900000000000233 ) ;
#41701=DIRECTION ( 'NONE',  ( -1.000000000000000000, 0.000000000000000000, 0.000000000000000000 ) ) ;
#41713=CARTESIAN_POINT ( 'NONE',  ( 10.00000000000000000, 0.000000000000000000, 0.000000000000000000 ) ) ;
#41715=CIRCLE ( 'NONE', #33875, 16.00000000000000000 ) ;
#41717=CARTESIAN_POINT ( 'NONE',  ( 10.00000000000000000, 12.26510123303308752, -35.53030884539072787 ) ) ;
#41721=LINE ( 'NONE', #41249, #14381 ) ;
#41726=LINE ( 'NONE', #38060, #16660 ) ;
#41730=CIRCLE ( 'NONE', #28445, 16.00000000000000000 ) ;
#41734=AXIS2_PLACEMENT_3D ( 'NONE', #29957, #14795, #7199 ) ;
#41735=AXIS2_PLACEMENT_3D ( 'NONE', #32457, #9438, #39308 ) ;
#41736=ORIENTED_EDGE ( 'NONE', *, *, #29018, .T. ) ;
#41746=CIRCLE ( 'NONE', #20641, 16.00000000000000000 ) ;
#41755=EDGE_LOOP ( 'NONE', ( #11921, #12932, #41253, #12790 ) ) ;
#41757=LINE ( 'NONE', #858, #24760 ) ;
#41758=ORIENTED_EDGE ( 'NONE', *, *, #10111, .F. ) ;
#41763=DIRECTION ( 'NONE',  ( 0.000000000000000000, -0.5877852522924624790, -0.8090169943749550008 ) ) ;
#41774=ORIENTED_EDGE ( 'NONE', *, *, #38605, .T. ) ;
#41783=CYLINDRICAL_SURFACE ( 'NONE', #47418, 37.49900000000000233 ) ;
#41786=AXIS2_PLACEMENT_3D ( 'NONE', #20475, #13146, #9702 ) ;
#41793=FILL_AREA_STYLE_COLOUR ( '', #37453 ) ;
#41806=AXIS2_PLACEMENT_3D ( 'NONE', #11001, #26421, #8041 ) ;
#41809=CIRCLE ( 'NONE', #14448, 16.00000000000000000 ) ;
#41817=DIRECTION ( 'NONE',  ( -1.000000000000000000, -0.000000000000000000, -0.000000000000000000 ) ) ;
#41818=ORIENTED_EDGE ( 'NONE', *, *, #22104, .T. ) ;
#41822=CIRCLE ( 'NONE', #45036, 42.00000000000000000 ) ;
#41824=DIRECTION ( 'NONE',  ( -1.000000000000000000, -0.000000000000000000, 0.000000000000000000 ) ) ;
#41855=ORIENTED_EDGE ( 'NONE', *, *, #1863, .F. ) ;
#41875=DIRECTION ( 'NONE',  ( 0.000000000000000000, 0.9876883405951372152, 0.1564344650402346160 ) ) ;
#41894=DIRECTION ( 'NONE',  ( -1.000000000000000000, 0.000000000000000000, -0.000000000000000000 ) ) ;
#41903=DIRECTION ( 'NONE',  ( 0.000000000000000000, 0.000000000000000000, 1.000000000000000000 ) ) ;
#41905=DIRECTION ( 'NONE',  ( 1.000000000000000000, 0.000000000000000000, 0.000000000000000000 ) ) ;
#41916=DIRECTION ( 'NONE',  ( -1.000000000000000000, 0.000000000000000000, -0.000000000000000000 ) ) ;
#41919=CARTESIAN_POINT ( 'NONE',  ( 10.00000000000000000, -30.84782396557201878, -21.32104025579148399 ) ) ;
#41925=EDGE_CURVE ( 'NONE', #17779, #45724, #36016, .T. ) ;
#41928=DIRECTION ( 'NONE',  ( 0.000000000000000000, 0.3090169943749480619, -0.9510565162951533091 ) ) ;
#41932=AXIS2_PLACEMENT_3D ( 'NONE', #38137, #46203, #35175 ) ;
#41934=AXIS2_PLACEMENT_3D ( 'NONE', #37254, #3718, #3965 ) ;
#41944=LINE ( 'NONE', #22113, #43130 ) ;
#41946=CARTESIAN_POINT ( 'NONE',  ( 0.000000000000000000, 12.42422080174688404, -35.38097989696498047 ) ) ;
#41973=FACE_OUTER_BOUND ( 'NONE', #37235, .T. ) ;
#41982=ORIENTED_EDGE ( 'NONE', *, *, #1384, .F. ) ;
#41984=EDGE_CURVE ( 'NONE', #38924, #41064, #24365, .T. ) ;
#41990=DIRECTION ( 'NONE',  ( 0.000000000000000000, 0.000000000000000000, -1.000000000000000000 ) ) ;
#41998=CARTESIAN_POINT ( 'NONE',  ( 0.000000000000000000, 10.41901085202078292, 40.68715046381932865 ) ) ;
#42001=VECTOR ( 'NONE', #25510, 1000.000000000000000 ) ;
#42005=EDGE_CURVE ( 'NONE', #39757, #3577, #11897, .T. ) ;
#42022=EDGE_CURVE ( 'NONE', #41093, #18791, #38482, .T. ) ;
#42024=ADVANCED_FACE ( 'NONE', ( #37959 ), #45529, .T. ) ;
#42034=ORIENTED_EDGE ( 'NONE', *, *, #46245, .T. ) ;
#42040=ORIENTED_EDGE ( 'NONE', *, *, #40807, .T. ) ;
#42060=EDGE_LOOP ( 'NONE', ( #18183, #35387, #47610, #18412 ) ) ;
#42062=DIRECTION ( 'NONE',  ( 0.000000000000000000, -1.000000000000000000, -1.040834085586084257E-14 ) ) ;
#42077=EDGE_CURVE ( 'NONE', #25452, #20812, #28144, .T. ) ;
#42115=CARTESIAN_POINT ( 'NONE',  ( 10.00000000000000000, -33.00180498840060039, 17.80606268964528027 ) ) ;
#42123=AXIS2_PLACEMENT_3D ( 'NONE', #46745, #35717, #24213 ) ;
#42124=VERTEX_POINT ( 'NONE', #46990 ) ;
#42127=AXIS2_PLACEMENT_3D ( 'NONE', #42328, #31572, #5136 ) ;
#42128=DIRECTION ( 'NONE',  ( 1.000000000000000000, 0.000000000000000000, 0.000000000000000000 ) ) ;
#42130=DIRECTION ( 'NONE',  ( -1.000000000000000000, -0.000000000000000000, -0.000000000000000000 ) ) ;
#42139=AXIS2_PLACEMENT_3D ( 'NONE', #29317, #47433, #44245 ) ;
#42154=EDGE_CURVE ( 'NONE', #27731, #9130, #39412, .T. ) ;
#42157=DIRECTION ( 'NONE',  ( 1.000000000000000000, 0.000000000000000000, 0.000000000000000000 ) ) ;
#42159=CARTESIAN_POINT ( 'NONE',  ( 5.000000000000000000, -32.34446384429951138, -26.79245525562750530 ) ) ;
#42165=CARTESIAN_POINT ( 'NONE',  ( 10.00000000000000000, 33.80338159004283938, 16.23288003029508886 ) ) ;
#42174=EDGE_CURVE ( 'NONE', #46331, #26170, #14226, .T. ) ;
#42181=CARTESIAN_POINT ( 'NONE',  ( 10.00000000000000000, 22.48208911017551515, -35.47612816024499693 ) ) ;
#42182=DIRECTION ( 'NONE',  ( 0.000000000000000000, 0.000000000000000000, 1.000000000000000000 ) ) ;
#42188=CARTESIAN_POINT ( 'NONE',  ( 10.00000000000000000, 26.08949754953062694, -27.05870788708203989 ) ) ;
#42195=VERTEX_POINT ( 'NONE', #38935 ) ;
#42200=FACE_OUTER_BOUND ( 'NONE', #42852, .T. ) ;
#42205=ORIENTED_EDGE ( 'NONE', *, *, #41526, .T. ) ;
#42217=VERTEX_POINT ( 'NONE', #2912 ) ;
#42229=VECTOR ( 'NONE', #30148, 1000.000000000000000 ) ;
#42238=CARTESIAN_POINT ( 'NONE',  ( 0.000000000000000000, -17.67226234102849958, 33.17418723428301774 ) ) ;
#42249=CARTESIAN_POINT ( 'NONE',  ( 10.00000000000000000, 0.9569279952884557350, -2.499999999999984457 ) ) ;
#42256=CARTESIAN_POINT ( 'NONE',  ( 10.00000000000000000, -27.13269053701114331, 25.88420570971391754 ) ) ;
#42258=VECTOR ( 'NONE', #791, 1000.000000000000000 ) ;
#42267=EDGE_CURVE ( 'NONE', #42195, #28886, #2663, .T. ) ;
#42270=EDGE_CURVE ( 'NONE', #40406, #13266, #33260, .T. ) ;
#42299=CARTESIAN_POINT ( 'NONE',  ( 0.000000000000000000, 22.64427369931169309, 30.00120703465213623 ) ) ;
#42301=AXIS2_PLACEMENT_3D ( 'NONE', #8519, #1674, #16595 ) ;
#42304=CARTESIAN_POINT ( 'NONE',  ( 10.00000000000000000, 35.38097989696512968, 12.42422080174651100 ) ) ;
#42305=DIRECTION ( 'NONE',  ( -1.000000000000000000, 0.000000000000000000, 0.000000000000000000 ) ) ;
#42310=CARTESIAN_POINT ( 'NONE',  ( 10.00000000000000000, 0.000000000000000000, 0.000000000000000000 ) ) ;
#42313=DIRECTION ( 'NONE',  ( -1.000000000000000000, -0.000000000000000000, 0.000000000000000000 ) ) ;
#42316=DIRECTION ( 'NONE',  ( 0.000000000000000000, -0.8910065241883627918, -0.4539904997395569630 ) ) ;
#42325=CIRCLE ( 'NONE', #39961, 42.00000000000000000 ) ;
#42328=CARTESIAN_POINT ( 'NONE',  ( 0.000000000000000000, 17.67226234102826510, 33.17418723428314564 ) ) ;
#42330=FACE_OUTER_BOUND ( 'NONE', #10581, .T. ) ;
#42335=ADVANCED_FACE ( 'NONE', ( #13703 ), #36447, .T. ) ;
#42338=AXIS2_PLACEMENT_3D ( 'NONE', #23021, #45525, #12019 ) ;
#42340=VERTEX_POINT ( 'NONE', #26163 ) ;
#42343=ORIENTED_EDGE ( 'NONE', *, *, #24259, .F. ) ;
#42346=CARTESIAN_POINT ( 'NONE',  ( 4.999999999999999112, -40.98264845739755202, 9.188173127307159405 ) ) ;
#42357=CYLINDRICAL_SURFACE ( 'NONE', #29747, 16.00000000000000000 ) ;
#42359=CIRCLE ( 'NONE', #41556, 42.00000000000000000 ) ;
#42361=ORIENTED_EDGE ( 'NONE', *, *, #26048, .T. ) ;
#42362=ORIENTED_EDGE ( 'NONE', *, *, #40565, .F. ) ;
#42366=DIRECTION ( 'NONE',  ( 0.000000000000000000, 0.000000000000000000, 1.000000000000000000 ) ) ;
#42377=FACE_OUTER_BOUND ( 'NONE', #24107, .T. ) ;
#42380=DIRECTION ( 'NONE',  ( -1.000000000000000000, 0.000000000000000000, 0.000000000000000000 ) ) ;
#42402=ADVANCED_FACE ( 'NONE', ( #19044 ), #11960, .F. ) ;
#42404=EDGE_LOOP ( 'NONE', ( #47092, #14778, #3927, #14941 ) ) ;
#42408=ORIENTED_EDGE ( 'NONE', *, *, #4943, .F. ) ;
#42421=DIRECTION ( 'NONE',  ( -1.000000000000000000, 0.000000000000000000, 0.000000000000000000 ) ) ;
#42441=EDGE_CURVE ( 'NONE', #1423, #38423, #37752, .T. ) ;
#42450=VERTEX_POINT ( 'NONE', #29824 ) ;
#42452=EDGE_CURVE ( 'NONE', #43260, #26882, #30082, .T. ) ;
#42454=VECTOR ( 'NONE', #28176, 1000.000000000000000 ) ;
#42455=VERTEX_POINT ( 'NONE', #41341 ) ;
#42462=VECTOR ( 'NONE', #3699, 1000.000000000000000 ) ;
#42467=VERTEX_POINT ( 'NONE', #22721 ) ;
#42503=DIRECTION ( 'NONE',  ( 0.000000000000000000, 0.000000000000000000, 1.000000000000000000 ) ) ;
#42509=VECTOR ( 'NONE', #35764, 1000.000000000000000 ) ;
#42513=ORIENTED_EDGE ( 'NONE', *, *, #3713, .F. ) ;
#42514=EDGE_CURVE ( 'NONE', #8618, #14862, #27373, .T. ) ;
#42521=DIRECTION ( 'NONE',  ( -1.000000000000000000, 0.000000000000000000, 0.000000000000000000 ) ) ;
#42527=CARTESIAN_POINT ( 'NONE',  ( 5.000000000000000000, -26.79245525562738095, 32.34446384429961796 ) ) ;
#42552=CARTESIAN_POINT ( 'NONE',  ( 4.999999999999999112, 9.188173127307294408, 40.98264845739752360 ) ) ;
#42554=AXIS2_PLACEMENT_3D ( 'NONE', #20772, #10226, #6559 ) ;
#42559=LINE ( 'NONE', #39118, #39762 ) ;
#42570=DIRECTION ( 'NONE',  ( -1.000000000000000000, 0.000000000000000000, 0.000000000000000000 ) ) ;
#42571=DIRECTION ( 'NONE',  ( -1.000000000000000000, -0.000000000000000000, 0.000000000000000000 ) ) ;
#42573=EDGE_CURVE ( 'NONE', #28599, #46997, #47108, .T. ) ;
#42583=DIRECTION ( 'NONE',  ( -1.000000000000000000, 0.000000000000000000, 0.000000000000000000 ) ) ;
#42595=CIRCLE ( 'NONE', #5072, 16.00000000000000355 ) ;
#42599=CARTESIAN_POINT ( 'NONE',  ( 10.00000000000000000, 0.000000000000000000, 0.000000000000000000 ) ) ;
#42605=CARTESIAN_POINT ( 'NONE',  ( 0.000000000000000000, 0.000000000000000000, 0.000000000000000000 ) ) ;
#42607=ORIENTED_EDGE ( 'NONE', *, *, #45847, .F. ) ;
#42608=DIRECTION ( 'NONE',  ( -1.000000000000000000, -0.000000000000000000, 0.000000000000000000 ) ) ;
#42623=EDGE_CURVE ( 'NONE', #929, #46997, #39283, .T. ) ;
#42639=EDGE_LOOP ( 'NONE', ( #11243, #8429, #15393, #5062 ) ) ;
#42641=CIRCLE ( 'NONE', #16086, 12.50000000000000000 ) ;
#42643=DIRECTION ( 'NONE',  ( -1.000000000000000000, 0.000000000000000000, 0.000000000000000000 ) ) ;
#42648=CIRCLE ( 'NONE', #24640, 16.00000000000000000 ) ;
#42661=ORIENTED_EDGE ( 'NONE', *, *, #39943, .F. ) ;
#42664=EDGE_CURVE ( 'NONE', #19470, #19520, #15116, .T. ) ;
#42674=ORIENTED_EDGE ( 'NONE', *, *, #2445, .F. ) ;
#42675=CYLINDRICAL_SURFACE ( 'NONE', #38626, 42.00000000000000000 ) ;
#42677=CARTESIAN_POINT ( 'NONE',  ( 0.000000000000000000, -32.34446384429951138, -26.79245525562750530 ) ) ;
#42688=DIRECTION ( 'NONE',  ( 0.000000000000000000, 0.000000000000000000, -1.000000000000000000 ) ) ;
#42708=EDGE_CURVE ( 'NONE', #17599, #48430, #30725, .T. ) ;
#42716=ORIENTED_EDGE ( 'NONE', *, *, #11908, .F. ) ;
#42720=ORIENTED_EDGE ( 'NONE', *, *, #32509, .T. ) ;
#42721=CARTESIAN_POINT ( 'NONE',  ( 10.00000000000000000, -37.22597642581153821, 10.79786254984320415 ) ) ;
#42736=DIRECTION ( 'NONE',  ( -1.000000000000000000, 0.000000000000000000, 0.000000000000000000 ) ) ;
#42753=EDGE_CURVE ( 'NONE', #22493, #20399, #29181, .T. ) ;
#42757=ORIENTED_EDGE ( 'NONE', *, *, #8016, .F. ) ;
#42766=ORIENTED_EDGE ( 'NONE', *, *, #25564, .F. ) ;
#42769=VERTEX_POINT ( 'NONE', #45421 ) ;
#42770=ORIENTED_EDGE ( 'NONE', *, *, #13370, .T. ) ;
#42780=VERTEX_POINT ( 'NONE', #145 ) ;
#42785=EDGE_CURVE ( 'NONE', #25865, #17779, #43235, .T. ) ;
#42790=ORIENTED_EDGE ( 'NONE', *, *, #7931, .F. ) ;
#42792=CARTESIAN_POINT ( 'NONE',  ( 0.000000000000000000, 0.000000000000000000, 0.000000000000000000 ) ) ;
#42798=CARTESIAN_POINT ( 'NONE',  ( 10.00000000000000000, 33.17418723428333749, -17.67226234102790272 ) ) ;
#42800=ORIENTED_EDGE ( 'NONE', *, *, #113, .F. ) ;
#42801=ADVANCED_FACE ( 'NONE', ( #11181 ), #37602, .T. ) ;
#42818=CARTESIAN_POINT ( 'NONE',  ( 10.00000000000000000, 33.00180498840046539, 17.80606268964551120 ) ) ;
#42829=AXIS2_PLACEMENT_3D ( 'NONE', #42986, #38844, #20220 ) ;
#42852=EDGE_LOOP ( 'NONE', ( #30364, #41402, #36619, #3814 ) ) ;
#42870=CARTESIAN_POINT ( 'NONE',  ( 10.00000000000000000, 3.925862922256769583, -41.81611651403858332 ) ) ;
#42871=DIRECTION ( 'NONE',  ( 0.000000000000000000, 0.3090169943749482839, -0.9510565162951533091 ) ) ;
#42872=EDGE_CURVE ( 'NONE', #38126, #46920, #26103, .T. ) ;
#42873=DIRECTION ( 'NONE',  ( 0.000000000000000000, 0.000000000000000000, 1.000000000000000000 ) ) ;
#42884=AXIS2_PLACEMENT_3D ( 'NONE', #44845, #41195, #7648 ) ;
#42887=EDGE_LOOP ( 'NONE', ( #7842, #45961, #28208, #27406 ) ) ;
#42890=DIRECTION ( 'NONE',  ( -1.000000000000000000, 0.000000000000000000, -0.000000000000000000 ) ) ;
#42892=CYLINDRICAL_SURFACE ( 'NONE', #17489, 37.49900000000000233 ) ;
#42905=CARTESIAN_POINT ( 'NONE',  ( 0.000000000000000000, 21.53537804866081373, 30.80686688397018358 ) ) ;
#42907=ORIENTED_EDGE ( 'NONE', *, *, #42872, .T. ) ;
#42918=PRODUCT ( 'small gear_ISO - Spur gear 2M 40T 20PA 10FW ---S40A75H50L20.0N', 'small gear_ISO - Spur gear 2M 40T 20PA 10FW ---S40A75H50L20.0N', '', ( #27472 ) ) ;
#42925=CARTESIAN_POINT ( 'NONE',  ( 0.000000000000000000, 0.000000000000000000, 0.000000000000000000 ) ) ;
#42930=CARTESIAN_POINT ( 'NONE',  ( 10.00000000000000000, 0.000000000000000000, 0.000000000000000000 ) ) ;
#42932=ORIENTED_EDGE ( 'NONE', *, *, #16150, .F. ) ;
#42933=CARTESIAN_POINT ( 'NONE',  ( 0.000000000000000000, 0.000000000000000000, 0.000000000000000000 ) ) ;
#42941=EDGE_LOOP ( 'NONE', ( #17887, #5637, #2179, #625 ) ) ;
#42944=EDGE_CURVE ( 'NONE', #26170, #3496, #1832, .T. ) ;
#42961=ORIENTED_EDGE ( 'NONE', *, *, #31945, .T. ) ;
#42965=ORIENTED_EDGE ( 'NONE', *, *, #20166, .T. ) ;
#42968=EDGE_CURVE ( 'NONE', #5995, #19357, #36198, .T. ) ;
#42972=CYLINDRICAL_SURFACE ( 'NONE', #11754, 16.00000000000000000 ) ;
#42982=LINE ( 'NONE', #42249, #35286 ) ;
#42985=CARTESIAN_POINT ( 'NONE',  ( 10.00000000000000000, 12.26510123303259725, 35.53030884539089840 ) ) ;
#42986=CARTESIAN_POINT ( 'NONE',  ( 10.00000000000000000, 5.202137450156389953, 37.22597642581160216 ) ) ;
#42994=EDGE_CURVE ( 'NONE', #46829, #19329, #35126, .T. ) ;
#43003=CIRCLE ( 'NONE', #39888, 37.49900000000000233 ) ;
#43018=VERTEX_POINT ( 'NONE', #17012 ) ;
#43021=ORIENTED_EDGE ( 'NONE', *, *, #12594, .T. ) ;
#43025=CARTESIAN_POINT ( 'NONE',  ( 50.00005079999999680, 1.530808498934191521E-15, -12.50000000000000000 ) ) ;
#43031=DIRECTION ( 'NONE',  ( 0.000000000000000000, -0.8090169943749402348, -0.5877852522924830181 ) ) ;
#43034=DIRECTION ( 'NONE',  ( 0.000000000000000000, 0.000000000000000000, 1.000000000000000000 ) ) ;
#43053=ORIENTED_EDGE ( 'NONE', *, *, #45919, .F. ) ;
#43062=CARTESIAN_POINT ( 'NONE',  ( 0.000000000000000000, -41.91543099594819921, 2.663952781846001816 ) ) ;
#43064=DIRECTION ( 'NONE',  ( 0.000000000000000000, 0.000000000000000000, -1.000000000000000000 ) ) ;
#43065=CIRCLE ( 'NONE', #46976, 16.00000000000000000 ) ;
#43071=EDGE_CURVE ( 'NONE', #43945, #29887, #28418, .T. ) ;
#43087=ORIENTED_EDGE ( 'NONE', *, *, #45210, .T. ) ;
#43091=CARTESIAN_POINT ( 'NONE',  ( 10.00000000000000000, 0.000000000000000000, 0.000000000000000000 ) ) ;
#43098=DIRECTION ( 'NONE',  ( 1.000000000000000000, 0.000000000000000000, 0.000000000000000000 ) ) ;
#43099=CIRCLE ( 'NONE', #36063, 42.00000000000000000 ) ;
#43100=AXIS2_PLACEMENT_3D ( 'NONE', #20975, #35897, #28803 ) ;
#43101=EDGE_CURVE ( 'NONE', #48430, #34442, #1878, .T. ) ;
#43110=ORIENTED_EDGE ( 'NONE', *, *, #24973, .T. ) ;
#43130=VECTOR ( 'NONE', #33383, 1000.000000000000000 ) ;
#43133=DIRECTION ( 'NONE',  ( 0.000000000000000000, 0.000000000000000000, 1.000000000000000000 ) ) ;
#43139=AXIS2_PLACEMENT_3D ( 'NONE', #41059, #15100, #11185 ) ;
#43146=DIRECTION ( 'NONE',  ( -1.000000000000000000, 0.000000000000000000, 0.000000000000000000 ) ) ;
#43163=FACE_OUTER_BOUND ( 'NONE', #19432, .T. ) ;
#43165=EDGE_CURVE ( 'NONE', #26395, #18356, #30768, .T. ) ;
#43178=DIRECTION ( 'NONE',  ( 0.000000000000000000, 0.000000000000000000, 1.000000000000000000 ) ) ;
#43183=ORIENTED_EDGE ( 'NONE', *, *, #3002, .F. ) ;
#43204=DIRECTION ( 'NONE',  ( 1.000000000000000000, -0.000000000000000000, -0.000000000000000000 ) ) ;
#43210=ADVANCED_FACE ( 'NONE', ( #18924 ), #4274, .T. ) ;
#43212=ORIENTED_EDGE ( 'NONE', *, *, #16473, .F. ) ;
#43213=AXIS2_PLACEMENT_3D ( 'NONE', #4331, #11905, #12393 ) ;
#43214=CARTESIAN_POINT ( 'NONE',  ( 0.000000000000000000, 37.01155633439068282, -6.555932627142014191 ) ) ;
#43219=EDGE_CURVE ( 'NONE', #48358, #37278, #20620, .T. ) ;
#43227=ORIENTED_EDGE ( 'NONE', *, *, #24145, .T. ) ;
#43231=ORIENTED_EDGE ( 'NONE', *, *, #31330, .T. ) ;
#43235=CIRCLE ( 'NONE', #4940, 42.00000000000000000 ) ;
#43247=ORIENTED_EDGE ( 'NONE', *, *, #13061, .F. ) ;
#43249=CIRCLE ( 'NONE', #46400, 37.49900000000000233 ) ;
#43253=CARTESIAN_POINT ( 'NONE',  ( 10.00000000000000000, 0.8828120875900632436, 37.48860685352291000 ) ) ;
#43259=DIRECTION ( 'NONE',  ( 0.000000000000000000, 0.000000000000000000, 1.000000000000000000 ) ) ;
#43260=VERTEX_POINT ( 'NONE', #33622 ) ;
#43263=CARTESIAN_POINT ( 'NONE',  ( 0.000000000000000000, 35.47612816024523852, 22.48208911017513145 ) ) ;
#43264=DIRECTION ( 'NONE',  ( -1.000000000000000000, 0.000000000000000000, 0.000000000000000000 ) ) ;
#43271=ORIENTED_EDGE ( 'NONE', *, *, #36365, .T. ) ;
#43272=LINE ( 'NONE', #12946, #9273 ) ;
#43276=AXIS2_PLACEMENT_3D ( 'NONE', #10018, #36201, #24943 ) ;
#43285=CARTESIAN_POINT ( 'NONE',  ( 10.00000000000000000, 40.68715046381928602, 10.41901085202092503 ) ) ;
#43292=ORIENTED_EDGE ( 'NONE', *, *, #39759, .F. ) ;
#43302=CARTESIAN_POINT ( 'NONE',  ( -1.200000000000000030E-05, 16.95692799528845640, -2.500000000000000000 ) ) ;
#43303=ORIENTED_EDGE ( 'NONE', *, *, #42441, .T. ) ;
#43309=AXIS2_PLACEMENT_3D ( 'NONE', #5308, #1876, #17506 ) ;
#43316=AXIS2_PLACEMENT_3D ( 'NONE', #22533, #12424, #19739 ) ;
#43317=CIRCLE ( 'NONE', #22213, 37.49900000000000233 ) ;
#43319=DIRECTION ( 'NONE',  ( -1.000000000000000000, -0.000000000000000000, 0.000000000000000000 ) ) ;
#43325=DIRECTION ( 'NONE',  ( -1.000000000000000000, 0.000000000000000000, 0.000000000000000000 ) ) ;
#43329=ORIENTED_EDGE ( 'NONE', *, *, #3465, .F. ) ;
#43336=CARTESIAN_POINT ( 'NONE',  ( 10.00000000000000000, 0.000000000000000000, 0.000000000000000000 ) ) ;
#43337=CARTESIAN_POINT ( 'NONE',  ( 10.00000000000000000, 16.45098606841126454, 33.79645857604518966 ) ) ;
#43338=ORIENTED_EDGE ( 'NONE', *, *, #8425, .F. ) ;
#43351=DIRECTION ( 'NONE',  ( 0.000000000000000000, 0.7071067811865487940, -0.7071067811865462405 ) ) ;
#43362=CIRCLE ( 'NONE', #14417, 15.99999999999999467 ) ;
#43369=EDGE_LOOP ( 'NONE', ( #46771, #21388, #17787, #32099 ) ) ;
#43370=DIRECTION ( 'NONE',  ( -1.000000000000000000, 0.000000000000000000, -0.000000000000000000 ) ) ;
#43378=DIRECTION ( 'NONE',  ( 0.000000000000000000, 0.9510565162951521989, 0.3090169943749515591 ) ) ;
#43390=VERTEX_POINT ( 'NONE', #24075 ) ;
#43398=DIRECTION ( 'NONE',  ( -1.000000000000000000, 0.000000000000000000, 0.000000000000000000 ) ) ;
#43404=VECTOR ( 'NONE', #10308, 1000.000000000000000 ) ;
#43405=CARTESIAN_POINT ( 'NONE',  ( 0.000000000000000000, 26.08949754953024325, 27.05870788708241648 ) ) ;
#43413=DIRECTION ( 'NONE',  ( 0.000000000000000000, 0.000000000000000000, 1.000000000000000000 ) ) ;
#43432=ORIENTED_EDGE ( 'NONE', *, *, #22995, .F. ) ;
#43436=CIRCLE ( 'NONE', #27786, 15.99999999999999822 ) ;
#43485=CIRCLE ( 'NONE', #28625, 15.99999999999999645 ) ;
#43498=EDGE_CURVE ( 'NONE', #35718, #18061, #44524, .T. ) ;
#43509=CARTESIAN_POINT ( 'NONE',  ( 10.00000000000000000, 22.74946021919175720, -29.81001611430984255 ) ) ;
#43515=AXIS2_PLACEMENT_3D ( 'NONE', #12268, #31110, #8339 ) ;
#43517=DIRECTION ( 'NONE',  ( -1.000000000000000000, 0.000000000000000000, 0.000000000000000000 ) ) ;
#43519=DIRECTION ( 'NONE',  ( -1.000000000000000000, -0.000000000000000000, -0.000000000000000000 ) ) ;
#43527=CARTESIAN_POINT ( 'NONE',  ( 10.00000000000000000, 0.000000000000000000, 0.000000000000000000 ) ) ;
#43541=CIRCLE ( 'NONE', #21633, 37.49900000000000944 ) ;
#43552=EDGE_CURVE ( 'NONE', #33236, #32480, #39238, .T. ) ;
#43561=CARTESIAN_POINT ( 'NONE',  ( 0.000000000000000000, -30.00120703465189465, -22.64427369931201639 ) ) ;
#43562=CARTESIAN_POINT ( 'NONE',  ( 5.000000000000000000, 39.04073710021344112, 15.48615015657596850 ) ) ;
#43573=ORIENTED_EDGE ( 'NONE', *, *, #21833, .F. ) ;
#43575=CARTESIAN_POINT ( 'NONE',  ( 10.00000000000000000, -30.00120703465189465, -22.64427369931201639 ) ) ;
#43583=DIRECTION ( 'NONE',  ( 0.000000000000000000, 0.5877852522924744694, -0.8090169943749465631 ) ) ;
#43587=ORIENTED_EDGE ( 'NONE', *, *, #40729, .F. ) ;
#43612=VERTEX_POINT ( 'NONE', #45020 ) ;
#43616=CARTESIAN_POINT ( 'NONE',  ( 4.999999999999999112, 41.81611651403868990, -3.925862922255709542 ) ) ;
#43630=DIRECTION ( 'NONE',  ( 0.000000000000000000, 0.000000000000000000, 1.000000000000000000 ) ) ;
#43632=DIRECTION ( 'NONE',  ( -1.000000000000000000, -0.000000000000000000, 0.000000000000000000 ) ) ;
#43639=DIRECTION ( 'NONE',  ( 1.000000000000000000, 0.000000000000000000, 0.000000000000000000 ) ) ;
#43664=ADVANCED_FACE ( 'NONE', ( #208 ), #45255, .T. ) ;
#43674=CARTESIAN_POINT ( 'NONE',  ( 0.000000000000000000, 0.000000000000000000, 0.000000000000000000 ) ) ;
#43679=ORIENTED_EDGE ( 'NONE', *, *, #46356, .T. ) ;
#43688=DIRECTION ( 'NONE',  ( -1.000000000000000000, -0.000000000000000000, 0.000000000000000000 ) ) ;
#43695=DIRECTION ( 'NONE',  ( -1.000000000000000000, -0.000000000000000000, -0.000000000000000000 ) ) ;
#43696=DIRECTION ( 'NONE',  ( -1.000000000000000000, -0.000000000000000000, -0.000000000000000000 ) ) ;
#43700=CARTESIAN_POINT ( 'NONE',  ( 0.000000000000000000, 35.38097989696528600, -12.42422080174602605 ) ) ;
#43701=ORIENTED_EDGE ( 'NONE', *, *, #22873, .F. ) ;
#43707=EDGE_CURVE ( 'NONE', #32864, #3407, #18275, .T. ) ;
#43711=ORIENTED_EDGE ( 'NONE', *, *, #2987, .T. ) ;
#43713=EDGE_CURVE ( 'NONE', #11050, #45431, #19116, .T. ) ;
#43718=ORIENTED_EDGE ( 'NONE', *, *, #8552, .T. ) ;
#43723=DIRECTION ( 'NONE',  ( -1.000000000000000000, -0.000000000000000000, -0.000000000000000000 ) ) ;
#43729=VERTEX_POINT ( 'NONE', #48349 ) ;
#43734=DIRECTION ( 'NONE',  ( 0.000000000000000000, 0.000000000000000000, 1.000000000000000000 ) ) ;
#43742=DIRECTION ( 'NONE',  ( 0.000000000000000000, 0.8910065241883656784, 0.4539904997395510788 ) ) ;
#43745=ADVANCED_FACE ( 'NONE', ( #24450 ), #6518, .T. ) ;
#43746=CYLINDRICAL_SURFACE ( 'NONE', #23557, 16.00000000000000000 ) ;
#43749=ORIENTED_EDGE ( 'NONE', *, *, #24386, .T. ) ;
#43756=AXIS2_PLACEMENT_3D ( 'NONE', #11734, #22739, #30342 ) ;
#43776=ORIENTED_EDGE ( 'NONE', *, *, #9125, .T. ) ;
#43781=AXIS2_PLACEMENT_3D ( 'NONE', #25475, #36009, #43378 ) ;
#43816=DIRECTION ( 'NONE',  ( 0.000000000000000000, 0.000000000000000000, -1.000000000000000000 ) ) ;
#43826=EDGE_CURVE ( 'NONE', #41225, #14780, #33956, .T. ) ;
#43827=CARTESIAN_POINT ( 'NONE',  ( 5.000000000000000000, 22.48208911017500355, 35.47612816024530957 ) ) ;
#43851=EDGE_CURVE ( 'NONE', #9070, #1962, #10530, .T. ) ;
#43852=CARTESIAN_POINT ( 'NONE',  ( 10.00000000000000000, 35.95386929396241271, 10.96151621346552751 ) ) ;
#43862=AXIS2_PLACEMENT_3D ( 'NONE', #22483, #11479, #15392 ) ;
#43875=CARTESIAN_POINT ( 'NONE',  ( 10.00000000000000000, 0.000000000000000000, 0.000000000000000000 ) ) ;
#43882=DIRECTION ( 'NONE',  ( -1.000000000000000000, -0.000000000000000000, 0.000000000000000000 ) ) ;
#43888=VERTEX_POINT ( 'NONE', #33655 ) ;
#43896=VECTOR ( 'NONE', #20192, 1000.000000000000000 ) ;
#43903=DIRECTION ( 'NONE',  ( -1.000000000000000000, 0.000000000000000000, 0.000000000000000000 ) ) ;
#43913=ORIENTED_EDGE ( 'NONE', *, *, #9674, .T. ) ;
#43922=ORIENTED_EDGE ( 'NONE', *, *, #31801, .F. ) ;
#43945=VERTEX_POINT ( 'NONE', #28521 ) ;
#43960=ORIENTED_EDGE ( 'NONE', *, *, #9905, .F. ) ;
#43964=AXIS2_PLACEMENT_3D ( 'NONE', #26663, #22507, #41591 ) ;
#43966=DIRECTION ( 'NONE',  ( 0.000000000000000000, 0.000000000000000000, 1.000000000000000000 ) ) ;
#43980=CARTESIAN_POINT ( 'NONE',  ( 10.00000000000000000, 35.95386929396256903, -10.96151621346501237 ) ) ;
#43993=AXIS2_PLACEMENT_3D ( 'NONE', #46301, #5198, #20112 ) ;
#43999=CARTESIAN_POINT ( 'NONE',  ( 0.000000000000000000, 29.81001611431041098, -22.74946021919100403 ) ) ;
#44003=CARTESIAN_POINT ( 'NONE',  ( 0.000000000000000000, 0.000000000000000000, 0.000000000000000000 ) ) ;
#44005=EDGE_LOOP ( 'NONE', ( #16617, #21532, #35776, #26711 ) ) ;
#44039=ORIENTED_EDGE ( 'NONE', *, *, #29221, .F. ) ;
#44044=CARTESIAN_POINT ( 'NONE',  ( 10.00000000000000000, -25.88420570971381807, -27.13269053701123212 ) ) ;
#44049=CARTESIAN_POINT ( 'NONE',  ( 10.00000000000000000, 35.53030884539084866, 12.26510123303271982 ) ) ;
#44051=CYLINDRICAL_SURFACE ( 'NONE', #10139, 16.00000000000000000 ) ;
#44076=EDGE_LOOP ( 'NONE', ( #42034, #4541, #838, #13030 ) ) ;
#44092=DIRECTION ( 'NONE',  ( 1.000000000000000000, -0.000000000000000000, 0.000000000000000000 ) ) ;
#44118=DIRECTION ( 'NONE',  ( -1.000000000000000000, -0.000000000000000000, 0.000000000000000000 ) ) ;
#44125=CARTESIAN_POINT ( 'NONE',  ( 0.000000000000000000, 0.000000000000000000, 0.000000000000000000 ) ) ;
#44136=VECTOR ( 'NONE', #33402, 1000.000000000000000 ) ;
#44147=ORIENTED_EDGE ( 'NONE', *, *, #5534, .F. ) ;
#44151=EDGE_LOOP ( 'NONE', ( #33386, #46151, #25063, #47558 ) ) ;
#44155=ORIENTED_EDGE ( 'NONE', *, *, #12143, .T. ) ;
#44160=FACE_OUTER_BOUND ( 'NONE', #28262, .T. ) ;
#44173=DIRECTION ( 'NONE',  ( -1.000000000000000000, -0.000000000000000000, 0.000000000000000000 ) ) ;
#44182=DIRECTION ( 'NONE',  ( 0.000000000000000000, 0.000000000000000000, 1.000000000000000000 ) ) ;
#44192=CIRCLE ( 'NONE', #17630, 16.00000000000000000 ) ;
#44195=EDGE_CURVE ( 'NONE', #48169, #37035, #40017, .T. ) ;
#44227=DIRECTION ( 'NONE',  ( -1.000000000000000000, -0.000000000000000000, 0.000000000000000000 ) ) ;
#44230=LINE ( 'NONE', #48134, #4174 ) ;
#44237=VERTEX_POINT ( 'NONE', #2798 ) ;
#44245=DIRECTION ( 'NONE',  ( 0.000000000000000000, 0.000000000000000000, 1.000000000000000000 ) ) ;
#44260=DIRECTION ( 'NONE',  ( 1.000000000000000000, 0.000000000000000000, 0.000000000000000000 ) ) ;
#44267=AXIS2_PLACEMENT_3D ( 'NONE', #44817, #11772, #26703 ) ;
#44270=DIRECTION ( 'NONE',  ( 1.000000000000000000, 0.000000000000000000, 0.000000000000000000 ) ) ;
#44273=EDGE_CURVE ( 'NONE', #6623, #5626, #1053, .T. ) ;
#44274=ORIENTED_EDGE ( 'NONE', *, *, #21102, .T. ) ;
#44279=ORIENTED_EDGE ( 'NONE', *, *, #24588, .F. ) ;
#44286=CARTESIAN_POINT ( 'NONE',  ( 5.000000000000000000, 31.52238457039599595, 27.75498641678753842 ) ) ;
#44290=LINE ( 'NONE', #3397, #8954 ) ;
#44292=DIRECTION ( 'NONE',  ( 0.000000000000000000, 0.000000000000000000, 1.000000000000000000 ) ) ;
#44295=DIRECTION ( 'NONE',  ( 0.000000000000000000, -0.9876883405951393247, 0.1564344650402207104 ) ) ;
#44306=ORIENTED_EDGE ( 'NONE', *, *, #42022, .F. ) ;
#44309=CIRCLE ( 'NONE', #12288, 42.00000000000000000 ) ;
#44315=EDGE_CURVE ( 'NONE', #18326, #22246, #44947, .T. ) ;
#44324=AXIS2_PLACEMENT_3D ( 'NONE', #478, #38663, #33996 ) ;
#44350=DIRECTION ( 'NONE',  ( -1.000000000000000000, -0.000000000000000000, -0.000000000000000000 ) ) ;
#44358=AXIS2_PLACEMENT_3D ( 'NONE', #46095, #27743, #8877 ) ;
#44362=CARTESIAN_POINT ( 'NONE',  ( 0.000000000000000000, 40.98264845739763018, -9.188173127306864529 ) ) ;
#44371=ORIENTED_EDGE ( 'NONE', *, *, #28363, .T. ) ;
#44375=ADVANCED_FACE ( 'NONE', ( #37540 ), #8167, .T. ) ;
#44382=EDGE_CURVE ( 'NONE', #45431, #40832, #11841, .T. ) ;
#44388=CARTESIAN_POINT ( 'NONE',  ( 10.00000000000000000, 33.80338159004307386, -16.23288003029461279 ) ) ;
#44398=CYLINDRICAL_SURFACE ( 'NONE', #25886, 16.00000000000000000 ) ;
#44407=CARTESIAN_POINT ( 'NONE',  ( 5.000000000000000000, -38.55633173626998911, -16.65560815589452304 ) ) ;
#44426=CARTESIAN_POINT ( 'NONE',  ( 4.999999999999999112, 41.81611651403861885, 3.925862922256313503 ) ) ;
#44427=DIRECTION ( 'NONE',  ( 1.000000000000000000, -0.000000000000000000, -0.000000000000000000 ) ) ;
#44429=AXIS2_PLACEMENT_3D ( 'NONE', #6298, #21210, #21703 ) ;
#44433=ADVANCED_FACE ( 'NONE', ( #32140 ), #42675, .T. ) ;
#44441=CARTESIAN_POINT ( 'NONE',  ( 10.00000000000000000, 17.67226234102826510, 33.17418723428314564 ) ) ;
#44449=EDGE_LOOP ( 'NONE', ( #10198, #47002, #11480, #43776 ) ) ;
#44456=VERTEX_POINT ( 'NONE', #16958 ) ;
#44458=CIRCLE ( 'NONE', #17100, 37.49900000000000233 ) ;
#44462=CARTESIAN_POINT ( 'NONE',  ( 10.00000000000000000, 0.000000000000000000, 0.000000000000000000 ) ) ;
#44476=CARTESIAN_POINT ( 'NONE',  ( -10.00000000000000000, 0.000000000000000000, 0.000000000000000000 ) ) ;
#44479=CYLINDRICAL_SURFACE ( 'NONE', #42139, 42.00000000000000000 ) ;
#44486=CARTESIAN_POINT ( 'NONE',  ( 10.00000000000000000, -37.16516213103273714, -4.992566952385376844 ) ) ;
#44488=EDGE_CURVE ( 'NONE', #41511, #38924, #41730, .T. ) ;
#44494=EDGE_LOOP ( 'NONE', ( #30334, #44847, #47303, #20778 ) ) ;
#44509=CARTESIAN_POINT ( 'NONE',  ( 0.000000000000000000, -38.55633173627022359, 16.65560815589396526 ) ) ;
#44524=LINE ( 'NONE', #5705, #8145 ) ;
#44530=LINE ( 'NONE', #25921, #32303 ) ;
#44562=DIRECTION ( 'NONE',  ( -1.000000000000000000, -0.000000000000000000, -0.000000000000000000 ) ) ;
#44563=CIRCLE ( 'NONE', #3117, 16.00000000000000711 ) ;
#44571=LINE ( 'NONE', #37229, #42462 ) ;
#44572=CYLINDRICAL_SURFACE ( 'NONE', #44267, 37.49900000000000233 ) ;
#44578=VERTEX_POINT ( 'NONE', #47305 ) ;
#44592=CARTESIAN_POINT ( 'NONE',  ( 10.00000000000000000, 4.992566952384984269, 37.16516213103279398 ) ) ;
#44593=AXIS2_PLACEMENT_3D ( 'NONE', #25595, #18250, #33190 ) ;
#44605=DIRECTION ( 'NONE',  ( -1.000000000000000000, -0.000000000000000000, 0.000000000000000000 ) ) ;
#44606=CIRCLE ( 'NONE', #1635, 15.99999999999999822 ) ;
#44611=VECTOR ( 'NONE', #22549, 1000.000000000000000 ) ;
#44617=EDGE_LOOP ( 'NONE', ( #7288, #12189, #28799, #3318 ) ) ;
#44623=CARTESIAN_POINT ( 'NONE',  ( 10.00000000000000000, 0.000000000000000000, 0.000000000000000000 ) ) ;
#44640=ORIENTED_EDGE ( 'NONE', *, *, #43219, .F. ) ;
#44664=CARTESIAN_POINT ( 'NONE',  ( 0.000000000000000000, -6.555932627142143865, -37.01155633439065440 ) ) ;
#44665=DIRECTION ( 'NONE',  ( -1.000000000000000000, 0.000000000000000000, -0.000000000000000000 ) ) ;
#44668=AXIS2_PLACEMENT_3D ( 'NONE', #32243, #17056, #43734 ) ;
#44683=ORIENTED_EDGE ( 'NONE', *, *, #1669, .F. ) ;
#44694=ORIENTED_EDGE ( 'NONE', *, *, #19488, .F. ) ;
#44706=FACE_OUTER_BOUND ( 'NONE', #47395, .T. ) ;
#44712=EDGE_CURVE ( 'NONE', #3893, #32798, #27693, .T. ) ;
#44729=VECTOR ( 'NONE', #23743, 1000.000000000000000 ) ;
#44744=CARTESIAN_POINT ( 'NONE',  ( 10.00000000000000000, 22.64427369931169309, 30.00120703465213623 ) ) ;
#44751=ADVANCED_FACE ( 'NONE', ( #22560 ), #3712, .T. ) ;
#44752=CARTESIAN_POINT ( 'NONE',  ( 10.00000000000000000, 30.84782396557218931, 21.32104025579126017 ) ) ;
#44759=CYLINDRICAL_SURFACE ( 'NONE', #27461, 37.49900000000000233 ) ;
#44764=DIRECTION ( 'NONE',  ( 1.000000000000000000, 0.000000000000000000, 0.000000000000000000 ) ) ;
#44775=AXIS2_PLACEMENT_3D ( 'NONE', #15038, #3773, #6730 ) ;
#44779=DIRECTION ( 'NONE',  ( 0.000000000000000000, 0.000000000000000000, -1.000000000000000000 ) ) ;
#44811=LINE ( 'NONE', #11296, #43404 ) ;
#44817=CARTESIAN_POINT ( 'NONE',  ( 10.00000000000000000, 0.000000000000000000, 0.000000000000000000 ) ) ;
#44818=EDGE_CURVE ( 'NONE', #47647, #20, #353, .T. ) ;
#44823=DIRECTION ( 'NONE',  ( 0.000000000000000000, 0.000000000000000000, -1.000000000000000000 ) ) ;
#44836=LINE ( 'NONE', #40681, #21565 ) ;
#44845=CARTESIAN_POINT ( 'NONE',  ( 10.00000000000000000, -35.95386929396248377, -10.96151621346525751 ) ) ;
#44847=ORIENTED_EDGE ( 'NONE', *, *, #13370, .F. ) ;
#44855=VECTOR ( 'NONE', #10547, 1000.000000000000000 ) ;
#44864=EDGE_CURVE ( 'NONE', #19937, #7880, #24485, .T. ) ;
#44871=AXIS2_PLACEMENT_3D ( 'NONE', #2096, #16299, #45922 ) ;
#44876=DIRECTION ( 'NONE',  ( -1.000000000000000000, 0.000000000000000000, -0.000000000000000000 ) ) ;
#44887=CARTESIAN_POINT ( 'NONE',  ( 0.000000000000000000, 37.58145647212455032, -0.6853352020786441789 ) ) ;
#44888=AXIS2_PLACEMENT_3D ( 'NONE', #12971, #23721, #38677 ) ;
#44889=DIRECTION ( 'NONE',  ( -1.000000000000000000, 0.000000000000000000, -0.000000000000000000 ) ) ;
#44894=FACE_OUTER_BOUND ( 'NONE', #46274, .T. ) ;
#44896=CARTESIAN_POINT ( 'NONE',  ( -1.200000000000000030E-05, 0.9569279952884607310, 2.500000000000015543 ) ) ;
#44900=CARTESIAN_POINT ( 'NONE',  ( 10.00000000000000000, -37.16516213103280108, 4.992566952384862589 ) ) ;
#44910=CARTESIAN_POINT ( 'NONE',  ( 0.000000000000000000, 32.34446384429971033, 26.79245525562726371 ) ) ;
#44911=LINE ( 'NONE', #22870, #14538 ) ;
#44925=VECTOR ( 'NONE', #6369, 1000.000000000000000 ) ;
#44938=ORIENTED_EDGE ( 'NONE', *, *, #20597, .F. ) ;
#44941=CIRCLE ( 'NONE', #23844, 37.49900000000000944 ) ;
#44947=CIRCLE ( 'NONE', #45757, 16.00000000000000000 ) ;
#44949=FACE_OUTER_BOUND ( 'NONE', #22079, .T. ) ;
#44950=DIRECTION ( 'NONE',  ( -1.000000000000000000, -0.000000000000000000, -0.000000000000000000 ) ) ;
#44951=DIRECTION ( 'NONE',  ( -1.000000000000000000, 0.000000000000000000, -0.000000000000000000 ) ) ;
#44954=CARTESIAN_POINT ( 'NONE',  ( -10.00000000000000000, 0.000000000000000000, 0.000000000000000000 ) ) ;
#44955=EDGE_LOOP ( 'NONE', ( #1438, #40314, #8315, #23022 ) ) ;
#44964=CIRCLE ( 'NONE', #29338, 37.49900000000001654 ) ;
#44967=LINE ( 'NONE', #45209, #6485 ) ;
#44968=EDGE_CURVE ( 'NONE', #6290, #48430, #44290, .T. ) ;
#44969=AXIS2_PLACEMENT_3D ( 'NONE', #36807, #7914, #6958 ) ;
#44997=AXIS2_PLACEMENT_3D ( 'NONE', #45355, #9133, #23567 ) ;
#45020=CARTESIAN_POINT ( 'NONE',  ( 10.00000000000000000, -35.47612816024539484, 22.48208911017487921 ) ) ;
#45026=CARTESIAN_POINT ( 'NONE',  ( 10.00000000000000000, -29.81001611430991360, -22.74946021919165418 ) ) ;
#45036=AXIS2_PLACEMENT_3D ( 'NONE', #7139, #14496, #36745 ) ;
#45040=DIRECTION ( 'NONE',  ( 0.000000000000000000, 0.000000000000000000, 1.000000000000000000 ) ) ;
#45044=VECTOR ( 'NONE', #9841, 1000.000000000000000 ) ;
#45046=ORIENTED_EDGE ( 'NONE', *, *, #16160, .F. ) ;
#45078=ORIENTED_EDGE ( 'NONE', *, *, #26687, .F. ) ;
#45100=ORIENTED_EDGE ( 'NONE', *, *, #14867, .T. ) ;
#45109=EDGE_CURVE ( 'NONE', #5369, #44237, #30836, .T. ) ;
#45113=AXIS2_PLACEMENT_3D ( 'NONE', #29493, #25567, #29728 ) ;
#45116=DIRECTION ( 'NONE',  ( 1.000000000000000000, 0.000000000000000000, 0.000000000000000000 ) ) ;
#45119=ORIENTED_EDGE ( 'NONE', *, *, #10278, .F. ) ;
#45128=ORIENTED_EDGE ( 'NONE', *, *, #35159, .T. ) ;
#45136=DIRECTION ( 'NONE',  ( 0.000000000000000000, -0.1564344650402380854, 0.9876883405951365491 ) ) ;
#45145=CIRCLE ( 'NONE', #40471, 15.99999999999999822 ) ;
#45148=CARTESIAN_POINT ( 'NONE',  ( 10.00000000000000000, 0.000000000000000000, 0.000000000000000000 ) ) ;
#45156=CARTESIAN_POINT ( 'NONE',  ( 0.000000000000000000, 10.41901085202135491, -40.68715046381917944 ) ) ;
#45176=LINE ( 'NONE', #38306, #46500 ) ;
#45189=VERTEX_POINT ( 'NONE', #40859 ) ;
#45195=CARTESIAN_POINT ( 'NONE',  ( 0.000000000000000000, 0.000000000000000000, 0.000000000000000000 ) ) ;
#45201=CIRCLE ( 'NONE', #38956, 42.00000000000000000 ) ;
#45203=ORIENTED_EDGE ( 'NONE', *, *, #32868, .F. ) ;
#45209=CARTESIAN_POINT ( 'NONE',  ( 10.00000000000000000, 25.88420570971438650, -27.13269053701069566 ) ) ;
#45210=EDGE_CURVE ( 'NONE', #34499, #20591, #5860, .T. ) ;
#45214=DIRECTION ( 'NONE',  ( 0.000000000000000000, 0.1564344650402313408, -0.9876883405951376593 ) ) ;
#45221=SHAPE_REPRESENTATION_RELATIONSHIP ( 'NONE' , 'NONE' ,  #9091, #37976 ) ;
#45224=CIRCLE ( 'NONE', #10843, 15.99999999999999822 ) ;
#45236=EDGE_CURVE ( 'NONE', #8389, #42455, #44941, .T. ) ;
#45237=CARTESIAN_POINT ( 'NONE',  ( 4.999999999999999112, 38.55633173627034438, -16.65560815589369881 ) ) ;
#45242=CYLINDRICAL_SURFACE ( 'NONE', #26003, 16.00000000000000000 ) ;
#45244=ORIENTED_EDGE ( 'NONE', *, *, #12459, .F. ) ;
#45248=EDGE_CURVE ( 'NONE', #3496, #37278, #1193, .T. ) ;
#45255=CYLINDRICAL_SURFACE ( 'NONE', #1916, 16.00000000000000000 ) ;
#45260=CARTESIAN_POINT ( 'NONE',  ( 10.00000000000000000, -21.32104025579091910, -30.84782396557241313 ) ) ;
#45266=DIRECTION ( 'NONE',  ( -1.000000000000000000, 0.000000000000000000, 0.000000000000000000 ) ) ;
#45273=CARTESIAN_POINT ( 'NONE',  ( 10.00000000000000000, -41.81611651403859042, -3.925862922256606602 ) ) ;
#45287=AXIS2_PLACEMENT_3D ( 'NONE', #32696, #43723, #28793 ) ;
#45295=ORIENTED_EDGE ( 'NONE', *, *, #26568, .F. ) ;
#45303=DIRECTION ( 'NONE',  ( 0.000000000000000000, 0.000000000000000000, -1.000000000000000000 ) ) ;
#45310=DIRECTION ( 'NONE',  ( -1.000000000000000000, 0.000000000000000000, -0.000000000000000000 ) ) ;
#45314=ORIENTED_EDGE ( 'NONE', *, *, #42573, .T. ) ;
#45319=EDGE_CURVE ( 'NONE', #42455, #43390, #31804, .T. ) ;
#45320=DIRECTION ( 'NONE',  ( 0.000000000000000000, -0.8910065241883627918, -0.4539904997395568520 ) ) ;
#45325=CARTESIAN_POINT ( 'NONE',  ( 10.00000000000000000, 5.202137450156907761, -37.22597642581151689 ) ) ;
#45327=DIRECTION ( 'NONE',  ( 0.000000000000000000, 0.000000000000000000, -1.000000000000000000 ) ) ;
#45333=FACE_OUTER_BOUND ( 'NONE', #22424, .T. ) ;
#45345=CARTESIAN_POINT ( 'NONE',  ( 10.00000000000000000, 0.000000000000000000, 0.000000000000000000 ) ) ;
#45348=AXIS2_PLACEMENT_3D ( 'NONE', #126, #28797, #36383 ) ;
#45355=CARTESIAN_POINT ( 'NONE',  ( 0.000000000000000000, 22.64427369931212297, -30.00120703465181293 ) ) ;
#45357=VECTOR ( 'NONE', #22302, 1000.000000000000000 ) ;
#45359=DIRECTION ( 'NONE',  ( -1.000000000000000000, 0.000000000000000000, -0.000000000000000000 ) ) ;
#45367=EDGE_CURVE ( 'NONE', #1493, #25865, #11385, .T. ) ;
#45372=AXIS2_PLACEMENT_3D ( 'NONE', #9071, #2203, #35007 ) ;
#45375=DIRECTION ( 'NONE',  ( 0.000000000000000000, 0.9876883405951372152, 0.1564344650402346160 ) ) ;
#45378=LINE ( 'NONE', #15302, #37993 ) ;
#45389=AXIS2_PLACEMENT_3D ( 'NONE', #4735, #46101, #13291 ) ;
#45401=ORIENTED_EDGE ( 'NONE', *, *, #42944, .F. ) ;
#45403=EDGE_LOOP ( 'NONE', ( #47430, #2578, #17744, #36903 ) ) ;
#45411=ORIENTED_EDGE ( 'NONE', *, *, #28363, .F. ) ;
#45421=CARTESIAN_POINT ( 'NONE',  ( 0.000000000000000000, 37.58145647212453611, 16.68533520207917675 ) ) ;
#45424=EDGE_CURVE ( 'NONE', #8618, #13986, #13659, .T. ) ;
#45431=VERTEX_POINT ( 'NONE', #22391 ) ;
#45432=VERTEX_POINT ( 'NONE', #28592 ) ;
#45454=ORIENTED_EDGE ( 'NONE', *, *, #29102, .T. ) ;
#45456=AXIS2_PLACEMENT_3D ( 'NONE', #28514, #7908, #15025 ) ;
#45457=FACE_OUTER_BOUND ( 'NONE', #21519, .T. ) ;
#45458=VECTOR ( 'NONE', #3448, 1000.000000000000000 ) ;
#45459=VERTEX_POINT ( 'NONE', #48323 ) ;
#45482=ORIENTED_EDGE ( 'NONE', *, *, #5378, .F. ) ;
#45483=EDGE_CURVE ( 'NONE', #18791, #46639, #23579, .T. ) ;
#45485=ORIENTED_EDGE ( 'NONE', *, *, #37871, .F. ) ;
#45499=DIRECTION ( 'NONE',  ( -1.000000000000000000, 0.000000000000000000, 0.000000000000000000 ) ) ;
#45505=DIRECTION ( 'NONE',  ( -1.000000000000000000, 0.000000000000000000, 0.000000000000000000 ) ) ;
#45517=ADVANCED_FACE ( 'NONE', ( #8417 ), #27271, .T. ) ;
#45525=DIRECTION ( 'NONE',  ( 1.000000000000000000, 0.000000000000000000, 0.000000000000000000 ) ) ;
#45529=CYLINDRICAL_SURFACE ( 'NONE', #37705, 16.00000000000000355 ) ;
#45536=VERTEX_POINT ( 'NONE', #38523 ) ;
#45548=CARTESIAN_POINT ( 'NONE',  ( 10.00000000000000000, 37.58145647212453611, 16.68533520207917675 ) ) ;
#45549=VERTEX_POINT ( 'NONE', #23344 ) ;
#45565=DIRECTION ( 'NONE',  ( -1.000000000000000000, -0.000000000000000000, 0.000000000000000000 ) ) ;
#45566=AXIS2_PLACEMENT_3D ( 'NONE', #29301, #2605, #32720 ) ;
#45569=AXIS2_PLACEMENT_3D ( 'NONE', #37905, #19291, #42062 ) ;
#45583=DIRECTION ( 'NONE',  ( 0.000000000000000000, 0.000000000000000000, 1.000000000000000000 ) ) ;
#45584=VERTEX_POINT ( 'NONE', #4989 ) ;
#45591=CARTESIAN_POINT ( 'NONE',  ( 0.000000000000000000, 0.000000000000000000, 0.000000000000000000 ) ) ;
#45593=CARTESIAN_POINT ( 'NONE',  ( 10.00000000000000000, 0.000000000000000000, 0.000000000000000000 ) ) ;
#45598=AXIS2_PLACEMENT_3D ( 'NONE', #41465, #33863, #18692 ) ;
#45610=DIRECTION ( 'NONE',  ( 0.000000000000000000, 0.000000000000000000, 1.000000000000000000 ) ) ;
#45611=CARTESIAN_POINT ( 'NONE',  ( 0.000000000000000000, 4.992566952384984269, 37.16516213103279398 ) ) ;
#45618=CARTESIAN_POINT ( 'NONE',  ( 0.000000000000000000, 31.52238457039637609, -27.75498641678709788 ) ) ;
#45633=EDGE_LOOP ( 'NONE', ( #38542, #43087, #27890, #40981 ) ) ;
#45640=DIRECTION ( 'NONE',  ( 0.000000000000000000, 0.000000000000000000, 1.000000000000000000 ) ) ;
#45666=EDGE_CURVE ( 'NONE', #20, #46331, #42648, .T. ) ;
#45689=CARTESIAN_POINT ( 'NONE',  ( 10.00000000000000000, 30.80686688397010542, 21.53537804866092387 ) ) ;
#45691=EDGE_CURVE ( 'NONE', #22548, #20595, #16735, .T. ) ;
#45699=SURFACE_STYLE_FILL_AREA ( #22468 ) ;
#45706=ORIENTED_EDGE ( 'NONE', *, *, #39943, .T. ) ;
#45715=CARTESIAN_POINT ( 'NONE',  ( 10.00000000000000000, 0.000000000000000000, 0.000000000000000000 ) ) ;
#45719=ORIENTED_EDGE ( 'NONE', *, *, #23214, .T. ) ;
#45724=VERTEX_POINT ( 'NONE', #24799 ) ;
#45734=CIRCLE ( 'NONE', #48101, 37.49900000000000944 ) ;
#45757=AXIS2_PLACEMENT_3D ( 'NONE', #30942, #23569, #15512 ) ;
#45759=CARTESIAN_POINT ( 'NONE',  ( 0.000000000000000000, -22.64427369931191336, 30.00120703465197280 ) ) ;
#45761=EDGE_CURVE ( 'NONE', #28089, #34957, #29328, .T. ) ;
#45768=ORIENTED_EDGE ( 'NONE', *, *, #17413, .F. ) ;
#45770=CYLINDRICAL_SURFACE ( 'NONE', #47955, 42.00000000000000000 ) ;
#45774=AXIS2_PLACEMENT_3D ( 'NONE', #43561, #40376, #3381 ) ;
#45784=AXIS2_PLACEMENT_3D ( 'NONE', #47438, #35703, #28346 ) ;
#45787=VECTOR ( 'NONE', #26725, 1000.000000000000000 ) ;
#45795=CARTESIAN_POINT ( 'NONE',  ( 10.00000000000000000, -22.64427369931191336, 30.00120703465197280 ) ) ;
#45797=DIRECTION ( 'NONE',  ( 0.000000000000000000, 0.000000000000000000, 1.000000000000000000 ) ) ;
#45800=LINE ( 'NONE', #16183, #4739 ) ;
#45803=CARTESIAN_POINT ( 'NONE',  ( 0.000000000000000000, -39.04073710021356192, 15.48615015657568073 ) ) ;
#45818=CARTESIAN_POINT ( 'NONE',  ( 0.000000000000000000, 31.52238457039599595, 27.75498641678753842 ) ) ;
#45819=CARTESIAN_POINT ( 'NONE',  ( 0.000000000000000000, -35.47612816024506088, -22.48208911017539435 ) ) ;
#45820=EDGE_CURVE ( 'NONE', #36993, #23918, #7457, .T. ) ;
#45822=EDGE_CURVE ( 'NONE', #41107, #28690, #22336, .T. ) ;
#45825=CARTESIAN_POINT ( 'NONE',  ( 5.000000000000000000, 36.13751322684419165, 21.40280677340384585 ) ) ;
#45834=ADVANCED_FACE ( 'NONE', ( #39978 ), #47769, .T. ) ;
#45839=CARTESIAN_POINT ( 'NONE',  ( 0.000000000000000000, -5.202137450156129717, -37.22597642581163768 ) ) ;
#45847=EDGE_CURVE ( 'NONE', #9112, #7054, #38741, .T. ) ;
#45855=EDGE_CURVE ( 'NONE', #9305, #15480, #44836, .T. ) ;
#45856=CIRCLE ( 'NONE', #3630, 42.00000000000000000 ) ;
#45873=DIRECTION ( 'NONE',  ( -1.000000000000000000, -0.000000000000000000, -0.000000000000000000 ) ) ;
#45890=AXIS2_PLACEMENT_3D ( 'NONE', #15047, #34587, #45375 ) ;
#45892=ORIENTED_EDGE ( 'NONE', *, *, #26537, .T. ) ;
#45893=ADVANCED_FACE ( 'NONE', ( #3721 ), #29662, .T. ) ;
#45897=VECTOR ( 'NONE', #3289, 1000.000000000000000 ) ;
#45899=ORIENTED_EDGE ( 'NONE', *, *, #34019, .F. ) ;
#45912=LINE ( 'NONE', #12862, #43896 ) ;
#45919=EDGE_CURVE ( 'NONE', #6623, #6273, #37177, .T. ) ;
#45922=DIRECTION ( 'NONE',  ( 0.000000000000000000, 0.1564344650402244852, 0.9876883405951387696 ) ) ;
#45932=ORIENTED_EDGE ( 'NONE', *, *, #16473, .T. ) ;
#45933=DIRECTION ( 'NONE',  ( 0.000000000000000000, 0.1564344650402312298, -0.9876883405951375483 ) ) ;
#45946=EDGE_CURVE ( 'NONE', #9070, #27388, #16199, .T. ) ;
#45961=ORIENTED_EDGE ( 'NONE', *, *, #14978, .T. ) ;
#45981=VECTOR ( 'NONE', #6292, 1000.000000000000000 ) ;
#45982=ADVANCED_FACE ( 'NONE', ( #761 ), #23049, .T. ) ;
#45992=DIRECTION ( 'NONE',  ( 0.000000000000000000, 0.000000000000000000, 1.000000000000000000 ) ) ;
#45997=EDGE_CURVE ( 'NONE', #33539, #15162, #13746, .T. ) ;
#46002=CYLINDRICAL_SURFACE ( 'NONE', #17638, 42.00000000000000000 ) ;
#46003=EDGE_LOOP ( 'NONE', ( #26704, #38700, #9656, #45100 ) ) ;
#46008=ORIENTED_EDGE ( 'NONE', *, *, #2875, .T. ) ;
#46018=ORIENTED_EDGE ( 'NONE', *, *, #19191, .T. ) ;
#46023=ORIENTED_EDGE ( 'NONE', *, *, #14978, .F. ) ;
#46042=CARTESIAN_POINT ( 'NONE',  ( 0.000000000000000000, 27.05870788708231700, 26.08949754953034272 ) ) ;
#46043=DIRECTION ( 'NONE',  ( 0.000000000000000000, 0.000000000000000000, 1.000000000000000000 ) ) ;
#46056=DIRECTION ( 'NONE',  ( -1.000000000000000000, 0.000000000000000000, 0.000000000000000000 ) ) ;
#46072=AXIS2_PLACEMENT_3D ( 'NONE', #26481, #8583, #3963 ) ;
#46075=AXIS2_PLACEMENT_3D ( 'NONE', #31271, #42521, #46911 ) ;
#46085=EDGE_CURVE ( 'NONE', #41024, #1214, #35022, .T. ) ;
#46092=EDGE_CURVE ( 'NONE', #30519, #8511, #6718, .T. ) ;
#46093=LINE ( 'NONE', #12560, #10927 ) ;
#46094=ORIENTED_EDGE ( 'NONE', *, *, #36424, .T. ) ;
#46095=CARTESIAN_POINT ( 'NONE',  ( 0.000000000000000000, -16.45098606841149902, 33.79645857604508308 ) ) ;
#46099=CARTESIAN_POINT ( 'NONE',  ( 10.00000000000000000, 16.45098606841126454, 33.79645857604518966 ) ) ;
#46101=DIRECTION ( 'NONE',  ( 1.000000000000000000, 0.000000000000000000, 0.000000000000000000 ) ) ;
#46121=DIRECTION ( 'NONE',  ( 0.000000000000000000, 0.000000000000000000, 1.000000000000000000 ) ) ;
#46124=CARTESIAN_POINT ( 'NONE',  ( 10.00000000000000000, 22.64427369931169309, 30.00120703465213623 ) ) ;
#46128=ORIENTED_EDGE ( 'NONE', *, *, #28888, .F. ) ;
#46141=DIRECTION ( 'NONE',  ( -1.000000000000000000, 0.000000000000000000, 0.000000000000000000 ) ) ;
#46148=VECTOR ( 'NONE', #13840, 1000.000000000000000 ) ;
#46149=DIRECTION ( 'NONE',  ( 0.000000000000000000, 0.000000000000000000, -1.000000000000000000 ) ) ;
#46150=VERTEX_POINT ( 'NONE', #39684 ) ;
#46151=ORIENTED_EDGE ( 'NONE', *, *, #38248, .T. ) ;
#46168=DIRECTION ( 'NONE',  ( -1.000000000000000000, 0.000000000000000000, -0.000000000000000000 ) ) ;
#46172=DIRECTION ( 'NONE',  ( -1.000000000000000000, -0.000000000000000000, -0.000000000000000000 ) ) ;
#46175=DIRECTION ( 'NONE',  ( -1.000000000000000000, -0.000000000000000000, -0.000000000000000000 ) ) ;
#46177=VECTOR ( 'NONE', #23550, 1000.000000000000000 ) ;
#46178=ORIENTED_EDGE ( 'NONE', *, *, #39580, .T. ) ;
#46188=VERTEX_POINT ( 'NONE', #17141 ) ;
#46202=VERTEX_POINT ( 'NONE', #28875 ) ;
#46203=DIRECTION ( 'NONE',  ( -1.000000000000000000, -0.000000000000000000, 0.000000000000000000 ) ) ;
#46216=ORIENTED_EDGE ( 'NONE', *, *, #21667, .T. ) ;
#46221=FACE_OUTER_BOUND ( 'NONE', #175, .T. ) ;
#46225=EDGE_LOOP ( 'NONE', ( #27441, #27419, #17004, #11825 ) ) ;
#46232=CARTESIAN_POINT ( 'NONE',  ( 0.000000000000000000, 36.88895765772642221, -6.736453364083161865 ) ) ;
#46245=EDGE_CURVE ( 'NONE', #24728, #47328, #18346, .T. ) ;
#46253=ORIENTED_EDGE ( 'NONE', *, *, #27703, .T. ) ;
#46260=DIRECTION ( 'NONE',  ( 0.000000000000000000, -0.1564344650402170744, -0.9876883405951398798 ) ) ;
#46266=CYLINDRICAL_SURFACE ( 'NONE', #2779, 16.00000000000000000 ) ;
#46273=DIRECTION ( 'NONE',  ( -1.000000000000000000, 0.000000000000000000, 0.000000000000000000 ) ) ;
#46274=EDGE_LOOP ( 'NONE', ( #13783, #3930, #13377, #23685 ) ) ;
#46283=DIRECTION ( 'NONE',  ( -1.000000000000000000, 0.000000000000000000, 0.000000000000000000 ) ) ;
#46301=CARTESIAN_POINT ( 'NONE',  ( -10.00000000000000000, 0.000000000000000000, 0.000000000000000000 ) ) ;
#46327=ADVANCED_FACE ( 'NONE', ( #14196 ), #10528, .T. ) ;
#46331=VERTEX_POINT ( 'NONE', #37435 ) ;
#46345=CARTESIAN_POINT ( 'NONE',  ( 0.000000000000000000, 10.96151621346540317, -35.95386929396244113 ) ) ;
#46347=CARTESIAN_POINT ( 'NONE',  ( 10.00000000000000000, -26.08949754953005495, -27.05870788708258701 ) ) ;
#46348=CIRCLE ( 'NONE', #32300, 37.49900000000000944 ) ;
#46349=CYLINDRICAL_SURFACE ( 'NONE', #33007, 37.49900000000000233 ) ;
#46353=CARTESIAN_POINT ( 'NONE',  ( 10.00000000000000000, 27.05870788708267582, -26.08949754952995903 ) ) ;
#46356=EDGE_CURVE ( 'NONE', #5626, #41024, #43485, .T. ) ;
#46377=CIRCLE ( 'NONE', #38557, 15.99999999999999822 ) ;
#46391=ORIENTED_EDGE ( 'NONE', *, *, #37028, .F. ) ;
#46392=AXIS2_PLACEMENT_3D ( 'NONE', #21096, #47308, #43630 ) ;
#46400=AXIS2_PLACEMENT_3D ( 'NONE', #44623, #10858, #14042 ) ;
#46402=EDGE_LOOP ( 'NONE', ( #4122, #26052, #28847, #8613 ) ) ;
#46403=DIRECTION ( 'NONE',  ( 0.000000000000000000, -1.000000000000000000, -1.047444401652940007E-14 ) ) ;
#46410=DIRECTION ( 'NONE',  ( 0.000000000000000000, 0.000000000000000000, -1.000000000000000000 ) ) ;
#46435=ORIENTED_EDGE ( 'NONE', *, *, #44488, .F. ) ;
#46453=ORIENTED_EDGE ( 'NONE', *, *, #41609, .F. ) ;
#46454=FACE_OUTER_BOUND ( 'NONE', #18168, .T. ) ;
#46480=VECTOR ( 'NONE', #40798, 1000.000000000000000 ) ;
#46491=VERTEX_POINT ( 'NONE', #46232 ) ;
#46493=EDGE_CURVE ( 'NONE', #22815, #31993, #6756, .T. ) ;
#46500=VECTOR ( 'NONE', #8444, 1000.000000000000000 ) ;
#46521=DIRECTION ( 'NONE',  ( 0.000000000000000000, 0.9510565162951544194, -0.3090169943749447867 ) ) ;
#46524=LINE ( 'NONE', #8814, #27212 ) ;
#46526=ORIENTED_EDGE ( 'NONE', *, *, #36015, .F. ) ;
#46528=VECTOR ( 'NONE', #21651, 1000.000000000000000 ) ;
#46540=FACE_OUTER_BOUND ( 'NONE', #16244, .T. ) ;
#46543=CARTESIAN_POINT ( 'NONE',  ( 10.00000000000000000, 27.05870788708231700, 26.08949754953034272 ) ) ;
#46549=EDGE_CURVE ( 'NONE', #12539, #23303, #19257, .T. ) ;
#46553=CARTESIAN_POINT ( 'NONE',  ( 10.00000000000000000, 16.65560815589411092, 38.55633173627015964 ) ) ;
#46557=VECTOR ( 'NONE', #45266, 1000.000000000000000 ) ;
#46562=CARTESIAN_POINT ( 'NONE',  ( 10.00000000000000000, 33.00180498840046539, 17.80606268964551120 ) ) ;
#46563=CARTESIAN_POINT ( 'NONE',  ( 10.00000000000000000, -30.80686688396994910, -21.53537804866113703 ) ) ;
#46566=CIRCLE ( 'NONE', #30150, 42.00000000000000000 ) ;
#46572=CARTESIAN_POINT ( 'NONE',  ( 0.000000000000000000, 0.000000000000000000, 0.000000000000000000 ) ) ;
#46596=CIRCLE ( 'NONE', #27840, 42.00000000000000000 ) ;
#46607=CARTESIAN_POINT ( 'NONE',  ( 10.00000000000000000, -29.81001611430991360, -22.74946021919165418 ) ) ;
#46610=EDGE_CURVE ( 'NONE', #31375, #36483, #35716, .T. ) ;
#46619=DIRECTION ( 'NONE',  ( -1.000000000000000000, 0.000000000000000000, 0.000000000000000000 ) ) ;
#46629=VERTEX_POINT ( 'NONE', #5854 ) ;
#46632=CARTESIAN_POINT ( 'NONE',  ( 0.000000000000000000, 0.000000000000000000, 0.000000000000000000 ) ) ;
#46639=VERTEX_POINT ( 'NONE', #47900 ) ;
#46648=DIRECTION ( 'NONE',  ( -1.000000000000000000, 0.000000000000000000, 0.000000000000000000 ) ) ;
#46655=LINE ( 'NONE', #47117, #4837 ) ;
#46672=VERTEX_POINT ( 'NONE', #43999 ) ;
#46677=ORIENTED_EDGE ( 'NONE', *, *, #28693, .T. ) ;
#46681=AXIS2_PLACEMENT_3D ( 'NONE', #15805, #393, #4320 ) ;
#46696=ORIENTED_EDGE ( 'NONE', *, *, #30515, .T. ) ;
#46703=CARTESIAN_POINT ( 'NONE',  ( 10.00000000000000000, -35.92658777277502935, -10.74501242461320594 ) ) ;
#46712=DIRECTION ( 'NONE',  ( -1.000000000000000000, 0.000000000000000000, -0.000000000000000000 ) ) ;
#46718=DIRECTION ( 'NONE',  ( -1.000000000000000000, 0.000000000000000000, 0.000000000000000000 ) ) ;
#46720=DIRECTION ( 'NONE',  ( 0.000000000000000000, -0.9876883405951393247, 0.1564344650402205161 ) ) ;
#46745=CARTESIAN_POINT ( 'NONE',  ( 0.000000000000000000, 0.000000000000000000, 0.000000000000000000 ) ) ;
#46760=ADVANCED_FACE ( 'NONE', ( #7760 ), #33699, .T. ) ;
#46771=ORIENTED_EDGE ( 'NONE', *, *, #44195, .T. ) ;
#46810=CIRCLE ( 'NONE', #42127, 16.00000000000000000 ) ;
#46815=LINE ( 'NONE', #43616, #45044 ) ;
#46818=EDGE_LOOP ( 'NONE', ( #31507, #6699, #34275, #190 ) ) ;
#46820=ORIENTED_EDGE ( 'NONE', *, *, #9565, .T. ) ;
#46822=EDGE_CURVE ( 'NONE', #2634, #36936, #11478, .T. ) ;
#46823=CARTESIAN_POINT ( 'NONE',  ( 0.000000000000000000, 33.79645857604513992, 16.45098606841138178 ) ) ;
#46829=VERTEX_POINT ( 'NONE', #19479 ) ;
#46838=DIRECTION ( 'NONE',  ( -1.000000000000000000, -0.000000000000000000, -0.000000000000000000 ) ) ;
#46851=ORIENTED_EDGE ( 'NONE', *, *, #19191, .F. ) ;
#46868=ORIENTED_EDGE ( 'NONE', *, *, #15325, .T. ) ;
#46870=EDGE_CURVE ( 'NONE', #18356, #3376, #11197, .T. ) ;
#46877=AXIS2_PLACEMENT_3D ( 'NONE', #6993, #21917, #33187 ) ;
#46886=LINE ( 'NONE', #47372, #37718 ) ;
#46888=PRODUCT_DEFINITION ( 'UNKNOWN', '', #17834, #11018 ) ;
#46895=CYLINDRICAL_SURFACE ( 'NONE', #19014, 16.00000000000000000 ) ;
#46911=DIRECTION ( 'NONE',  ( 0.000000000000000000, 0.000000000000000000, 1.000000000000000000 ) ) ;
#46915=ORIENTED_EDGE ( 'NONE', *, *, #24109, .F. ) ;
#46916=AXIS2_PLACEMENT_3D ( 'NONE', #22313, #29155, #3702 ) ;
#46920=VERTEX_POINT ( 'NONE', #27104 ) ;
#46924=EDGE_CURVE ( 'NONE', #33911, #19660, #44309, .T. ) ;
#46936=LINE ( 'NONE', #43025, #39362 ) ;
#46939=DIRECTION ( 'NONE',  ( -1.000000000000000000, 0.000000000000000000, 0.000000000000000000 ) ) ;
#46958=CIRCLE ( 'NONE', #26618, 16.00000000000000000 ) ;
#46966=EDGE_CURVE ( 'NONE', #34876, #32798, #36504, .T. ) ;
#46976=AXIS2_PLACEMENT_3D ( 'NONE', #29088, #44270, #32294 ) ;
#46990=CARTESIAN_POINT ( 'NONE',  ( 0.000000000000000000, -35.47612816024539484, 22.48208911017487921 ) ) ;
#46993=ORIENTED_EDGE ( 'NONE', *, *, #46966, .T. ) ;
#46997=VERTEX_POINT ( 'NONE', #24374 ) ;
#47002=ORIENTED_EDGE ( 'NONE', *, *, #30409, .F. ) ;
#47004=DIRECTION ( 'NONE',  ( -1.000000000000000000, 0.000000000000000000, 0.000000000000000000 ) ) ;
#47018=ORIENTED_EDGE ( 'NONE', *, *, #17208, .F. ) ;
#47025=ADVANCED_FACE ( 'NONE', ( #23649 ), #1392, .T. ) ;
#47040=CARTESIAN_POINT ( 'NONE',  ( 5.000000000000000000, -22.48208911017525580, 35.47612816024516036 ) ) ;
#47068=DIRECTION ( 'NONE',  ( -1.000000000000000000, -0.000000000000000000, -0.000000000000000000 ) ) ;
#47071=FACE_OUTER_BOUND ( 'NONE', #29930, .T. ) ;
#47078=ORIENTED_EDGE ( 'NONE', *, *, #38242, .T. ) ;
#47091=EDGE_CURVE ( 'NONE', #19660, #34492, #21175, .T. ) ;
#47092=ORIENTED_EDGE ( 'NONE', *, *, #36950, .T. ) ;
#47104=AXIS2_PLACEMENT_3D ( 'NONE', #8461, #23386, #27318 ) ;
#47108=CIRCLE ( 'NONE', #13498, 16.00000000000000000 ) ;
#47111=LINE ( 'NONE', #47368, #21221 ) ;
#47116=FACE_OUTER_BOUND ( 'NONE', #38368, .T. ) ;
#47117=CARTESIAN_POINT ( 'NONE',  ( 5.000000000000000000, 27.75498641678742473, 31.52238457039609187 ) ) ;
#47120=ORIENTED_EDGE ( 'NONE', *, *, #21698, .F. ) ;
#47122=CARTESIAN_POINT ( 'NONE',  ( 10.00000000000000000, -39.04073710021333454, -15.48615015657624738 ) ) ;
#47141=ORIENTED_EDGE ( 'NONE', *, *, #42944, .T. ) ;
#47160=FACE_OUTER_BOUND ( 'NONE', #42887, .T. ) ;
#47175=CARTESIAN_POINT ( 'NONE',  ( 10.00000000000000000, -4.992566952384716927, -37.16516213103282951 ) ) ;
#47187=CARTESIAN_POINT ( 'NONE',  ( 10.00000000000000000, -0.6853352020793173072, 37.58145647212453611 ) ) ;
#47217=ORIENTED_EDGE ( 'NONE', *, *, #20053, .F. ) ;
#47221=AXIS2_PLACEMENT_3D ( 'NONE', #35162, #38366, #18843 ) ;
#47234=ORIENTED_EDGE ( 'NONE', *, *, #10271, .T. ) ;
#47238=VERTEX_POINT ( 'NONE', #19201 ) ;
#47239=DIRECTION ( 'NONE',  ( -1.000000000000000000, -0.000000000000000000, -0.000000000000000000 ) ) ;
#47263=EDGE_CURVE ( 'NONE', #6273, #30039, #27127, .T. ) ;
#47265=ORIENTED_EDGE ( 'NONE', *, *, #12577, .T. ) ;
#47266=CIRCLE ( 'NONE', #41786, 16.00000000000000355 ) ;
#47272=AXIS2_PLACEMENT_3D ( 'NONE', #43337, #21043, #39899 ) ;
#47278=CARTESIAN_POINT ( 'NONE',  ( 0.000000000000000000, 37.48860685352291000, 0.8828120875901893649 ) ) ;
#47282=ORIENTED_EDGE ( 'NONE', *, *, #24262, .T. ) ;
#47288=CARTESIAN_POINT ( 'NONE',  ( 4.999999999999999112, -38.55633173627022359, 16.65560815589396526 ) ) ;
#47303=ORIENTED_EDGE ( 'NONE', *, *, #17449, .F. ) ;
#47305=CARTESIAN_POINT ( 'NONE',  ( 10.00000000000000000, 10.74501242461333028, -35.92658777277499382 ) ) ;
#47308=DIRECTION ( 'NONE',  ( -1.000000000000000000, -0.000000000000000000, -0.000000000000000000 ) ) ;
#47315=AXIS2_PLACEMENT_3D ( 'NONE', #33065, #22308, #14958 ) ;
#47318=DIRECTION ( 'NONE',  ( -1.000000000000000000, 0.000000000000000000, 0.000000000000000000 ) ) ;
#47324=DIRECTION ( 'NONE',  ( -1.000000000000000000, -0.000000000000000000, -0.000000000000000000 ) ) ;
#47326=ORIENTED_EDGE ( 'NONE', *, *, #6239, .T. ) ;
#47328=VERTEX_POINT ( 'NONE', #45156 ) ;
#47337=DIRECTION ( 'NONE',  ( -1.000000000000000000, -0.000000000000000000, -0.000000000000000000 ) ) ;
#47350=DIRECTION ( 'NONE',  ( -1.000000000000000000, -0.000000000000000000, -0.000000000000000000 ) ) ;
#47354=AXIS2_PLACEMENT_3D ( 'NONE', #48093, #10894, #44182 ) ;
#47356=CARTESIAN_POINT ( 'NONE',  ( 0.000000000000000000, -40.98264845739743123, -9.188173127307734944 ) ) ;
#47360=VECTOR ( 'NONE', #1504, 1000.000000000000000 ) ;
#47364=ORIENTED_EDGE ( 'NONE', *, *, #14198, .F. ) ;
#47368=CARTESIAN_POINT ( 'NONE',  ( 4.999999999999999112, -21.40280677340345505, -36.13751322684441192 ) ) ;
#47372=CARTESIAN_POINT ( 'NONE',  ( 10.00000000000000000, -10.74501242461308159, 35.92658777277507909 ) ) ;
#47392=VERTEX_POINT ( 'NONE', #1075 ) ;
#47395=EDGE_LOOP ( 'NONE', ( #27795, #6945, #33191, #13132 ) ) ;
#47404=ORIENTED_EDGE ( 'NONE', *, *, #27703, .F. ) ;
#47406=CARTESIAN_POINT ( 'NONE',  ( -10.00000000000000000, 0.000000000000000000, 0.000000000000000000 ) ) ;
#47409=AXIS2_PLACEMENT_3D ( 'NONE', #2384, #24676, #20763 ) ;
#47418=AXIS2_PLACEMENT_3D ( 'NONE', #23404, #41539, #34182 ) ;
#47422=FACE_OUTER_BOUND ( 'NONE', #48020, .T. ) ;
#47428=DIRECTION ( 'NONE',  ( -1.000000000000000000, 0.000000000000000000, -0.000000000000000000 ) ) ;
#47430=ORIENTED_EDGE ( 'NONE', *, *, #5203, .F. ) ;
#47433=DIRECTION ( 'NONE',  ( -1.000000000000000000, -0.000000000000000000, -0.000000000000000000 ) ) ;
#47438=CARTESIAN_POINT ( 'NONE',  ( 0.000000000000000000, 37.22597642581158084, -5.202137450156524068 ) ) ;
#47471=AXIS2_PLACEMENT_3D ( 'NONE', #23409, #12410, #34410 ) ;
#47487=CARTESIAN_POINT ( 'NONE',  ( 0.000000000000000000, -10.41901085202107247, 40.68715046381925049 ) ) ;
#47497=AXIS2_PLACEMENT_3D ( 'NONE', #5782, #13127, #29188 ) ;
#47498=CARTESIAN_POINT ( 'NONE',  ( 0.000000000000000000, 30.80686688397041451, -21.53537804866048688 ) ) ;
#47508=EDGE_LOOP ( 'NONE', ( #12252, #42961, #10641, #9564 ) ) ;
#47525=CARTESIAN_POINT ( 'NONE',  ( 10.00000000000000000, -2.663952781845854378, -41.91543099594820632 ) ) ;
#47526=ORIENTED_EDGE ( 'NONE', *, *, #23068, .F. ) ;
#47530=VERTEX_POINT ( 'NONE', #29121 ) ;
#47541=DIRECTION ( 'NONE',  ( 0.000000000000000000, 0.000000000000000000, 1.000000000000000000 ) ) ;
#47544=ORIENTED_EDGE ( 'NONE', *, *, #36824, .F. ) ;
#47558=ORIENTED_EDGE ( 'NONE', *, *, #34309, .T. ) ;
#47563=ORIENTED_EDGE ( 'NONE', *, *, #29172, .T. ) ;
#47568=CARTESIAN_POINT ( 'NONE',  ( 0.000000000000000000, -0.6853352020787742971, -37.58145647212455032 ) ) ;
#47577=ORIENTED_EDGE ( 'NONE', *, *, #24818, .F. ) ;
#47580=APPLICATION_CONTEXT ( 'automotive_design' ) ;
#47587=DIRECTION ( 'NONE',  ( 0.000000000000000000, 0.8090169943749445647, 0.5877852522924771339 ) ) ;
#47591=EDGE_CURVE ( 'NONE', #39073, #34102, #28730, .T. ) ;
#47598=CARTESIAN_POINT ( 'NONE',  ( 10.00000000000000000, -17.67226234102849958, 33.17418723428301774 ) ) ;
#47601=ADVANCED_FACE ( 'NONE', ( #17864 ), #32788, .T. ) ;
#47608=EDGE_LOOP ( 'NONE', ( #46453, #22900, #41541, #47749 ) ) ;
#47610=ORIENTED_EDGE ( 'NONE', *, *, #45919, .T. ) ;
#47620=EDGE_CURVE ( 'NONE', #37035, #21662, #35821, .T. ) ;
#47641=CARTESIAN_POINT ( 'NONE',  ( 0.000000000000000000, 0.000000000000000000, 0.000000000000000000 ) ) ;
#47647=VERTEX_POINT ( 'NONE', #45273 ) ;
#47649=DIRECTION ( 'NONE',  ( 0.000000000000000000, 0.000000000000000000, 1.000000000000000000 ) ) ;
#47678=VECTOR ( 'NONE', #10072, 1000.000000000000000 ) ;
#47680=DIRECTION ( 'NONE',  ( -1.000000000000000000, -0.000000000000000000, 0.000000000000000000 ) ) ;
#47686=DIRECTION ( 'NONE',  ( -1.000000000000000000, 0.000000000000000000, -0.000000000000000000 ) ) ;
#47688=AXIS2_PLACEMENT_3D ( 'NONE', #27968, #42890, #28190 ) ;
#47690=CIRCLE ( 'NONE', #34420, 16.00000000000000000 ) ;
#47694=VECTOR ( 'NONE', #8570, 1000.000000000000000 ) ;
#47714=VERTEX_POINT ( 'NONE', #946 ) ;
#47717=CIRCLE ( 'NONE', #26632, 42.00000000000000000 ) ;
#47719=UNCERTAINTY_MEASURE_WITH_UNIT (LENGTH_MEASURE( 1.000000000000000082E-05 ), #4820, 'distance_accuracy_value', 'NONE');
#47729=VECTOR ( 'NONE', #39112, 1000.000000000000000 ) ;
#47744=DIRECTION ( 'NONE',  ( 0.000000000000000000, 0.000000000000000000, 1.000000000000000000 ) ) ;
#47746=DIRECTION ( 'NONE',  ( -1.000000000000000000, 0.000000000000000000, 0.000000000000000000 ) ) ;
#47749=ORIENTED_EDGE ( 'NONE', *, *, #16567, .T. ) ;
#47769=CYLINDRICAL_SURFACE ( 'NONE', #11383, 37.49900000000000233 ) ;
#47777=DIRECTION ( 'NONE',  ( -1.000000000000000000, -0.000000000000000000, -0.000000000000000000 ) ) ;
#47781=ADVANCED_FACE ( 'NONE', ( #18516 ), #3332, .T. ) ;
#47791=ADVANCED_FACE ( 'NONE', ( #44949 ), #2859, .T. ) ;
#47803=VECTOR ( 'NONE', #19752, 1000.000000000000000 ) ;
#47830=VECTOR ( 'NONE', #35240, 1000.000000000000000 ) ;
#47867=CARTESIAN_POINT ( 'NONE',  ( 0.000000000000000000, -37.58145647212453611, -0.6853352020794456489 ) ) ;
#47876=VERTEX_POINT ( 'NONE', #7738 ) ;
#47882=DIRECTION ( 'NONE',  ( -1.000000000000000000, -0.000000000000000000, 0.000000000000000000 ) ) ;
#47890=AXIS2_PLACEMENT_3D ( 'NONE', #32312, #31365, #17359 ) ;
#47892=CARTESIAN_POINT ( 'NONE',  ( 0.000000000000000000, 37.16516213103285082, -4.992566952384588141 ) ) ;
#47893=CYLINDRICAL_SURFACE ( 'NONE', #31402, 42.00000000000000000 ) ;
#47897=DIRECTION ( 'NONE',  ( -1.000000000000000000, 0.000000000000000000, 0.000000000000000000 ) ) ;
#47899=AXIS2_PLACEMENT_3D ( 'NONE', #1254, #23035, #34046 ) ;
#47900=CARTESIAN_POINT ( 'NONE',  ( 0.000000000000000000, -36.13751322684434797, 21.40280677340357940 ) ) ;
#47908=EDGE_LOOP ( 'NONE', ( #13521, #29673, #13592, #40990 ) ) ;
#47912=VECTOR ( 'NONE', #20904, 1000.000000000000000 ) ;
#47927=FACE_OUTER_BOUND ( 'NONE', #47508, .T. ) ;
#47928=AXIS2_PLACEMENT_3D ( 'NONE', #27812, #42736, #24126 ) ;
#47929=AXIS2_PLACEMENT_3D ( 'NONE', #5344, #43264, #12935 ) ;
#47937=DIRECTION ( 'NONE',  ( -1.000000000000000000, 0.000000000000000000, 0.000000000000000000 ) ) ;
#47942=AXIS2_PLACEMENT_3D ( 'NONE', #23514, #42130, #998 ) ;
#47955=AXIS2_PLACEMENT_3D ( 'NONE', #37450, #15187, #8063 ) ;
#47967=VERTEX_POINT ( 'NONE', #4792 ) ;
#47984=ORIENTED_EDGE ( 'NONE', *, *, #17936, .F. ) ;
#47985=DIRECTION ( 'NONE',  ( 0.000000000000000000, 0.000000000000000000, 1.000000000000000000 ) ) ;
#47989=ORIENTED_EDGE ( 'NONE', *, *, #20324, .F. ) ;
#48020=EDGE_LOOP ( 'NONE', ( #14605, #37215, #803, #22945 ) ) ;
#48023=DIRECTION ( 'NONE',  ( -1.000000000000000000, 0.000000000000000000, 0.000000000000000000 ) ) ;
#48031=CYLINDRICAL_SURFACE ( 'NONE', #36914, 42.00000000000000000 ) ;
#48034=CYLINDRICAL_SURFACE ( 'NONE', #38975, 37.49900000000000233 ) ;
#48038=ORIENTED_EDGE ( 'NONE', *, *, #12501, .F. ) ;
#48060=CARTESIAN_POINT ( 'NONE',  ( 0.000000000000000000, 0.000000000000000000, 0.000000000000000000 ) ) ;
#48069=FACE_OUTER_BOUND ( 'NONE', #33481, .T. ) ;
#48075=CARTESIAN_POINT ( 'NONE',  ( 5.000000000000000000, -22.48208911017474065, -35.47612816024548721 ) ) ;
#48076=CARTESIAN_POINT ( 'NONE',  ( 10.00000000000000000, -33.00180498840035170, -17.80606268964575278 ) ) ;
#48085=AXIS2_PLACEMENT_3D ( 'NONE', #28716, #47068, #31926 ) ;
#48093=CARTESIAN_POINT ( 'NONE',  ( 10.00000000000000000, 0.000000000000000000, 0.000000000000000000 ) ) ;
#48096=AXIS2_PLACEMENT_3D ( 'NONE', #14288, #34998, #27428 ) ;
#48098=DIRECTION ( 'NONE',  ( 1.000000000000000000, 0.000000000000000000, 0.000000000000000000 ) ) ;
#48101=AXIS2_PLACEMENT_3D ( 'NONE', #9079, #31366, #32082 ) ;
#48112=EDGE_CURVE ( 'NONE', #20812, #2760, #33496, .T. ) ;
#48114=CARTESIAN_POINT ( 'NONE',  ( 10.00000000000000000, -40.68715046381921496, -10.41901085202121457 ) ) ;
#48134=CARTESIAN_POINT ( 'NONE',  ( 10.00000000000000000, -22.74946021919110706, -29.81001611431033282 ) ) ;
#48142=LINE ( 'NONE', #7018, #905 ) ;
#48148=AXIS2_PLACEMENT_3D ( 'NONE', #4463, #541, #23294 ) ;
#48154=ADVANCED_FACE ( 'NONE', ( #14022 ), #48034, .T. ) ;
#48156=ORIENTED_EDGE ( 'NONE', *, *, #27736, .F. ) ;
#48161=DIRECTION ( 'NONE',  ( 0.000000000000000000, 0.000000000000000000, 1.000000000000000000 ) ) ;
#48166=CARTESIAN_POINT ( 'NONE',  ( 10.00000000000000000, 0.000000000000000000, 0.000000000000000000 ) ) ;
#48167=CARTESIAN_POINT ( 'NONE',  ( 0.000000000000000000, 27.75498641678742473, 31.52238457039609187 ) ) ;
#48169=VERTEX_POINT ( 'NONE', #40691 ) ;
#48178=EDGE_CURVE ( 'NONE', #34100, #43888, #45224, .T. ) ;
#48195=VERTEX_POINT ( 'NONE', #41919 ) ;
#48199=ORIENTED_EDGE ( 'NONE', *, *, #42077, .T. ) ;
#48223=CIRCLE ( 'NONE', #38070, 37.49900000000000233 ) ;
#48228=EDGE_CURVE ( 'NONE', #18781, #14446, #13183, .T. ) ;
#48229=CARTESIAN_POINT ( 'NONE',  ( 10.00000000000000000, 33.17418723428307459, 17.67226234102837878 ) ) ;
#48238=ORIENTED_EDGE ( 'NONE', *, *, #4482, .F. ) ;
#48286=EDGE_CURVE ( 'NONE', #45432, #7133, #25658, .T. ) ;
#48307=ORIENTED_EDGE ( 'NONE', *, *, #20722, .T. ) ;
#48308=DIRECTION ( 'NONE',  ( 0.000000000000000000, 0.000000000000000000, 1.000000000000000000 ) ) ;
#48323=CARTESIAN_POINT ( 'NONE',  ( -3.308722450212110699E-21, 16.95692799528845995, 2.500000000000000000 ) ) ;
#48341=ORIENTED_EDGE ( 'NONE', *, *, #30793, .T. ) ;
#48346=ADVANCED_FACE ( 'NONE', ( #9808 ), #24498, .T. ) ;
#48349=CARTESIAN_POINT ( 'NONE',  ( 0.000000000000000000, -21.40280677340345505, -36.13751322684441192 ) ) ;
#48358=VERTEX_POINT ( 'NONE', #16675 ) ;
#48365=DIRECTION ( 'NONE',  ( 1.000000000000000000, 0.000000000000000000, 0.000000000000000000 ) ) ;
#48376=CARTESIAN_POINT ( 'NONE',  ( 10.00000000000000000, 40.98264845739763018, -9.188173127306866306 ) ) ;
#48379=ORIENTED_EDGE ( 'NONE', *, *, #39477, .F. ) ;
#48386=DIRECTION ( 'NONE',  ( -1.000000000000000000, 0.000000000000000000, -0.000000000000000000 ) ) ;
#48387=DIRECTION ( 'NONE',  ( 0.000000000000000000, 0.000000000000000000, 1.000000000000000000 ) ) ;
#48394=EDGE_CURVE ( 'NONE', #29150, #14780, #35079, .T. ) ;
#48429=CARTESIAN_POINT ( 'NONE',  ( 0.000000000000000000, 0.000000000000000000, 0.000000000000000000 ) ) ;
#48430=VERTEX_POINT ( 'NONE', #35757 ) ;
#48441=CIRCLE ( 'NONE', #4709, 12.50000000000000000 ) ;
ENDSEC;
END-ISO-10303-21;
